ISO-10303-21;
HEADER;
/* Generated by software containing ST-Developer
 * from STEP Tools, Inc. (www.steptools.com) 
 */

FILE_DESCRIPTION(
/* description */ (''),
/* implementation_level */ '2;1');

FILE_NAME(
/* name */ 'ISO 7380-1 - M5 x 8 - 10.9.step',
/* time_stamp */ '2026-10-14T18:40:07-07:00',
/* author */ (''),
/* organization */ (''),
/* preprocessor_version */ 'ST-DEVELOPER v20.2',
/* originating_system */ 'Autodesk Translation Framework v15.15.0.0',
/* authorisation */ '');

FILE_SCHEMA (('AUTOMOTIVE_DESIGN { 1 0 10303 214 3 1 1 }'));
ENDSEC;

DATA;
#10=MECHANICAL_DESIGN_GEOMETRIC_PRESENTATION_REPRESENTATION('',(#839),#81040);
#259=SPHERICAL_SURFACE('',#16510,6.05489130434781);
#362=TOROIDAL_SURFACE('',#16478,2.6505,0.2);
#368=B_SPLINE_SURFACE_WITH_KNOTS('',3,3,((#70659,#70660,#70661,#70662,#70663,
#70664,#70665,#70666,#70667,#70668,#70669,#70670,#70671,#70672,#70673,#70674,
#70675,#70676,#70677,#70678,#70679,#70680,#70681,#70682,#70683,#70684,#70685,
#70686,#70687,#70688,#70689,#70690,#70691,#70692,#70693,#70694,#70695,#70696,
#70697,#70698,#70699,#70700,#70701,#70702,#70703,#70704,#70705,#70706,#70707,
#70708,#70709,#70710,#70711,#70712,#70713,#70714,#70715,#70716,#70717,#70718,
#70719,#70720,#70721,#70722,#70723,#70724,#70725,#70726),(#70727,#70728,
#70729,#70730,#70731,#70732,#70733,#70734,#70735,#70736,#70737,#70738,#70739,
#70740,#70741,#70742,#70743,#70744,#70745,#70746,#70747,#70748,#70749,#70750,
#70751,#70752,#70753,#70754,#70755,#70756,#70757,#70758,#70759,#70760,#70761,
#70762,#70763,#70764,#70765,#70766,#70767,#70768,#70769,#70770,#70771,#70772,
#70773,#70774,#70775,#70776,#70777,#70778,#70779,#70780,#70781,#70782,#70783,
#70784,#70785,#70786,#70787,#70788,#70789,#70790,#70791,#70792,#70793,#70794),
(#70795,#70796,#70797,#70798,#70799,#70800,#70801,#70802,#70803,#70804,
#70805,#70806,#70807,#70808,#70809,#70810,#70811,#70812,#70813,#70814,#70815,
#70816,#70817,#70818,#70819,#70820,#70821,#70822,#70823,#70824,#70825,#70826,
#70827,#70828,#70829,#70830,#70831,#70832,#70833,#70834,#70835,#70836,#70837,
#70838,#70839,#70840,#70841,#70842,#70843,#70844,#70845,#70846,#70847,#70848,
#70849,#70850,#70851,#70852,#70853,#70854,#70855,#70856,#70857,#70858,#70859,
#70860,#70861,#70862),(#70863,#70864,#70865,#70866,#70867,#70868,#70869,
#70870,#70871,#70872,#70873,#70874,#70875,#70876,#70877,#70878,#70879,#70880,
#70881,#70882,#70883,#70884,#70885,#70886,#70887,#70888,#70889,#70890,#70891,
#70892,#70893,#70894,#70895,#70896,#70897,#70898,#70899,#70900,#70901,#70902,
#70903,#70904,#70905,#70906,#70907,#70908,#70909,#70910,#70911,#70912,#70913,
#70914,#70915,#70916,#70917,#70918,#70919,#70920,#70921,#70922,#70923,#70924,
#70925,#70926,#70927,#70928,#70929,#70930)),.UNSPECIFIED.,.F.,.F.,.F.,(4,
4),(4,1,1,1,1,1,1,1,1,1,1,1,1,1,1,1,1,1,1,1,1,1,1,1,1,1,1,1,1,1,1,1,1,1,
1,1,1,1,1,1,1,1,1,1,1,1,1,1,1,1,1,1,1,1,1,1,1,1,1,1,1,1,1,1,1,4),(-0.000353530926813993,
0.0529178421063444),(13.6829908479658,14.6799027782905,15.6768147086152,
16.67372663894,17.6706385692647,18.6675504995894,19.6644624299141,20.6613743602388,
21.6582862905635,22.6551982208882,23.652110151213,24.6490220815377,25.6459340118624,
26.6428459421871,27.6397578725118,28.6366698028365,29.6335817331613,30.630493663486,
31.6274055938107,32.6243175241354,33.6212294544601,34.6181413847848,35.6150533151095,
36.6119652454343,37.608877175759,38.6057891060837,39.6027010364084,40.5996129667331,
41.5965248970578,42.5934368273825,43.5903487577073,44.587260688032,45.5841726183567,
46.5810845486814,47.5779964790061,48.5749084093308,49.5718203396556,50.5687322699803,
51.565644200305,52.5625561306297,53.5594680609544,54.5563799912791,55.5532919216039,
56.5502038519286,57.5471157822533,58.544027712578,59.5409396429027,60.5378515732274,
61.5347635035521,62.5316754338769,63.5285873642016,64.5254992945263,65.522411224851,
66.5193231551757,67.5162350855004,68.5131470158251,69.5100589461499,70.5069708764746,
71.5038828067993,72.500794737124,73.4977066674487,74.4946185977734,75.4915305280982,
76.4884424584229,77.4853543887476,78.4822663190723),.UNSPECIFIED.);
#369=B_SPLINE_SURFACE_WITH_KNOTS('',3,3,((#71108,#71109,#71110,#71111,#71112,
#71113,#71114,#71115,#71116,#71117,#71118,#71119,#71120,#71121,#71122,#71123,
#71124,#71125,#71126,#71127,#71128,#71129,#71130,#71131,#71132,#71133,#71134,
#71135,#71136,#71137,#71138,#71139,#71140,#71141,#71142,#71143,#71144,#71145,
#71146,#71147,#71148,#71149,#71150,#71151,#71152,#71153,#71154,#71155,#71156,
#71157,#71158,#71159,#71160,#71161,#71162,#71163,#71164,#71165,#71166,#71167,
#71168,#71169,#71170,#71171,#71172,#71173,#71174,#71175,#71176,#71177),
(#71178,#71179,#71180,#71181,#71182,#71183,#71184,#71185,#71186,#71187,
#71188,#71189,#71190,#71191,#71192,#71193,#71194,#71195,#71196,#71197,#71198,
#71199,#71200,#71201,#71202,#71203,#71204,#71205,#71206,#71207,#71208,#71209,
#71210,#71211,#71212,#71213,#71214,#71215,#71216,#71217,#71218,#71219,#71220,
#71221,#71222,#71223,#71224,#71225,#71226,#71227,#71228,#71229,#71230,#71231,
#71232,#71233,#71234,#71235,#71236,#71237,#71238,#71239,#71240,#71241,#71242,
#71243,#71244,#71245,#71246,#71247),(#71248,#71249,#71250,#71251,#71252,
#71253,#71254,#71255,#71256,#71257,#71258,#71259,#71260,#71261,#71262,#71263,
#71264,#71265,#71266,#71267,#71268,#71269,#71270,#71271,#71272,#71273,#71274,
#71275,#71276,#71277,#71278,#71279,#71280,#71281,#71282,#71283,#71284,#71285,
#71286,#71287,#71288,#71289,#71290,#71291,#71292,#71293,#71294,#71295,#71296,
#71297,#71298,#71299,#71300,#71301,#71302,#71303,#71304,#71305,#71306,#71307,
#71308,#71309,#71310,#71311,#71312,#71313,#71314,#71315,#71316,#71317),
(#71318,#71319,#71320,#71321,#71322,#71323,#71324,#71325,#71326,#71327,
#71328,#71329,#71330,#71331,#71332,#71333,#71334,#71335,#71336,#71337,#71338,
#71339,#71340,#71341,#71342,#71343,#71344,#71345,#71346,#71347,#71348,#71349,
#71350,#71351,#71352,#71353,#71354,#71355,#71356,#71357,#71358,#71359,#71360,
#71361,#71362,#71363,#71364,#71365,#71366,#71367,#71368,#71369,#71370,#71371,
#71372,#71373,#71374,#71375,#71376,#71377,#71378,#71379,#71380,#71381,#71382,
#71383,#71384,#71385,#71386,#71387)),.UNSPECIFIED.,.F.,.F.,.F.,(4,4),(4,
1,1,1,1,1,1,1,1,1,1,1,1,1,1,1,1,1,1,1,1,1,1,1,1,1,1,1,1,1,1,1,1,1,1,1,1,
1,1,1,1,1,1,1,1,1,1,1,1,1,1,1,1,1,1,1,1,1,1,1,1,1,1,1,1,1,1,4),(-0.000420248331794808,
0.0529960453941712),(8.30815772716266,9.30615583345715,10.3041539397516,
11.3021520460461,12.3001501523406,13.2981482586351,14.2961463649296,15.2941444712241,
16.2921425775186,17.2901406838131,18.2881387901076,19.286136896402,20.2841350026965,
21.282133108991,22.2801312152855,23.27812932158,24.2761274278745,25.274125534169,
26.2721236404635,27.270121746758,28.2681198530525,29.2661179593469,30.2641160656414,
31.2621141719359,32.2601122782304,33.2581103845249,34.2561084908194,35.2541065971139,
36.2521047034084,37.2501028097029,38.2481009159974,39.2460990222918,40.2440971285863,
41.2420952348808,42.2400933411753,43.2380914474698,44.2360895537643,45.2340876600588,
46.2320857663533,47.2300838726478,48.2280819789423,49.2260800852367,50.2240781915312,
51.2220762978257,52.2200744041202,53.2180725104147,54.2160706167092,55.2140687230037,
56.2120668292982,57.2100649355927,58.2080630418872,59.2060611481816,60.2040592544761,
61.2020573607706,62.2000554670651,63.1980535733596,64.1960516796541,65.1940497859486,
66.1920478922431,67.1900459985376,68.188044104832,69.1860422111265,70.184040317421,
71.1820384237155,72.18003653001,73.1780346363045,74.176032742599,75.1744510972253),
 .UNSPECIFIED.);
#400=ELLIPSE('',#16473,1.70248048578179,1.37104286127159);
#401=ELLIPSE('',#16476,1.73906534450511,1.41773226323344);
#671=B_SPLINE_CURVE_WITH_KNOTS('',3,(#63350,#63351,#63352,#63353,#63354,
#63355,#63356,#63357,#63358,#63359,#63360,#63361,#63362,#63363,#63364,#63365,
#63366,#63367,#63368,#63369,#63370,#63371,#63372,#63373,#63374),
 .UNSPECIFIED.,.F.,.F.,(4,3,3,3,3,3,3,3,4),(13.9129741038925,14.0298422231105,
14.1472086449743,14.2651865303752,14.2961463649296,14.4010958048174,14.5059075633181,
14.6105993304191,14.6462589634952),.UNSPECIFIED.);
#672=B_SPLINE_CURVE_WITH_KNOTS('',3,(#63381,#63382,#63383,#63384,#63385,
#63386,#63387,#63388,#63389,#63390,#63391,#63392,#63393,#63394,#63395,#63396,
#63397,#63398,#63399,#63400,#63401,#63402,#63403,#63404,#63405,#63406,#63407,
#63408,#63409,#63410,#63411,#63412,#63413,#63414,#63415,#63416,#63417,#63418,
#63419,#63420,#63421,#63422,#63423,#63424,#63425,#63426,#63427,#63428,#63429,
#63430,#63431,#63432,#63433,#63434,#63435,#63436,#63437,#63438,#63439,#63440,
#63441,#63442,#63443,#63444,#63445,#63446,#63447,#63448,#63449,#63450,#63451,
#63452,#63453,#63454,#63455,#63456,#63457,#63458,#63459,#63460,#63461,#63462,
#63463,#63464,#63465,#63466,#63467,#63468,#63469,#63470,#63471,#63472,#63473,
#63474,#63475,#63476,#63477,#63478,#63479,#63480,#63481,#63482,#63483,#63484,
#63485,#63486,#63487,#63488,#63489,#63490,#63491,#63492,#63493,#63494,#63495,
#63496,#63497,#63498,#63499,#63500,#63501,#63502,#63503,#63504,#63505,#63506,
#63507,#63508,#63509,#63510,#63511,#63512,#63513,#63514,#63515,#63516,#63517,
#63518,#63519,#63520,#63521,#63522,#63523,#63524,#63525,#63526,#63527,#63528,
#63529,#63530,#63531,#63532,#63533,#63534),.UNSPECIFIED.,.F.,.F.,(4,2,2,
2,2,2,2,2,2,2,2,2,2,2,2,2,2,2,2,2,2,2,2,2,2,2,2,2,2,2,2,2,2,2,2,2,2,2,2,
2,2,2,2,2,2,2,2,2,2,2,2,2,2,2,2,2,2,2,2,2,2,2,2,2,2,2,2,2,2,2,2,2,2,2,2,
2,4),(-1.0446377710325,-1.03704628547549,-1.02453798687789,-1.01826350873426,
-1.01311579032622,-1.00702642354696,-0.995514059235476,-0.947709045396338,
-0.924297219571578,-0.919031598784486,-0.915866996576101,-0.912809965069769,
-0.908054054162346,-0.891699751850171,-0.852656081935246,-0.829130405191056,
-0.821244412043737,-0.816410755754987,-0.811111499453583,-0.803612062402073,
-0.782533692655034,-0.740280145029678,-0.723993434321385,-0.719119568461197,
-0.716342647433995,-0.713289272412789,-0.7085506531744,-0.692395375008069,
-0.654501639755035,-0.630010212765114,-0.62192770041256,-0.617060352471566,
-0.611789833475927,-0.604456364364755,-0.584839090837727,-0.549030241691706,
-0.52524011923178,-0.519962058444279,-0.516794816200759,-0.513739824324369,
-0.508994048639859,-0.492759522267891,-0.454420062653126,-0.43036810420016,
-0.422327522010767,-0.417466968026783,-0.412189851513824,-0.404820702068184,
-0.384905693225781,-0.347924053046102,-0.325585258048999,-0.320361737346843,
-0.31720570133217,-0.314140036955392,-0.309346210298665,-0.292552484015978,
-0.250772176410963,-0.229940259445161,-0.222307154400807,-0.21703582312508,
-0.211597412191101,-0.203362709041216,-0.1729171418179,-0.129868756538097,
-0.122377385415259,-0.11876359840398,-0.115846445273959,-0.112030289000885,
-0.103382003877119,-0.0905344276180329,-0.0573118511217321,-0.0312820276758043,
-0.0232232548363728,-0.0183617743957572,-0.0134528122916168,-0.00737114375286148,
-0.000589622106167569),.UNSPECIFIED.);
#673=B_SPLINE_CURVE_WITH_KNOTS('',3,(#63535,#63536,#63537,#63538,#63539,
#63540,#63541,#63542,#63543,#63544,#63545,#63546,#63547,#63548,#63549,#63550,
#63551,#63552,#63553,#63554,#63555,#63556,#63557,#63558,#63559,#63560,#63561,
#63562,#63563,#63564,#63565,#63566,#63567,#63568),.UNSPECIFIED.,.F.,.F.,
(4,3,3,3,3,3,3,3,3,3,3,4),(14.6462589634952,14.7508721781997,14.855467446032,
14.96513670233,15.0698705259915,15.1746781067958,15.2796561729127,15.2941444712241,
15.4095566049133,15.5246246005466,15.6391291191132,15.7079632676283),
 .UNSPECIFIED.);
#674=B_SPLINE_CURVE_WITH_KNOTS('',3,(#63572,#63573,#63574,#63575,#63576,
#63577,#63578,#63579,#63580,#63581,#63582,#63583,#63584,#63585,#63586,#63587,
#63588,#63589,#63590),.UNSPECIFIED.,.F.,.F.,(4,3,3,3,3,3,4),(15.1670719793089,
15.2750540414898,15.3832863567034,15.4916502992802,15.6002974383707,15.6768147086152,
15.7079632679489),.UNSPECIFIED.);
#675=B_SPLINE_CURVE_WITH_KNOTS('',3,(#63591,#63592,#63593,#63594,#63595,
#63596,#63597,#63598,#63599,#63600,#63601,#63602,#63603,#63604,#63605,#63606,
#63607,#63608,#63609,#63610,#63611,#63612,#63613,#63614,#63615,#63616,#63617,
#63618,#63619,#63620,#63621,#63622,#63623,#63624,#63625,#63626,#63627,#63628,
#63629,#63630,#63631,#63632,#63633,#63634,#63635,#63636,#63637,#63638,#63639,
#63640,#63641,#63642,#63643,#63644,#63645,#63646,#63647,#63648,#63649,#63650,
#63651,#63652,#63653,#63654,#63655,#63656,#63657,#63658,#63659,#63660,#63661,
#63662,#63663,#63664,#63665,#63666,#63667,#63668,#63669,#63670,#63671,#63672,
#63673,#63674,#63675,#63676,#63677,#63678,#63679,#63680,#63681,#63682,#63683,
#63684,#63685,#63686,#63687,#63688,#63689,#63690,#63691,#63692,#63693,#63694,
#63695,#63696,#63697,#63698,#63699,#63700,#63701,#63702,#63703,#63704,#63705,
#63706,#63707,#63708,#63709,#63710,#63711,#63712,#63713,#63714,#63715,#63716,
#63717,#63718,#63719,#63720,#63721,#63722,#63723,#63724,#63725,#63726,#63727,
#63728,#63729,#63730,#63731,#63732,#63733,#63734,#63735,#63736,#63737,#63738,
#63739,#63740,#63741,#63742,#63743,#63744,#63745,#63746,#63747,#63748,#63749,
#63750),.UNSPECIFIED.,.F.,.F.,(4,3,3,3,3,3,3,3,3,3,3,3,3,3,3,3,3,3,3,3,
3,3,3,3,3,3,3,3,3,3,3,3,3,3,3,3,3,3,3,3,3,3,3,3,3,3,3,3,3,3,3,3,3,4),(15.707963615131,
15.8124359612945,15.9200972960002,16.0242894539373,16.1284191800931,16.2325227207383,
16.3366362816606,16.4408602520689,16.545151109284,16.6496110332327,16.67372663894,
16.778864213501,16.8838480912526,16.9887133793969,17.0935156239512,17.1982900935492,
17.3030720155298,17.4079663194199,17.5129232696531,17.6180617879989,17.6706385692647,
17.7755020962003,17.8802068555822,17.9847868884979,18.0893002417826,18.1937826259329,
18.2982697066287,18.4028670126019,18.5075253033295,18.6123657467834,18.6675504995894,
18.7725356497586,18.8773635727404,18.9820684493609,19.0867076174307,19.191316598296,
19.2959308694104,19.4006553962451,19.5054411151893,19.6104079542118,19.6644624299141,
19.7694496102747,19.8742799638677,19.9789878560323,20.0836304009549,20.1882431156951,
20.2928614737947,20.3975905989735,20.502381213929,20.6073533634062,20.6613743602388,
20.7663251271889,20.8711079876035,20.9295978420031),.UNSPECIFIED.);
#676=B_SPLINE_CURVE_WITH_KNOTS('',3,(#63755,#63756,#63757,#63758,#63759,
#63760,#63761,#63762,#63763,#63764,#63765,#63766,#63767,#63768,#63769,#63770,
#63771,#63772,#63773,#63774,#63775,#63776,#63777,#63778,#63779,#63780,#63781,
#63782,#63783,#63784,#63785,#63786,#63787,#63788,#63789,#63790,#63791,#63792,
#63793,#63794,#63795,#63796,#63797,#63798,#63799,#63800,#63801,#63802,#63803,
#63804,#63805,#63806,#63807,#63808,#63809,#63810,#63811,#63812,#63813,#63814,
#63815,#63816,#63817,#63818,#63819,#63820,#63821,#63822,#63823,#63824,#63825,
#63826,#63827,#63828,#63829,#63830,#63831,#63832,#63833,#63834,#63835,#63836,
#63837,#63838,#63839,#63840,#63841,#63842,#63843,#63844,#63845,#63846,#63847,
#63848,#63849,#63850,#63851,#63852,#63853,#63854,#63855,#63856,#63857,#63858,
#63859,#63860,#63861,#63862,#63863,#63864,#63865,#63866,#63867,#63868,#63869,
#63870,#63871,#63872,#63873,#63874,#63875,#63876,#63877,#63878,#63879,#63880,
#63881,#63882,#63883,#63884,#63885,#63886,#63887,#63888,#63889,#63890,#63891,
#63892,#63893,#63894,#63895,#63896,#63897,#63898,#63899,#63900,#63901,#63902,
#63903,#63904,#63905,#63906,#63907,#63908,#63909,#63910,#63911,#63912,#63913,
#63914,#63915,#63916,#63917,#63918,#63919,#63920,#63921,#63922,#63923,#63924,
#63925,#63926,#63927,#63928,#63929,#63930),.UNSPECIFIED.,.F.,.F.,(4,2,2,
2,2,2,2,2,2,2,2,2,2,2,2,2,2,2,2,2,2,2,2,2,2,2,2,2,2,2,2,2,2,2,2,2,2,2,2,
2,2,2,2,2,2,2,2,2,2,2,2,2,2,2,2,2,2,2,2,2,2,2,2,2,2,2,2,2,2,2,2,2,2,2,2,
2,2,2,2,2,2,2,2,2,2,2,2,4),(-2.30066243309921,-2.29788522881955,-2.25643606788514,
-2.23231053948734,-2.2208999266823,-2.21483093325617,-2.2096837319818,-2.20338903083366,
-2.1911777499165,-2.14674900739685,-2.12948058846704,-2.11893355258783,
-2.11482350548001,-2.11187930309346,-2.10846627257702,-2.10219057115667,
-2.05840092364154,-2.02704354652168,-2.01876903108936,-2.01332541725472,
-2.00806430074847,-2.00047374523046,-1.98008732774641,-1.93781701131553,
-1.92094886167156,-1.9161511089752,-1.91308629977568,-1.91032182121032,
-1.90551082146163,-1.88983129230726,-1.84703778000152,-1.82586403756312,
-1.81835655060216,-1.81305734963996,-1.80758063617246,-1.79913899177679,
-1.76618947679809,-1.74118219640683,-1.72806218298243,-1.71928796613996,
-1.71545022891314,-1.71281098800718,-1.70935143126447,-1.70285538312276,
-1.67234372184617,-1.64306687837895,-1.6253960075888,-1.6183105974177,-1.61308099916133,
-1.60746915538487,-1.59835665179582,-1.55151207626044,-1.53210810751307,
-1.52429543297063,-1.51827267123986,-1.51494888437975,-1.51197840780787,
-1.50768793912509,-1.49664900107833,-1.46185758009169,-1.43502522348022,
-1.42322728284542,-1.41708470102283,-1.41193914795842,-1.40572499446052,
-1.39392685137102,-1.34085313215482,-1.32269209529888,-1.31779470287415,
-1.31470895160789,-1.31196123715408,-1.30724255800787,-1.29262423663785,
-1.25720059021258,-1.22903918551409,-1.22079248669028,-1.21535379123917,
-1.21002615087739,-1.20236320850391,-1.17967750017288,-1.12660399328951,
-1.11976116430686,-1.11627154936574,-1.11336903268774,-1.10940250060461,
-1.09982841549617,-1.08492361178958,-1.0446377710325),.UNSPECIFIED.);
#677=B_SPLINE_CURVE_WITH_KNOTS('',3,(#63932,#63933,#63934,#63935,#63936,
#63937,#63938,#63939,#63940,#63941,#63942,#63943,#63944,#63945,#63946,#63947,
#63948,#63949,#63950,#63951,#63952,#63953,#63954,#63955,#63956,#63957,#63958,
#63959,#63960,#63961,#63962),.UNSPECIFIED.,.F.,.F.,(4,3,3,3,3,3,3,3,3,3,
4),(20.9295978420031,21.034232002129,21.1388202476623,21.2433981166042,
21.3480763020097,21.4528016813787,21.5577233438514,21.6582862905635,21.78148022773,
21.9034423117292,21.9911485747748),.UNSPECIFIED.);
#678=B_SPLINE_CURVE_WITH_KNOTS('',3,(#63963,#63964,#63965,#63966,#63967,
#63968,#63969,#63970,#63971,#63972,#63973,#63974,#63975,#63976,#63977,#63978,
#63979,#63980,#63981,#63982,#63983,#63984,#63985,#63986,#63987,#63988,#63989,
#63990,#63991,#63992,#63993,#63994,#63995,#63996,#63997,#63998,#63999,#64000,
#64001,#64002,#64003,#64004,#64005,#64006,#64007,#64008,#64009,#64010,#64011,
#64012,#64013,#64014,#64015,#64016,#64017,#64018,#64019,#64020,#64021,#64022,
#64023,#64024,#64025,#64026,#64027,#64028,#64029,#64030,#64031,#64032,#64033,
#64034,#64035,#64036,#64037,#64038,#64039,#64040,#64041,#64042,#64043,#64044,
#64045,#64046,#64047,#64048,#64049,#64050,#64051,#64052,#64053,#64054,#64055,
#64056,#64057,#64058,#64059,#64060,#64061,#64062,#64063,#64064,#64065,#64066,
#64067,#64068,#64069,#64070,#64071,#64072,#64073,#64074,#64075,#64076,#64077,
#64078,#64079,#64080,#64081,#64082,#64083,#64084,#64085,#64086,#64087,#64088,
#64089,#64090,#64091,#64092,#64093,#64094,#64095,#64096,#64097,#64098,#64099,
#64100,#64101,#64102,#64103,#64104,#64105,#64106,#64107,#64108,#64109,#64110,
#64111,#64112,#64113,#64114,#64115,#64116,#64117,#64118,#64119,#64120,#64121,
#64122),.UNSPECIFIED.,.F.,.F.,(4,3,3,3,3,3,3,3,3,3,3,3,3,3,3,3,3,3,3,3,
3,3,3,3,3,3,3,3,3,3,3,3,3,3,3,3,3,3,3,3,3,3,3,3,3,3,3,3,3,3,3,3,3,4),(21.9911485751285,
22.095688555741,22.2002115015264,22.3047528752943,22.4094187078935,22.5141572541211,
22.6190804417956,22.6551982208882,22.7601694088621,22.8649834202261,22.9696745313311,
23.0743000328446,23.178895467564,23.2834963345106,23.3882077672821,23.4929805493257,
23.5979348357769,23.652110151213,23.7570778826979,23.8618883670311,23.9665758637526,
24.07119769881,24.1757894205315,24.2803865334175,24.385094175395,24.4898631401608,
24.5948136085044,24.6490220815377,24.7539919562389,24.8588046152603,24.9634943225966,
25.0681183892545,25.1727123601686,25.2773117364654,25.3820216478902,25.4867928888835,
25.591745619818,25.6459340118624,25.7509035844413,25.8557159417997,25.9604053496877,
26.0650291184504,26.1696227934869,26.27422187639,26.3789315002551,26.4837024565829,
26.5886549104258,26.6428459421871,26.7478058378387,26.8526160751731,26.9573035322347,
27.0619198861955,27.1665152309994,27.2120038885876),.UNSPECIFIED.);
#679=B_SPLINE_CURVE_WITH_KNOTS('',3,(#64128,#64129,#64130,#64131,#64132,
#64133,#64134,#64135,#64136,#64137,#64138,#64139,#64140,#64141,#64142,#64143,
#64144,#64145,#64146,#64147,#64148,#64149,#64150,#64151,#64152,#64153,#64154,
#64155,#64156,#64157,#64158,#64159,#64160,#64161,#64162,#64163,#64164,#64165,
#64166,#64167,#64168,#64169,#64170,#64171,#64172,#64173,#64174,#64175,#64176,
#64177,#64178,#64179,#64180,#64181,#64182,#64183,#64184,#64185,#64186,#64187,
#64188,#64189,#64190,#64191,#64192,#64193,#64194,#64195,#64196,#64197,#64198,
#64199,#64200,#64201,#64202,#64203,#64204,#64205,#64206,#64207,#64208,#64209,
#64210,#64211,#64212,#64213,#64214,#64215,#64216,#64217,#64218,#64219,#64220,
#64221,#64222,#64223,#64224,#64225,#64226,#64227,#64228,#64229,#64230,#64231,
#64232,#64233,#64234,#64235,#64236,#64237,#64238,#64239,#64240,#64241,#64242,
#64243,#64244,#64245,#64246,#64247,#64248,#64249,#64250,#64251,#64252,#64253,
#64254,#64255,#64256,#64257,#64258,#64259,#64260,#64261,#64262,#64263,#64264,
#64265,#64266,#64267,#64268,#64269,#64270,#64271,#64272,#64273,#64274,#64275,
#64276,#64277),.UNSPECIFIED.,.F.,.F.,(4,2,2,2,2,2,2,2,2,2,2,2,2,2,2,2,2,
2,2,2,2,2,2,2,2,2,2,2,2,2,2,2,2,2,2,2,2,2,2,2,2,2,2,2,2,2,2,2,2,2,2,2,2,
2,2,2,2,2,2,2,2,2,2,2,2,2,2,2,2,2,2,2,2,2,4),(-1.04468099360072,-1.01104765937819,
-1.00259006590934,-0.998844695782572,-0.995927263237864,-0.992305941515772,
-0.984770855439749,-0.974190770338106,-0.93945390892808,-0.911450453338721,
-0.903209196561764,-0.897770996660255,-0.892441539842163,-0.884771868974065,
-0.862024972451955,-0.810653544258749,-0.802759641619213,-0.799072772206062,
-0.796157071199431,-0.792419795704733,-0.7842410563506,-0.772376769687433,
-0.725601577139473,-0.70921626587037,-0.702832726546107,-0.697570332309719,
-0.692123839503641,-0.683841845073756,-0.652396847880456,-0.608663129143375,
-0.602366640022362,-0.598948362984966,-0.596003839861844,-0.591899157199889,
-0.581396787356787,-0.564246511806176,-0.520279466813033,-0.507514018233735,
-0.50119249911148,-0.496042267583961,-0.489991354373152,-0.47868366709079,
-0.44606513301449,-0.408796987329865,-0.402672218356862,-0.399290648278145,
-0.396336704030203,-0.392162834245318,-0.381164623297261,-0.362728953495016,
-0.313880882899363,-0.305054156032541,-0.299498434706146,-0.294240415059706,
-0.286986493010293,-0.268029948942486,-0.23686567177798,-0.209984437607884,
-0.203406725766932,-0.199929049164845,-0.197023975569625,-0.193037389752502,
-0.183335860251194,-0.168135428320574,-0.118035880101882,-0.107293205825593,
-0.10129079736115,-0.0961377416106961,-0.0897563339973962,-0.0766534350300926,
-0.0584458753898189,-0.0189947357403753,-0.00703089266578593,-0.0029658203194969,
-0.000590074059522167),.UNSPECIFIED.);
#680=B_SPLINE_CURVE_WITH_KNOTS('',3,(#64278,#64279,#64280,#64281,#64282,
#64283,#64284,#64285,#64286,#64287,#64288,#64289,#64290,#64291,#64292,#64293,
#64294,#64295,#64296,#64297,#64298,#64299,#64300,#64301,#64302,#64303,#64304,
#64305,#64306,#64307,#64308,#64309,#64310,#64311,#64312,#64313,#64314,#64315,
#64316,#64317),.UNSPECIFIED.,.F.,.F.,(4,2,2,2,2,2,2,2,2,2,2,2,2,2,2,2,2,
2,2,4),(-2.51292837387859,-2.51207339490121,-2.51041537048523,-2.50716497787441,
-2.50064795951601,-2.47306775569422,-2.44611086368794,-2.42444613760261,
-2.41688673613022,-2.41157827670629,-2.40611503543932,-2.39774151650212,
-2.36543277615857,-2.33431995757322,-2.32425922993822,-2.31699541168418,
-2.31342538340691,-2.31050531308142,-2.30670119723779,-2.30066243309921),
 .UNSPECIFIED.);
#681=B_SPLINE_CURVE_WITH_KNOTS('',3,(#64319,#64320,#64321,#64322,#64323,
#64324,#64325,#64326,#64327,#64328,#64329,#64330,#64331,#64332,#64333,#64334,
#64335,#64336,#64337,#64338,#64339,#64340,#64341,#64342,#64343,#64344,#64345,
#64346,#64347,#64348,#64349),.UNSPECIFIED.,.F.,.F.,(4,3,3,3,3,3,3,3,3,3,
4),(27.2120038885876,27.3189423845687,27.4236756493622,27.531716760937,
27.6397578725118,27.7453039754745,27.8506893660091,27.9566004950839,28.0617646729778,
28.1680492776429,28.2743338823081),.UNSPECIFIED.);
#682=B_SPLINE_CURVE_WITH_KNOTS('',3,(#64350,#64351,#64352,#64353,#64354,
#64355,#64356,#64357,#64358,#64359,#64360,#64361,#64362,#64363,#64364,#64365,
#64366,#64367,#64368,#64369,#64370,#64371,#64372,#64373,#64374,#64375,#64376,
#64377,#64378,#64379,#64380,#64381,#64382,#64383,#64384,#64385,#64386,#64387,
#64388,#64389,#64390,#64391,#64392,#64393,#64394,#64395,#64396,#64397,#64398,
#64399,#64400,#64401,#64402,#64403,#64404,#64405,#64406,#64407,#64408,#64409,
#64410,#64411,#64412,#64413,#64414,#64415,#64416,#64417,#64418,#64419,#64420,
#64421,#64422,#64423,#64424,#64425,#64426,#64427,#64428,#64429,#64430,#64431,
#64432,#64433,#64434,#64435,#64436,#64437,#64438,#64439,#64440,#64441,#64442,
#64443,#64444,#64445,#64446,#64447,#64448,#64449,#64450,#64451,#64452,#64453,
#64454,#64455,#64456,#64457,#64458,#64459,#64460,#64461,#64462,#64463,#64464,
#64465,#64466,#64467,#64468,#64469,#64470,#64471,#64472,#64473,#64474,#64475,
#64476,#64477,#64478,#64479,#64480,#64481,#64482,#64483,#64484,#64485,#64486,
#64487,#64488,#64489,#64490,#64491,#64492,#64493,#64494,#64495,#64496,#64497,
#64498,#64499,#64500,#64501,#64502,#64503,#64504,#64505,#64506),
 .UNSPECIFIED.,.F.,.F.,(4,3,3,3,3,3,3,3,3,3,3,3,3,3,3,3,3,3,3,3,3,3,3,3,
3,3,3,3,3,3,3,3,3,3,3,3,3,3,3,3,3,3,3,3,3,3,3,3,3,3,3,3,4),(28.2743338826888,
28.393063815122,28.5148668089793,28.6366698028365,28.7416392245898,28.8464514270167,
28.9511406746331,29.0557642799049,29.1603577884756,29.2649567021791,29.3696661538382,
29.4744369359963,29.5793892144469,29.6335817331613,29.7385511178593,29.8433632823423,
29.9480524908816,30.0526760563962,30.157269524589,30.2618683973533,30.3665778074985,
30.4713485477548,30.576300784142,30.630493663486,30.735463082248,30.8402752813481,
30.9449645251542,31.0495881263179,31.1541816304881,31.2587805395041,31.3634899860693,
31.4682607628949,31.5732130356956,31.6274055938107,31.7323750033433,31.8371871931352,
31.9418764275626,32.0465000193095,32.1510935140392,32.2556924136055,32.3604018507724,
32.4651726182151,32.5701248817571,32.6243175241354,32.7331396495773,32.8379273036281,
32.9426112832086,33.0472272190469,33.1518106575128,33.2564415872036,33.3611016458819,
33.4658787719657,33.4948945276705),.UNSPECIFIED.);
#683=B_SPLINE_CURVE_WITH_KNOTS('',3,(#64511,#64512,#64513,#64514,#64515,
#64516,#64517,#64518,#64519,#64520,#64521,#64522,#64523,#64524,#64525,#64526,
#64527,#64528,#64529,#64530,#64531,#64532,#64533,#64534,#64535,#64536,#64537,
#64538,#64539,#64540,#64541,#64542,#64543,#64544,#64545,#64546,#64547,#64548,
#64549,#64550,#64551,#64552,#64553,#64554,#64555,#64556,#64557,#64558,#64559,
#64560,#64561,#64562,#64563,#64564,#64565,#64566,#64567,#64568,#64569,#64570,
#64571,#64572,#64573,#64574,#64575,#64576,#64577,#64578,#64579,#64580,#64581,
#64582,#64583,#64584,#64585,#64586,#64587,#64588,#64589,#64590,#64591,#64592,
#64593,#64594,#64595,#64596,#64597,#64598,#64599,#64600,#64601,#64602,#64603,
#64604,#64605,#64606,#64607,#64608,#64609,#64610,#64611,#64612,#64613,#64614,
#64615,#64616,#64617,#64618,#64619,#64620,#64621,#64622,#64623,#64624,#64625,
#64626,#64627,#64628,#64629,#64630,#64631,#64632,#64633,#64634,#64635,#64636,
#64637,#64638,#64639,#64640,#64641,#64642,#64643,#64644,#64645,#64646,#64647,
#64648,#64649,#64650,#64651,#64652,#64653,#64654,#64655,#64656,#64657,#64658,
#64659,#64660,#64661,#64662,#64663,#64664,#64665,#64666,#64667,#64668,#64669,
#64670,#64671,#64672,#64673,#64674,#64675,#64676,#64677,#64678,#64679,#64680,
#64681,#64682,#64683,#64684,#64685,#64686,#64687,#64688,#64689,#64690,#64691,
#64692,#64693,#64694),.UNSPECIFIED.,.F.,.F.,(4,2,2,2,2,2,2,2,2,2,2,2,2,
2,2,2,2,2,2,2,2,2,2,2,2,2,2,2,2,2,2,2,2,2,2,2,2,2,2,2,2,2,2,2,2,2,2,2,2,
2,2,2,2,2,2,2,2,2,2,2,2,2,2,2,2,2,2,2,2,2,2,2,2,2,2,2,2,2,2,2,2,2,2,2,2,
2,2,2,2,2,2,4),(-2.30097243779293,-2.2982084838794,-2.29300504324686,-2.28730979449961,
-2.27779243223803,-2.23415843665506,-2.2130607051309,-2.20111173902322,
-2.19681393836065,-2.19384168655644,-2.19051969267145,-2.18450840712387,
-2.14551557849706,-2.10912812809171,-2.10067675346836,-2.09519706092268,
-2.08995769220102,-2.08366932417971,-2.06809639130763,-2.02211379568242,
-2.00912478124756,-2.00041054278591,-1.99658197821773,-1.99394296835498,
-1.99047489512536,-1.98394164174273,-1.9547577148748,-1.91401137189074,
-1.90317422854472,-1.89721522334071,-1.8920594167371,-1.88562246224264,
-1.8752837851228,-1.82979048226433,-1.81225532303406,-1.80489873878645,
-1.7991426198995,-1.79587388537908,-1.79291383950871,-1.78851338212549,
-1.77668381127525,-1.72996997801461,-1.70811713864274,-1.70053667164389,
-1.69522322247081,-1.68976305041935,-1.68141098379689,-1.64964070539387,
-1.61804960790433,-1.60791446342331,-1.60061096034024,-1.59703276096784,
-1.59411237100711,-1.59031581792478,-1.58155057719378,-1.53105887451293,
-1.5086776456401,-1.50104413206353,-1.49572127426977,-1.49027447815404,
-1.48198946467,-1.45280783481229,-1.41905664344557,-1.40369961322583,-1.39903251076247,
-1.39599345727858,-1.39280425651451,-1.38742299446439,-1.35781108261893,
-1.33324570910505,-1.3094676278794,-1.30170238600797,-1.29635536778667,
-1.29093883690591,-1.2828084729324,-1.25686005880491,-1.2339390603578,-1.20775013905048,
-1.20121672331594,-1.1977486848403,-1.19510971856197,-1.19128134342975,
-1.18256770076127,-1.16958109227768,-1.1239096827404,-1.10814925981019,
-1.10183267326071,-1.09658668681467,-1.09111748830219,-1.08271879721678,
-1.0482833648939,-1.04468099360072),.UNSPECIFIED.);
#684=B_SPLINE_CURVE_WITH_KNOTS('',3,(#64696,#64697,#64698,#64699,#64700,
#64701,#64702,#64703,#64704,#64705,#64706,#64707,#64708,#64709,#64710,#64711,
#64712,#64713,#64714,#64715,#64716,#64717,#64718,#64719,#64720,#64721,#64722,
#64723,#64724,#64725,#64726,#64727,#64728,#64729),.UNSPECIFIED.,.F.,.F.,
(4,3,3,3,3,3,3,3,3,3,3,4),(33.4948945276705,33.5998629780936,33.6212294544601,
33.7252663286542,33.8292979362022,33.9330581898076,34.0367561563849,34.140428630564,
34.2447012701825,34.3484924305647,34.4530058098014,34.5575191890381),
 .UNSPECIFIED.);
#685=B_SPLINE_CURVE_WITH_KNOTS('',3,(#64730,#64731,#64732,#64733,#64734,
#64735,#64736,#64737,#64738,#64739,#64740,#64741,#64742,#64743,#64744,#64745,
#64746,#64747,#64748,#64749,#64750,#64751,#64752,#64753,#64754,#64755,#64756,
#64757,#64758,#64759,#64760,#64761,#64762,#64763,#64764,#64765,#64766,#64767,
#64768,#64769,#64770,#64771,#64772,#64773,#64774,#64775,#64776,#64777,#64778,
#64779,#64780,#64781,#64782,#64783,#64784,#64785,#64786,#64787,#64788,#64789,
#64790,#64791,#64792,#64793,#64794,#64795,#64796,#64797,#64798,#64799,#64800,
#64801,#64802,#64803,#64804,#64805,#64806,#64807,#64808,#64809,#64810,#64811,
#64812,#64813,#64814,#64815,#64816,#64817,#64818,#64819,#64820,#64821,#64822,
#64823,#64824,#64825,#64826,#64827,#64828,#64829,#64830,#64831,#64832,#64833,
#64834,#64835,#64836,#64837,#64838,#64839,#64840,#64841,#64842,#64843,#64844,
#64845,#64846,#64847,#64848,#64849,#64850,#64851,#64852,#64853,#64854,#64855,
#64856,#64857,#64858,#64859,#64860,#64861,#64862,#64863,#64864,#64865,#64866,
#64867,#64868,#64869,#64870,#64871,#64872,#64873,#64874,#64875,#64876,#64877,
#64878,#64879,#64880,#64881,#64882,#64883,#64884,#64885,#64886,#64887,#64888,
#64889),.UNSPECIFIED.,.F.,.F.,(4,3,3,3,3,3,3,3,3,3,3,3,3,3,3,3,3,3,3,3,
3,3,3,3,3,3,3,3,3,3,3,3,3,3,3,3,3,3,3,3,3,3,3,3,3,3,3,3,3,3,3,3,3,4),(34.5575191894877,
34.6181413847848,34.72311079363,34.827922982696,34.9326122163436,35.0372358072776,
35.1418293011626,35.2464281998535,35.3511376361042,35.455908402606,35.5608606651787,
35.6150533151095,35.7200227236772,35.8248349124561,35.9295241458039,36.0341477364304,
36.1387412300007,36.24334012837,36.348049564291,36.4528203304579,36.5577725926912,
36.6119652454343,36.7169346544955,36.8217468437767,36.9264360776374,37.0310596687832,
37.1356531628781,37.2402520617767,37.3449614982305,37.449732264933,37.5546845277004,
37.608877175759,37.7138465846223,37.8186587737031,37.923348007361,38.0279715983023,
38.1325650921917,38.2371639908839,38.3418734271315,38.4466441936275,38.5515964561904,
38.6057891060837,38.7107585149317,38.8155707039964,38.9202599376368,39.02488352856,
39.1294770224305,39.2340759211033,39.3387853573303,39.4435561238053,39.5485083863464,
39.6027010364084,39.7076463034716,39.7791674689231),.UNSPECIFIED.);
#686=B_SPLINE_CURVE_WITH_KNOTS('',3,(#64895,#64896,#64897,#64898,#64899,
#64900,#64901,#64902,#64903,#64904,#64905,#64906,#64907,#64908,#64909,#64910,
#64911,#64912,#64913,#64914,#64915,#64916,#64917,#64918,#64919,#64920,#64921,
#64922,#64923,#64924,#64925,#64926,#64927,#64928,#64929,#64930,#64931,#64932,
#64933,#64934,#64935,#64936,#64937,#64938,#64939,#64940,#64941,#64942,#64943,
#64944,#64945,#64946,#64947,#64948,#64949,#64950,#64951,#64952,#64953,#64954,
#64955,#64956,#64957,#64958,#64959,#64960,#64961,#64962,#64963,#64964,#64965,
#64966,#64967,#64968,#64969,#64970,#64971,#64972,#64973,#64974,#64975,#64976,
#64977,#64978,#64979,#64980,#64981,#64982,#64983,#64984,#64985,#64986,#64987,
#64988,#64989,#64990,#64991,#64992,#64993,#64994,#64995,#64996,#64997,#64998,
#64999,#65000,#65001,#65002,#65003,#65004,#65005,#65006,#65007,#65008,#65009,
#65010,#65011,#65012,#65013,#65014,#65015,#65016,#65017,#65018,#65019,#65020,
#65021,#65022,#65023,#65024,#65025,#65026,#65027,#65028,#65029,#65030,#65031,
#65032,#65033,#65034,#65035,#65036,#65037,#65038),.UNSPECIFIED.,.F.,.F.,
(4,2,2,2,2,2,2,2,2,2,2,2,2,2,2,2,2,2,2,2,2,2,2,2,2,2,2,2,2,2,2,2,2,2,2,
2,2,2,2,2,2,2,2,2,2,2,2,2,2,2,2,2,2,2,2,2,2,2,2,2,2,2,2,2,2,2,2,2,2,2,2,
4),(-1.04476846723434,-1.02150271642865,-0.993063596993994,-0.9848039823034,
-0.979361582460874,-0.974033880152568,-0.966377200851466,-0.943772961992289,
-0.891483739472781,-0.884065891184975,-0.880465730964441,-0.877838866748591,
-0.87417164007109,-0.866388869442685,-0.855323679434048,-0.81669691676623,
-0.792924783185538,-0.784912136459898,-0.780056032336269,-0.77477431143751,
-0.767380752688617,-0.74726056802717,-0.709443651852004,-0.688096131336691,
-0.682917801108451,-0.679771349497663,-0.676698724781373,-0.671868768312631,
-0.6546184284537,-0.609649494447812,-0.591710754974352,-0.584406602933355,
-0.579139901386112,-0.573599585461145,-0.564851327222888,-0.528191572993887,
-0.490202957917336,-0.484144738453861,-0.480777245596411,-0.477818717440396,
-0.473615249035975,-0.462400607146182,-0.443384626730551,-0.395741783538845,
-0.386736941969618,-0.381144615420016,-0.375902277009579,-0.368750647334978,
-0.350603538309684,-0.319889862238882,-0.29143265093126,-0.284883531329093,
-0.281411520310055,-0.278772118211559,-0.274946507765831,-0.266254046123699,
-0.253314688736057,-0.20447525895154,-0.190468441596388,-0.183931492795003,
-0.178766680145095,-0.172873901467681,-0.162378502244032,-0.149027636898252,
-0.113059629756549,-0.0894576005504252,-0.0841843905074643,-0.0810176435442888,
-0.0779609679626385,-0.0732090866244718,-0.0569110159709185,-0.000590502373149791),
 .UNSPECIFIED.);
#687=B_SPLINE_CURVE_WITH_KNOTS('',3,(#65039,#65040,#65041,#65042,#65043,
#65044,#65045,#65046,#65047,#65048,#65049,#65050,#65051,#65052,#65053,#65054,
#65055,#65056,#65057,#65058,#65059,#65060,#65061,#65062,#65063,#65064,#65065,
#65066,#65067,#65068,#65069,#65070,#65071,#65072,#65073,#65074),
 .UNSPECIFIED.,.F.,.F.,(4,2,2,2,2,2,2,2,2,2,2,2,2,2,2,2,2,4),(-2.51338918611576,
-2.50374169630268,-2.49849421365228,-2.49362789901024,-2.48821474142374,
-2.48010299922175,-2.4532375491099,-2.42943506410213,-2.41123848858435,
-2.40033164905448,-2.39617065406752,-2.39321895615316,-2.3898316686122,
-2.38367881354038,-2.34682571576652,-2.32138694147655,-2.30510115965513,
-2.30097243779293),.UNSPECIFIED.);
#688=B_SPLINE_CURVE_WITH_KNOTS('',3,(#65076,#65077,#65078,#65079,#65080,
#65081,#65082,#65083,#65084,#65085,#65086,#65087,#65088,#65089,#65090,#65091,
#65092,#65093,#65094,#65095,#65096,#65097,#65098,#65099,#65100,#65101,#65102,
#65103,#65104,#65105,#65106),.UNSPECIFIED.,.F.,.F.,(4,3,3,3,3,3,3,3,3,3,
4),(39.7791674689231,39.8838850420608,39.9885256523606,40.0931248670507,
40.1977181979906,40.302414823731,40.4071626394716,40.5121024033064,40.5996129667331,
40.7373242033647,40.840704496397),.UNSPECIFIED.);
#689=B_SPLINE_CURVE_WITH_KNOTS('',3,(#65107,#65108,#65109,#65110,#65111,
#65112,#65113,#65114,#65115,#65116,#65117,#65118,#65119,#65120,#65121,#65122,
#65123,#65124,#65125,#65126,#65127,#65128,#65129,#65130,#65131,#65132,#65133,
#65134,#65135,#65136,#65137,#65138,#65139,#65140,#65141,#65142,#65143,#65144,
#65145,#65146,#65147,#65148,#65149,#65150,#65151,#65152,#65153,#65154,#65155,
#65156,#65157,#65158,#65159,#65160,#65161,#65162,#65163,#65164,#65165,#65166,
#65167,#65168,#65169,#65170,#65171,#65172,#65173,#65174,#65175,#65176,#65177,
#65178,#65179,#65180,#65181,#65182,#65183,#65184,#65185,#65186,#65187,#65188,
#65189,#65190,#65191,#65192,#65193,#65194,#65195,#65196,#65197,#65198,#65199,
#65200,#65201,#65202,#65203,#65204,#65205,#65206,#65207,#65208,#65209,#65210,
#65211,#65212,#65213,#65214,#65215,#65216,#65217,#65218,#65219,#65220,#65221,
#65222,#65223,#65224,#65225,#65226,#65227,#65228,#65229,#65230,#65231,#65232,
#65233,#65234,#65235,#65236,#65237,#65238,#65239,#65240,#65241,#65242,#65243,
#65244,#65245,#65246,#65247,#65248,#65249,#65250,#65251,#65252,#65253,#65254,
#65255,#65256,#65257,#65258,#65259,#65260,#65261,#65262,#65263,#65264,#65265,
#65266),.UNSPECIFIED.,.F.,.F.,(4,3,3,3,3,3,3,3,3,3,3,3,3,3,3,3,3,3,3,3,
3,3,3,3,3,3,3,3,3,3,3,3,3,3,3,3,3,3,3,3,3,3,3,3,3,3,3,3,3,3,3,3,3,4),(40.8407044966673,
40.9441437431212,41.047512994444,41.1508494291342,41.2541901753259,41.3576376869291,
41.4611485795811,41.5648311556846,41.5965248970578,41.7014943059365,41.8063064950327,
41.9109957287052,42.0156193196609,42.1202128135644,42.2248117122705,42.3295211485312,
42.4342919150401,42.5392441776152,42.5934368273825,42.6984062362677,42.8032184253704,
42.9079076590497,43.0125312500122,43.1171247439226,43.2217236426356,43.3264330789034,
43.4312038454195,43.5361561080017,43.5903487577073,43.6953181665887,43.8001303556876,
43.9048195893631,44.0094431803219,44.1140366742284,44.2186355729377,44.3233450092016,
44.4281157757136,44.533068038292,44.587260688032,44.6922300969138,44.7970422860127,
44.9017315196885,45.0063551106475,45.1109486045542,45.2155475032635,45.3202569395277,
45.42502770604,45.5299799686185,45.5841726183567,45.6891449771111,45.7939377108536,
45.8986263171477,46.0032482378794,46.0618376755064),.UNSPECIFIED.);
#690=B_SPLINE_CURVE_WITH_KNOTS('',3,(#65271,#65272,#65273,#65274,#65275,
#65276,#65277,#65278,#65279,#65280,#65281,#65282,#65283,#65284,#65285,#65286,
#65287,#65288,#65289,#65290,#65291,#65292,#65293,#65294,#65295,#65296,#65297,
#65298,#65299,#65300,#65301,#65302,#65303,#65304,#65305,#65306,#65307,#65308,
#65309,#65310,#65311,#65312,#65313,#65314,#65315,#65316,#65317,#65318,#65319,
#65320,#65321,#65322,#65323,#65324,#65325,#65326,#65327,#65328,#65329,#65330,
#65331,#65332,#65333,#65334,#65335,#65336,#65337,#65338,#65339,#65340,#65341,
#65342,#65343,#65344,#65345,#65346,#65347,#65348,#65349,#65350,#65351,#65352,
#65353,#65354,#65355,#65356,#65357,#65358,#65359,#65360,#65361,#65362,#65363,
#65364,#65365,#65366,#65367,#65368,#65369,#65370,#65371,#65372,#65373,#65374,
#65375,#65376,#65377,#65378,#65379,#65380,#65381,#65382,#65383,#65384,#65385,
#65386,#65387,#65388,#65389,#65390,#65391,#65392,#65393,#65394,#65395,#65396,
#65397,#65398,#65399,#65400,#65401,#65402,#65403,#65404,#65405,#65406,#65407,
#65408,#65409,#65410,#65411,#65412,#65413,#65414,#65415,#65416,#65417,#65418,
#65419,#65420,#65421,#65422,#65423,#65424,#65425,#65426,#65427,#65428,#65429,
#65430,#65431,#65432,#65433,#65434,#65435,#65436,#65437,#65438,#65439,#65440,
#65441,#65442,#65443,#65444,#65445,#65446,#65447,#65448,#65449,#65450,#65451,
#65452,#65453,#65454,#65455,#65456),.UNSPECIFIED.,.F.,.F.,(4,2,2,2,2,2,
2,2,2,2,2,2,2,2,2,2,2,2,2,2,2,2,2,2,2,2,2,2,2,2,2,2,2,2,2,2,2,2,2,2,2,2,
2,2,2,2,2,2,2,2,2,2,2,2,2,2,2,2,2,2,2,2,2,2,2,2,2,2,2,2,2,2,2,2,2,2,2,2,
2,2,2,2,2,2,2,2,2,2,2,2,2,2,4),(-2.30113049940868,-2.28395381723509,-2.27911355838418,
-2.27603930605954,-2.27289638060789,-2.26773249000325,-2.24671083359363,
-2.2086681222753,-2.18849926182321,-2.18110148672241,-2.17581991522202,
-2.17096603147906,-2.1629621128058,-2.13926611906222,-2.10054004779543,
-2.08423661461128,-2.07948482672064,-2.07642868911724,-2.07326293545978,
-2.06799225334365,-2.04441878173181,-1.99678704114304,-1.98529692454357,
-1.97921165659174,-1.97406354131609,-1.96778377988643,-1.95565527366273,
-1.91111370951703,-1.8938152493437,-1.88651880103419,-1.88079828986366,
-1.87753702425491,-1.87457354895486,-1.87015331940432,-1.85817511097887,
-1.82023363482106,-1.7910995737876,-1.78293960399924,-1.77751703402638,
-1.77223656446641,-1.76454562955879,-1.74334660796559,-1.70193614317224,
-1.68519457119303,-1.68040592973586,-1.6773422315343,-1.67457474782005,
-1.66975126908576,-1.65393982598308,-1.6112507192405,-1.59694130129796,
-1.58589834152536,-1.57989889439336,-1.57474596152609,-1.56836159141225,
-1.5582134364766,-1.50409687259827,-1.48583626369625,-1.48093060229145,
-1.4778424833586,-1.47509499078711,-1.47038083740912,-1.45582222708359,
-1.41192539191239,-1.39054217469516,-1.38301005123856,-1.37770475488341,
-1.3722312870301,-1.36381435924006,-1.33104009368651,-1.30617461108288,
-1.28646924331948,-1.2814668610639,-1.27835831635992,-1.2756256927715,-1.27099414663884,
-1.25725796700291,-1.22946477710496,-1.19576505927446,-1.1858831548253,
-1.18011368861761,-1.17492832734078,-1.16818419154964,-1.15288892991927,
-1.12989900952296,-1.09268773216276,-1.08419612089343,-1.08044466870857,
-1.07752652961233,-1.07390948022743,-1.06639935953652,-1.05586837319828,
-1.04476846723434),.UNSPECIFIED.);
#691=B_SPLINE_CURVE_WITH_KNOTS('',3,(#65458,#65459,#65460,#65461,#65462,
#65463,#65464,#65465,#65466,#65467,#65468,#65469,#65470,#65471,#65472,#65473,
#65474,#65475,#65476,#65477,#65478,#65479,#65480,#65481,#65482,#65483,#65484,
#65485,#65486,#65487,#65488),.UNSPECIFIED.,.F.,.F.,(4,3,3,3,3,3,3,3,3,3,
4),(46.0618376755064,46.1664298233713,46.271122390217,46.3758622586625,
46.4807982822054,46.5810845486814,46.6894780055152,46.7980809550981,46.9060565052648,
47.0149731545559,47.1238898038469),.UNSPECIFIED.);
#692=B_SPLINE_CURVE_WITH_KNOTS('',3,(#65489,#65490,#65491,#65492,#65493,
#65494,#65495,#65496,#65497,#65498,#65499,#65500,#65501,#65502,#65503,#65504,
#65505,#65506,#65507,#65508,#65509,#65510,#65511,#65512,#65513,#65514,#65515,
#65516,#65517,#65518,#65519,#65520,#65521,#65522,#65523,#65524,#65525,#65526,
#65527,#65528,#65529,#65530,#65531,#65532,#65533,#65534,#65535,#65536,#65537,
#65538,#65539,#65540,#65541,#65542,#65543,#65544,#65545,#65546,#65547,#65548,
#65549,#65550,#65551,#65552,#65553,#65554,#65555,#65556,#65557,#65558,#65559,
#65560,#65561,#65562,#65563,#65564,#65565,#65566,#65567,#65568,#65569,#65570,
#65571,#65572,#65573,#65574,#65575,#65576,#65577,#65578,#65579,#65580,#65581,
#65582,#65583,#65584,#65585,#65586,#65587,#65588,#65589,#65590,#65591,#65592,
#65593,#65594,#65595,#65596,#65597,#65598,#65599,#65600,#65601,#65602,#65603,
#65604,#65605,#65606,#65607,#65608,#65609,#65610,#65611,#65612,#65613,#65614,
#65615,#65616,#65617,#65618,#65619,#65620,#65621,#65622,#65623,#65624,#65625,
#65626,#65627,#65628,#65629,#65630,#65631,#65632,#65633,#65634,#65635,#65636,
#65637,#65638,#65639,#65640,#65641,#65642,#65643,#65644,#65645),
 .UNSPECIFIED.,.F.,.F.,(4,3,3,3,3,3,3,3,3,3,3,3,3,3,3,3,3,3,3,3,3,3,3,3,
3,3,3,3,3,3,3,3,3,3,3,3,3,3,3,3,3,3,3,3,3,3,3,3,3,3,3,3,4),(47.1238898042239,
47.2374164729195,47.3496420152373,47.4638192471217,47.5779964790061,47.6829658878876,
47.7877780769866,47.892467310662,47.9970909016209,48.1016843955274,48.2062832942367,
48.3109927305006,48.4157634970128,48.5207157595911,48.5749084093308,48.6798778182161,
48.7846900073189,48.8893792409982,48.9940028319608,49.0985963258712,49.2031952245843,
49.307904660852,49.4126754273679,49.51762768995,49.5718203396556,49.6767897485338,
49.7816019376294,49.8862911713016,49.9909147622572,50.0955082561606,50.2001071548667,
50.3048165911275,50.4095873576367,50.5145396202122,50.5687322699803,50.6737016788587,
50.7785138679544,50.8832031016266,50.9878266925821,51.0924201864853,51.1970190851913,
51.3017285214518,51.4064992879606,51.5114515505356,51.565644200305,51.6705832688796,
51.7753788717255,51.8800667792415,51.9846826335699,52.0892910010002,52.1938944136682,
52.2985747220174,52.3443673060611),.UNSPECIFIED.);
#693=B_SPLINE_CURVE_WITH_KNOTS('',3,(#65651,#65652,#65653,#65654,#65655,
#65656,#65657,#65658,#65659,#65660,#65661,#65662,#65663,#65664,#65665,#65666,
#65667,#65668,#65669,#65670,#65671,#65672,#65673,#65674,#65675,#65676,#65677,
#65678,#65679,#65680,#65681,#65682,#65683,#65684,#65685,#65686,#65687,#65688,
#65689,#65690,#65691,#65692,#65693,#65694,#65695,#65696,#65697,#65698,#65699,
#65700,#65701,#65702,#65703,#65704,#65705,#65706,#65707,#65708,#65709,#65710,
#65711,#65712,#65713,#65714,#65715,#65716,#65717,#65718,#65719,#65720,#65721,
#65722,#65723,#65724,#65725,#65726,#65727,#65728,#65729,#65730,#65731,#65732,
#65733,#65734,#65735,#65736,#65737,#65738,#65739,#65740,#65741,#65742,#65743,
#65744,#65745,#65746,#65747,#65748,#65749,#65750,#65751,#65752,#65753,#65754,
#65755,#65756,#65757,#65758,#65759,#65760,#65761,#65762,#65763,#65764,#65765,
#65766,#65767,#65768,#65769,#65770,#65771,#65772,#65773,#65774,#65775,#65776,
#65777,#65778,#65779,#65780,#65781,#65782,#65783,#65784,#65785,#65786,#65787,
#65788,#65789,#65790,#65791,#65792,#65793,#65794),.UNSPECIFIED.,.F.,.F.,
(4,2,2,2,2,2,2,2,2,2,2,2,2,2,2,2,2,2,2,2,2,2,2,2,2,2,2,2,2,2,2,2,2,2,2,
2,2,2,2,2,2,2,2,2,2,2,2,2,2,2,2,2,2,2,2,2,2,2,2,2,2,2,2,2,2,2,2,2,2,2,2,
4),(-1.04482798327345,-1.02521833172388,-0.972180197582751,-0.965310558681968,
-0.961815585981181,-0.95888580450642,-0.954908288972375,-0.945263772950211,
-0.930195614352971,-0.881098952879368,-0.870649047669339,-0.864181391520398,
-0.859023390789067,-0.853086348885525,-0.842361467695468,-0.828610786541678,
-0.790077000739879,-0.769620230500438,-0.764473565531389,-0.761334424353777,
-0.758257176819843,-0.75340224557667,-0.735817049268247,-0.688159890084346,
-0.672536397229376,-0.666240524652165,-0.660999363773463,-0.655522434708416,
-0.647085146240408,-0.611324400778314,-0.571460025601973,-0.565545794593591,
-0.56224392869706,-0.559263787029176,-0.554918443228039,-0.542583711759657,
-0.520325070808974,-0.478735874455346,-0.469032393960745,-0.463299284038973,
-0.458105845371439,-0.451291995923939,-0.43553902465202,-0.411442925616207,
-0.37200027436343,-0.366036174258641,-0.362723813758482,-0.359747569530664,
-0.355426507404534,-0.343291625879637,-0.321642007855759,-0.279020831328019,
-0.269404440677783,-0.263688778688569,-0.258490431235189,-0.251639667775339,
-0.235641944367935,-0.210937684362213,-0.172617574548671,-0.166622620027214,
-0.163269206157951,-0.160307077011138,-0.156076533213682,-0.144653888413341,
-0.125063991707449,-0.0786009326914746,-0.0694345400979581,-0.0638100911305126,
-0.0585820598898234,-0.0515195694092542,-0.043618414635837,-0.000590369335222942),
 .UNSPECIFIED.);
#694=B_SPLINE_CURVE_WITH_KNOTS('',3,(#65795,#65796,#65797,#65798,#65799,
#65800,#65801,#65802,#65803,#65804,#65805,#65806,#65807,#65808,#65809,#65810,
#65811,#65812,#65813,#65814,#65815,#65816,#65817,#65818,#65819,#65820,#65821,
#65822,#65823,#65824,#65825,#65826,#65827,#65828),.UNSPECIFIED.,.F.,.F.,
(4,2,2,2,2,2,2,2,2,2,2,2,2,2,2,2,4),(-2.51332854493083,-2.49186136662236,
-2.48284036378097,-2.47938770146182,-2.47614354600064,-2.47317215091288,
-2.46870608813633,-2.45637253479781,-2.41883687215827,-2.38979523543442,
-2.38161877317748,-2.37619320573188,-2.37091564981039,-2.36446931199275,
-2.34736277757965,-2.3013428215622,-2.30113049940868),.UNSPECIFIED.);
#695=B_SPLINE_CURVE_WITH_KNOTS('',3,(#65830,#65831,#65832,#65833,#65834,
#65835,#65836,#65837,#65838,#65839,#65840,#65841,#65842,#65843,#65844,#65845,
#65846,#65847,#65848,#65849,#65850,#65851,#65852,#65853,#65854,#65855,#65856,
#65857,#65858,#65859,#65860,#65861,#65862,#65863),.UNSPECIFIED.,.F.,.F.,
(4,3,3,3,3,3,3,3,3,3,3,4),(52.3443673060611,52.4534617183454,52.5625561306297,
52.6681209740064,52.7713623382937,52.8745054159359,52.9775877365012,53.0849595217868,
53.1880825012362,53.2912471673855,53.3945404609816,53.4070748776434),
 .UNSPECIFIED.);
#696=B_SPLINE_CURVE_WITH_KNOTS('',3,(#65864,#65865,#65866,#65867,#65868,
#65869,#65870,#65871,#65872,#65873),.UNSPECIFIED.,.F.,.F.,(4,1,1,1,1,1,
1,4),(53.4070751110264,53.5594680609544,54.5563799912791,55.5532919216039,
56.5502038519286,57.5471157822533,58.544027712578,58.6286430004606),
 .UNSPECIFIED.);
#697=B_SPLINE_CURVE_WITH_KNOTS('',3,(#65878,#65879,#65880,#65881,#65882,
#65883,#65884,#65885,#65886,#65887,#65888,#65889,#65890,#65891,#65892,#65893,
#65894,#65895,#65896,#65897,#65898,#65899,#65900,#65901,#65902,#65903,#65904,
#65905,#65906,#65907,#65908,#65909,#65910,#65911,#65912,#65913,#65914,#65915,
#65916,#65917,#65918,#65919,#65920,#65921,#65922,#65923,#65924,#65925,#65926,
#65927,#65928,#65929,#65930,#65931,#65932,#65933,#65934,#65935,#65936,#65937,
#65938,#65939,#65940,#65941,#65942,#65943,#65944,#65945,#65946,#65947,#65948,
#65949,#65950,#65951,#65952,#65953,#65954,#65955,#65956,#65957,#65958,#65959,
#65960,#65961,#65962,#65963,#65964,#65965,#65966,#65967,#65968,#65969,#65970,
#65971,#65972,#65973,#65974,#65975,#65976,#65977,#65978,#65979,#65980,#65981,
#65982,#65983,#65984,#65985,#65986,#65987,#65988,#65989,#65990,#65991,#65992,
#65993,#65994,#65995,#65996,#65997,#65998,#65999,#66000,#66001,#66002,#66003,
#66004,#66005,#66006,#66007,#66008,#66009,#66010,#66011,#66012,#66013,#66014,
#66015,#66016,#66017,#66018,#66019,#66020,#66021,#66022,#66023,#66024,#66025,
#66026,#66027,#66028,#66029,#66030,#66031,#66032,#66033,#66034,#66035,#66036,
#66037,#66038,#66039,#66040,#66041,#66042,#66043,#66044,#66045,#66046,#66047,
#66048,#66049,#66050,#66051,#66052,#66053,#66054,#66055,#66056,#66057,#66058,
#66059),.UNSPECIFIED.,.F.,.F.,(4,2,2,2,2,2,2,2,2,2,2,2,2,2,2,2,2,2,2,2,
2,2,2,2,2,2,2,2,2,2,2,2,2,2,2,2,2,2,2,2,2,2,2,2,2,2,2,2,2,2,2,2,2,2,2,2,
2,2,2,2,2,2,2,2,2,2,2,2,2,2,2,2,2,2,2,2,2,2,2,2,2,2,2,2,2,2,2,2,2,2,4),
(-2.30097507222157,-2.27184260697766,-2.26353996377759,-2.25809013588611,
-2.2528318611597,-2.24526132613213,-2.22511425467268,-2.18257822685029,
-2.16566793006745,-2.16086610611524,-2.15780008841559,-2.15464789182317,
-2.14944008827473,-2.127423792708,-2.09021166272833,-2.07024305908673,-2.0628685872235,
-2.05759110831319,-2.05273250288001,-2.04470069123103,-2.02073113458886,
-1.98229094023209,-1.9660377449484,-1.96129036166191,-1.95823515794079,
-1.9550683911771,-1.94979242052714,-1.92604329157949,-1.87857148150213,
-1.86710176762947,-1.86102065245453,-1.85587275367377,-1.84958915186538,
-1.83743951672762,-1.79292580938812,-1.77563464218439,-1.76507784620772,
-1.76096587045619,-1.7580209229682,-1.75460780473943,-1.74833367026587,
-1.7045180944078,-1.67316440965434,-1.66488865883195,-1.65944402534755,
-1.65418177731784,-1.64658933155429,-1.62619496017701,-1.58391902721668,
-1.56704778682396,-1.56224907817011,-1.5591836468353,-1.55603076680117,
-1.55081921957841,-1.52871536501292,-1.49157867342593,-1.47162925161676,
-1.46425738350926,-1.45898066026376,-1.45412200898185,-1.4460883830396,
-1.42128749281607,-1.38354035577394,-1.36740976601795,-1.36267325431155,
-1.35962043815872,-1.3564510544332,-1.35116225492438,-1.32694060534567,
-1.27933038786535,-1.26824465790243,-1.26223760085562,-1.25708619762342,
-1.25071408304169,-1.23765845465763,-1.21954412639077,-1.1972605483073,
-1.17128232626678,-1.16476013991665,-1.1612946917616,-1.15865569085706,
-1.15482462981984,-1.14609326872036,-1.13306797073562,-1.10275539929081,
-1.07457865085267,-1.06633096509937,-1.06089186133063,-1.05556399848102,
-1.04790104846741,-1.04482798327345),.UNSPECIFIED.);
#698=B_SPLINE_CURVE_WITH_KNOTS('',3,(#66061,#66062,#66063,#66064,#66065),
 .UNSPECIFIED.,.F.,.F.,(4,1,4),(58.6286430004606,59.5409396429027,59.690260418206),
 .UNSPECIFIED.);
#699=B_SPLINE_CURVE_WITH_KNOTS('',3,(#66066,#66067,#66068,#66069,#66070,
#66071,#66072,#66073,#66074,#66075,#66076,#66077,#66078,#66079,#66080,#66081,
#66082,#66083,#66084,#66085,#66086,#66087,#66088,#66089,#66090,#66091,#66092,
#66093,#66094,#66095,#66096,#66097,#66098,#66099,#66100,#66101,#66102,#66103,
#66104,#66105,#66106,#66107,#66108,#66109,#66110,#66111,#66112,#66113,#66114,
#66115,#66116,#66117,#66118,#66119,#66120,#66121,#66122,#66123,#66124,#66125,
#66126,#66127,#66128,#66129,#66130,#66131,#66132,#66133,#66134,#66135,#66136,
#66137,#66138,#66139,#66140,#66141,#66142,#66143,#66144,#66145,#66146,#66147,
#66148,#66149,#66150,#66151,#66152,#66153,#66154,#66155,#66156,#66157,#66158,
#66159,#66160,#66161,#66162,#66163,#66164,#66165,#66166,#66167,#66168,#66169,
#66170,#66171,#66172,#66173,#66174,#66175,#66176,#66177,#66178,#66179,#66180,
#66181,#66182,#66183,#66184,#66185,#66186,#66187,#66188,#66189,#66190,#66191,
#66192,#66193,#66194,#66195,#66196,#66197,#66198,#66199,#66200,#66201,#66202,
#66203,#66204,#66205,#66206,#66207,#66208,#66209,#66210,#66211,#66212,#66213,
#66214,#66215,#66216,#66217,#66218,#66219,#66220,#66221,#66222,#66223,#66224,
#66225),.UNSPECIFIED.,.F.,.F.,(4,3,3,3,3,3,3,3,3,3,3,3,3,3,3,3,3,3,3,3,
3,3,3,3,3,3,3,3,3,3,3,3,3,3,3,3,3,3,3,3,3,3,3,3,3,3,3,3,3,3,3,3,3,4),(59.6902606576805,
59.7962095221238,59.8993829629699,60.0024877467406,60.1055613221456,60.213633884916,
60.316822665245,60.4200786763603,60.5234998464774,60.5378515732274,60.6428209922896,
60.747633191622,60.8523224355587,60.9569460367901,61.0615395409651,61.166138449923,
61.2708478963356,61.3756186729547,61.4805709454672,61.5347635035521,61.6397328863229,
61.7445450493154,61.8492342570163,61.9538578220964,62.0584512902582,62.1630501633944,
62.2677595745191,62.3725303161014,62.4774825543385,62.5316754338769,62.6366448586233,
62.7414570633651,62.8461463122836,62.9507699182301,63.0553634268489,63.1599623399743,
63.2646717901123,63.3694425702111,63.4743948457886,63.5285873642016,63.6335568439146,
63.7383691043125,63.8430584096273,63.9476820723948,64.0522756381703,64.1568746087001,
64.2615841162163,64.3663549537629,64.4713072862801,64.5254992945263,64.6304386418885,
64.7352407025703,64.8399279937932,64.9116585324962),.UNSPECIFIED.);
#700=B_SPLINE_CURVE_WITH_KNOTS('',3,(#66231,#66232,#66233,#66234,#66235,
#66236,#66237,#66238,#66239,#66240,#66241,#66242,#66243,#66244,#66245,#66246,
#66247,#66248,#66249,#66250,#66251,#66252,#66253,#66254,#66255,#66256,#66257,
#66258,#66259,#66260,#66261,#66262,#66263,#66264,#66265,#66266,#66267,#66268,
#66269,#66270,#66271,#66272,#66273,#66274,#66275,#66276,#66277,#66278,#66279,
#66280,#66281,#66282,#66283,#66284,#66285,#66286,#66287,#66288,#66289,#66290,
#66291,#66292,#66293,#66294,#66295,#66296,#66297,#66298,#66299,#66300,#66301,
#66302,#66303,#66304,#66305,#66306,#66307,#66308,#66309,#66310,#66311,#66312,
#66313,#66314,#66315,#66316,#66317,#66318,#66319,#66320,#66321,#66322,#66323,
#66324,#66325,#66326,#66327,#66328,#66329,#66330,#66331,#66332,#66333,#66334,
#66335,#66336,#66337,#66338,#66339,#66340,#66341,#66342,#66343,#66344,#66345,
#66346,#66347,#66348,#66349,#66350,#66351,#66352,#66353,#66354,#66355,#66356,
#66357,#66358,#66359,#66360,#66361,#66362,#66363,#66364,#66365,#66366,#66367,
#66368,#66369,#66370,#66371,#66372,#66373,#66374,#66375,#66376,#66377,#66378,
#66379,#66380,#66381,#66382,#66383,#66384,#66385,#66386),.UNSPECIFIED.,
 .F.,.F.,(4,2,2,2,2,2,2,2,2,2,2,2,2,2,2,2,2,2,2,2,2,2,2,2,2,2,2,2,2,2,2,
2,2,2,2,2,2,2,2,2,2,2,2,2,2,2,2,2,2,2,2,2,2,2,2,2,2,2,2,2,2,2,2,2,2,2,2,
2,2,2,2,2,2,2,2,2,2,4),(-1.0443153183833,-1.04241560857417,-1.0394548464591,
-1.03573799890252,-1.02575940998438,-0.985758233817047,-0.961530523588478,
-0.95044472515653,-0.944458888694553,-0.939338584144273,-0.933023557475811,
-0.920170517525391,-0.902449044652388,-0.879473401761167,-0.85317485771094,
-0.846642782846574,-0.843188930944256,-0.840558470026248,-0.836748755654842,
-0.828146795396558,-0.815399212184051,-0.784406536744733,-0.756372102721844,
-0.74811987714739,-0.742673020800209,-0.737333483659212,-0.729645160127398,
-0.706758666737787,-0.681449487439988,-0.651722825886203,-0.64633127489472,
-0.643134028096896,-0.640089234738094,-0.635407192783891,-0.619916882197167,
-0.585517378644701,-0.557162184660311,-0.548905638304376,-0.543462612770092,
-0.538132194462761,-0.530467720558331,-0.50780144694809,-0.455014727323234,
-0.447940332893434,-0.44440530065395,-0.441481491866233,-0.437563651611919,
-0.428293602569473,-0.414082015187736,-0.378681545778949,-0.356479105908006,
-0.348711529911623,-0.343900157725863,-0.338585881880242,-0.330987466576925,
-0.308939408673464,-0.260987826958697,-0.250204724788896,-0.245955618970417,
-0.242991898655694,-0.239648765074693,-0.233537456253398,-0.225573648682296,
-0.205527386453999,-0.159895301639851,-0.150640824855572,-0.144997536919566,
-0.139774523257218,-0.132753490577631,-0.115716129881903,-0.0881644406393426,
-0.0548872374637813,-0.0484954929886149,-0.0450561579917568,-0.0421151848914067,
-0.0380438672445768,-0.0333678775887178,-0.000612794912691296),
 .UNSPECIFIED.);
#701=B_SPLINE_CURVE_WITH_KNOTS('',3,(#66387,#66388,#66389,#66390,#66391,
#66392,#66393,#66394,#66395,#66396,#66397,#66398,#66399,#66400,#66401,#66402,
#66403,#66404,#66405,#66406,#66407,#66408,#66409,#66410,#66411,#66412,#66413,
#66414,#66415,#66416,#66417,#66418),.UNSPECIFIED.,.F.,.F.,(4,2,2,2,2,2,
2,2,2,2,2,2,2,2,2,4),(-2.5135235169571,-2.48279461776556,-2.47022321311333,
-2.46246766610601,-2.45712250133492,-2.4517039407824,-2.44356287286976,
-2.41745455136848,-2.37196574750479,-2.3630699199823,-2.35921139583419,
-2.35656923776549,-2.35312238275445,-2.34668904599171,-2.30378846763817,
-2.30097507222157),.UNSPECIFIED.);
#702=B_SPLINE_CURVE_WITH_KNOTS('',3,(#66420,#66421,#66422,#66423,#66424,
#66425,#66426,#66427,#66428,#66429,#66430,#66431,#66432,#66433,#66434,#66435,
#66436,#66437,#66438,#66439,#66440,#66441,#66442,#66443,#66444,#66445,#66446,
#66447,#66448,#66449,#66450),.UNSPECIFIED.,.F.,.F.,(4,3,3,3,3,3,3,3,3,3,
4),(64.9116585324962,65.0162574550017,65.1208506087689,65.2255471356105,
65.3302949562089,65.4352346208628,65.522411224851,65.6352598287414,65.7478409063075,
65.8606433156557,65.973445725004),.UNSPECIFIED.);
#703=B_SPLINE_CURVE_WITH_KNOTS('',3,(#66451,#66452,#66453,#66454,#66455,
#66456,#66457,#66458,#66459,#66460,#66461,#66462,#66463,#66464,#66465,#66466,
#66467,#66468,#66469,#66470,#66471,#66472,#66473,#66474,#66475,#66476,#66477,
#66478,#66479,#66480,#66481,#66482,#66483,#66484,#66485,#66486,#66487,#66488,
#66489,#66490,#66491,#66492,#66493,#66494,#66495,#66496,#66497,#66498,#66499,
#66500,#66501,#66502,#66503,#66504,#66505,#66506,#66507,#66508,#66509,#66510,
#66511,#66512,#66513,#66514,#66515,#66516,#66517,#66518,#66519,#66520,#66521,
#66522,#66523,#66524,#66525,#66526,#66527,#66528,#66529,#66530,#66531,#66532,
#66533,#66534,#66535,#66536,#66537,#66538,#66539,#66540,#66541,#66542,#66543,
#66544,#66545,#66546,#66547,#66548,#66549,#66550,#66551,#66552,#66553,#66554,
#66555,#66556,#66557,#66558,#66559,#66560,#66561,#66562,#66563,#66564,#66565,
#66566,#66567,#66568,#66569,#66570,#66571,#66572,#66573,#66574,#66575,#66576,
#66577,#66578,#66579,#66580,#66581,#66582,#66583,#66584,#66585,#66586,#66587,
#66588,#66589,#66590,#66591,#66592,#66593,#66594,#66595,#66596,#66597,#66598,
#66599,#66600,#66601,#66602,#66603,#66604,#66605,#66606,#66607),
 .UNSPECIFIED.,.F.,.F.,(4,3,3,3,3,3,3,3,3,3,3,3,3,3,3,3,3,3,3,3,3,3,3,3,
3,3,3,3,3,3,3,3,3,3,3,3,3,3,3,3,3,3,3,3,3,3,3,3,3,3,3,3,4),(65.9734457253856,
66.081074447525,66.1906366244377,66.2985803622296,66.4089517587027,66.5193231551757,
66.6242930301999,66.7291056894711,66.8337953969479,66.9384194636786,67.0430134345979,
67.1476128108322,67.2523227220928,67.3570939628641,67.4620466934886,67.5162350855004,
67.6212027061388,67.7260131047489,67.8307005532449,67.9353223633164,68.0399140832534,
68.1445112175424,68.2492189158513,68.3539879568804,68.4589385316235,68.5131470158251,
68.6181184444408,68.7229326419031,68.8276238577,68.9322494134512,69.0368448520375,
69.1414456725101,69.2461569829797,69.3509295994489,69.4558836549037,69.5100589461499,
69.6150311701829,69.7198462083276,69.824538326873,69.9291648231743,70.03376123836,
70.1383630697676,70.24307543558,70.3478491341531,70.4528043012553,70.5069708764746,
70.6119036442383,70.7166902153778,70.8213663945815,70.9259799468757,71.0305556766275,
71.1351654797296,71.1940098997199),.UNSPECIFIED.);
#704=B_SPLINE_CURVE_WITH_KNOTS('',3,(#66614,#66615,#66616,#66617,#66618,
#66619,#66620,#66621,#66622,#66623,#66624,#66625,#66626,#66627,#66628,#66629,
#66630,#66631,#66632,#66633,#66634,#66635,#66636,#66637,#66638,#66639,#66640,
#66641),.UNSPECIFIED.,.F.,.F.,(4,2,2,2,2,2,2,2,2,2,2,2,2,4),(-1.11563238755794,
-1.07955432989617,-1.03866429355625,-0.965353884613767,-0.876709828383185,
-0.787134953185386,-0.711240432632776,-0.638657623954711,-0.583650144269578,
-0.53111472373597,-0.476882015471721,-0.423633401831507,-0.331772706465313,
-0.269307451570121),.UNSPECIFIED.);
#705=B_SPLINE_CURVE_WITH_KNOTS('',3,(#66644,#66645,#66646,#66647,#66648,
#66649,#66650,#66651,#66652,#66653),.UNSPECIFIED.,.F.,.F.,(4,2,2,2,4),(-0.269307451570121,
-0.238086410933035,-0.158868946271387,-0.0862199057315852,0.),
 .UNSPECIFIED.);
#706=B_SPLINE_CURVE_WITH_KNOTS('',3,(#66657,#66658,#66659,#66660,#66661,
#66662,#66663,#66664,#66665,#66666,#66667,#66668,#66669,#66670),
 .UNSPECIFIED.,.F.,.F.,(4,2,2,2,2,2,4),(-0.384491130116531,-0.271273669787035,
-0.181083343007982,-0.137241346038334,-0.067686198175976,-0.0316925286601113,
0.),.UNSPECIFIED.);
#707=B_SPLINE_CURVE_WITH_KNOTS('',3,(#66674,#66675,#66676,#66677,#66678,
#66679),.UNSPECIFIED.,.F.,.F.,(4,1,1,4),(-4.09157007060746,-4.06042151127377,
-3.06350958094905,-2.06659765062435),.UNSPECIFIED.);
#708=B_SPLINE_CURVE_WITH_KNOTS('',3,(#66681,#66682,#66683,#66684,#66685),
 .UNSPECIFIED.,.F.,.F.,(4,1,4),(0.,0.997998106294493,1.11662023360662),
 .UNSPECIFIED.);
#709=B_SPLINE_CURVE_WITH_KNOTS('',3,(#66687,#66688,#66689,#66690,#66691,
#66692,#66693,#66694,#66695,#66696,#66697,#66698,#66699,#66700,#66701,#66702,
#66703,#66704,#66705,#66706,#66707,#66708,#66709,#66710,#66711,#66712,#66713,
#66714,#66715,#66716,#66717,#66718,#66719,#66720,#66721,#66722,#66723,#66724,
#66725,#66726,#66727,#66728,#66729,#66730,#66731,#66732,#66733,#66734,#66735,
#66736,#66737,#66738,#66739,#66740,#66741,#66742,#66743,#66744,#66745,#66746,
#66747,#66748,#66749,#66750,#66751,#66752,#66753,#66754,#66755,#66756,#66757,
#66758,#66759,#66760,#66761,#66762,#66763,#66764,#66765,#66766,#66767,#66768,
#66769,#66770,#66771,#66772,#66773,#66774,#66775,#66776,#66777,#66778,#66779,
#66780,#66781,#66782,#66783,#66784,#66785,#66786,#66787,#66788,#66789,#66790,
#66791,#66792,#66793,#66794,#66795,#66796,#66797,#66798,#66799,#66800,#66801,
#66802,#66803,#66804,#66805,#66806,#66807,#66808,#66809,#66810,#66811,#66812,
#66813,#66814,#66815,#66816,#66817,#66818,#66819,#66820,#66821,#66822,#66823,
#66824,#66825,#66826,#66827,#66828,#66829,#66830,#66831,#66832,#66833,#66834,
#66835,#66836,#66837,#66838,#66839,#66840,#66841,#66842,#66843,#66844,#66845,
#66846,#66847,#66848,#66849,#66850,#66851,#66852,#66853,#66854,#66855,#66856,
#66857,#66858,#66859,#66860,#66861,#66862,#66863,#66864,#66865,#66866,#66867,
#66868,#66869,#66870,#66871,#66872,#66873,#66874,#66875,#66876),
 .UNSPECIFIED.,.F.,.F.,(4,3,3,3,3,3,3,3,3,3,3,3,3,3,3,3,3,3,3,3,3,3,3,3,
3,3,3,3,3,3,3,3,3,3,3,3,3,3,3,3,3,3,3,3,3,3,3,3,3,3,3,3,3,3,3,3,3,3,3,3,
3,3,3,4),(1.11662023360662,1.21411903985626,1.31185368644785,1.4091285442428,
1.50635618882577,1.60356917797076,1.70167593662532,1.79901395118647,1.89750508188772,
1.99599621258898,2.09575595181835,2.19537177172638,2.29519959012101,2.39463345345404,
2.49403329621222,2.59342947268088,2.69357068423153,2.7931075696835,2.89355094428349,
2.99399431888347,3.09384741984894,3.19356069033868,3.29336465719359,3.39290523805578,
3.49241505814163,3.59192433049513,3.69194135416584,3.79159787439762,3.89179514978779,
3.99199242517796,4.09158324220157,4.19102961866606,4.29089973276686,4.39016417384572,
4.48939498922613,4.58862276885971,4.6889647095129,4.78833649761076,4.8891635145416,
4.98999053147245,5.08969774466914,5.18926191652918,5.2891027566839,5.38848753760586,
5.48783938456321,5.58718872579993,5.68738870379168,5.7868821230465,5.88743538040672,
5.98798863776694,6.08769799308571,6.18726467488049,6.2871049335281,6.38649310806084,
6.48584867520973,6.58520205952138,6.68539823065639,6.78489645125149,6.88544159765645,
6.98598674406142,7.09561182117547,7.20492700212712,7.31371639735308,7.39980554040546),
 .UNSPECIFIED.);
#710=B_SPLINE_CURVE_WITH_KNOTS('',3,(#66878,#66879,#66880,#66881,#66882,
#66883,#66884,#66885,#66886,#66887,#66888,#66889,#66890,#66891,#66892,#66893,
#66894,#66895,#66896,#66897,#66898,#66899,#66900,#66901,#66902,#66903,#66904,
#66905,#66906,#66907,#66908,#66909,#66910,#66911,#66912,#66913,#66914,#66915,
#66916,#66917,#66918,#66919,#66920,#66921,#66922,#66923,#66924,#66925,#66926,
#66927,#66928,#66929,#66930,#66931,#66932,#66933,#66934,#66935,#66936,#66937,
#66938,#66939,#66940,#66941,#66942,#66943,#66944,#66945,#66946,#66947,#66948,
#66949,#66950,#66951,#66952,#66953,#66954,#66955,#66956,#66957,#66958,#66959,
#66960,#66961,#66962,#66963,#66964,#66965,#66966,#66967,#66968,#66969,#66970,
#66971,#66972,#66973,#66974,#66975,#66976,#66977,#66978,#66979,#66980,#66981,
#66982,#66983,#66984,#66985,#66986,#66987,#66988,#66989,#66990,#66991,#66992,
#66993,#66994,#66995,#66996,#66997,#66998,#66999,#67000,#67001,#67002,#67003,
#67004,#67005,#67006,#67007,#67008,#67009,#67010,#67011,#67012,#67013,#67014,
#67015,#67016,#67017,#67018,#67019,#67020,#67021,#67022,#67023,#67024,#67025,
#67026,#67027,#67028,#67029,#67030,#67031,#67032,#67033,#67034,#67035,#67036,
#67037,#67038,#67039,#67040,#67041,#67042,#67043,#67044,#67045,#67046,#67047,
#67048,#67049,#67050,#67051,#67052,#67053,#67054,#67055,#67056,#67057,#67058,
#67059,#67060,#67061,#67062,#67063,#67064,#67065,#67066,#67067,#67068,#67069,
#67070),.UNSPECIFIED.,.F.,.F.,(4,3,3,3,3,3,3,3,3,3,3,3,3,3,3,3,3,3,3,3,
3,3,3,3,3,3,3,3,3,3,3,3,3,3,3,3,3,3,3,3,3,3,3,3,3,3,3,3,3,3,3,3,3,3,3,3,
3,3,3,3,3,3,3,3,4),(7.39980554078621,7.50085641996669,7.60195463078282,
7.70320978748876,7.80454701233738,7.90609535985808,7.98398485035592,8.08367982463198,
8.1832317804571,8.28307567748127,8.38244839256476,8.48178825804934,8.5811257191651,
8.68134002853643,8.78082194156904,8.88140244910973,8.98198295665041,9.08167691055587,
9.18122787135141,9.2810720203006,9.38044381022138,9.47978277908141,9.57911937347872,
9.67933479584527,9.77881592522409,9.87939849408449,9.9799810629449,10.0796716629935,
10.1792192051011,10.2790642006184,10.3784324389066,10.477767813924,10.5771007770452,
10.6773203750937,10.776797817893,10.8773884935662,10.9779791692394,11.0776718340994,
11.1772214697375,11.2770659454621,11.3764363317309,11.4757738704398,11.5751090100447,
11.675326076417,11.7748057049477,11.8753914902408,11.9759772755339,12.0756696578348,
12.1752190114948,12.2750635577865,12.3744336656699,12.4737709279859,12.5731057935813,
12.6733231906431,12.7728025538994,12.8733889678639,12.9739753818284,13.0729162403087,
13.1717239927683,13.2704302143224,13.3735703727333,13.4721850961793,13.5707915293105,
13.6694467689652,13.6829908479658),.UNSPECIFIED.);
#711=B_SPLINE_CURVE_WITH_KNOTS('',3,(#67072,#67073,#67074,#67075,#67076,
#67077,#67078,#67079,#67080,#67081,#67082,#67083,#67084,#67085,#67086,#67087,
#67088,#67089,#67090,#67091,#67092,#67093,#67094,#67095,#67096,#67097,#67098,
#67099,#67100,#67101,#67102,#67103,#67104,#67105,#67106,#67107,#67108,#67109,
#67110,#67111,#67112,#67113,#67114,#67115,#67116,#67117,#67118,#67119,#67120,
#67121,#67122,#67123,#67124,#67125,#67126,#67127,#67128,#67129,#67130,#67131,
#67132,#67133,#67134,#67135,#67136,#67137,#67138,#67139,#67140,#67141,#67142,
#67143,#67144,#67145,#67146,#67147,#67148,#67149,#67150,#67151,#67152,#67153,
#67154,#67155,#67156,#67157,#67158,#67159,#67160,#67161,#67162,#67163,#67164,
#67165,#67166,#67167,#67168,#67169,#67170,#67171,#67172,#67173,#67174,#67175,
#67176,#67177,#67178,#67179,#67180,#67181,#67182,#67183,#67184,#67185,#67186,
#67187,#67188,#67189,#67190,#67191,#67192,#67193,#67194,#67195,#67196,#67197,
#67198,#67199,#67200,#67201,#67202,#67203,#67204,#67205,#67206,#67207,#67208,
#67209,#67210,#67211,#67212,#67213,#67214,#67215,#67216,#67217,#67218,#67219,
#67220,#67221,#67222,#67223,#67224,#67225,#67226,#67227,#67228,#67229,#67230,
#67231,#67232,#67233,#67234,#67235,#67236,#67237,#67238,#67239,#67240,#67241,
#67242,#67243,#67244,#67245,#67246,#67247,#67248,#67249,#67250,#67251,#67252,
#67253,#67254,#67255,#67256,#67257,#67258,#67259,#67260,#67261,#67262,#67263,
#67264),.UNSPECIFIED.,.F.,.F.,(4,3,3,3,3,3,3,3,3,3,3,3,3,3,3,3,3,3,3,3,
3,3,3,3,3,3,3,3,3,3,3,3,3,3,3,3,3,3,3,3,3,3,3,3,3,3,3,3,3,3,3,3,3,3,3,3,
3,3,3,3,3,3,3,3,4),(13.6829908482554,13.8040460294717,13.9269629425475,
13.9719734881229,14.0716657749935,14.1712150296549,14.2710596002502,14.3704296011319,
14.4697667536623,14.5691015068274,14.6693190287249,14.7687982741564,14.8693849342869,
14.9699715944174,15.0696638277482,15.1692130286241,15.2690576126351,15.3684275595413,
15.4677646581471,15.5670993575134,15.667316943313,15.7667961358123,15.867382918262,
15.9679697007118,16.0676618972506,16.1672110605043,16.267055653817,16.3664255613515,
16.4657626200133,16.565097278916,16.6653149109386,16.7647940621039,16.8653809345551,
16.9659678070063,17.0656600367114,17.1652092336409,17.2650538185984,17.3644237608008,
17.4637608544271,17.5630955485436,17.6633131397329,17.762792326367,17.8633791198339,
17.9639659133008,18.0636581342268,18.1632073223082,18.2630519094691,18.362421842722,
18.4617589273806,18.5610936125237,18.6613112142916,18.7607903920308,18.861377205813,
18.9619640195953,19.0616562370282,19.1612054215272,19.2610500095725,19.3604199390515,
19.4597570198723,19.5590917011189,19.6593093073117,19.7587884810486,19.8593753034692,
19.9599621258898,19.9661761551454),.UNSPECIFIED.);
#712=B_SPLINE_CURVE_WITH_KNOTS('',3,(#67266,#67267,#67268,#67269,#67270,
#67271,#67272,#67273,#67274,#67275,#67276,#67277,#67278,#67279,#67280,#67281,
#67282,#67283,#67284,#67285,#67286,#67287,#67288,#67289,#67290,#67291,#67292,
#67293,#67294,#67295,#67296,#67297,#67298,#67299,#67300,#67301,#67302,#67303,
#67304,#67305,#67306,#67307,#67308,#67309,#67310,#67311,#67312,#67313,#67314,
#67315,#67316,#67317,#67318,#67319,#67320,#67321,#67322,#67323,#67324,#67325,
#67326,#67327,#67328,#67329,#67330,#67331,#67332,#67333,#67334,#67335,#67336,
#67337,#67338,#67339,#67340,#67341,#67342,#67343,#67344,#67345,#67346,#67347,
#67348,#67349,#67350,#67351,#67352,#67353,#67354,#67355,#67356,#67357,#67358,
#67359,#67360,#67361,#67362,#67363,#67364,#67365,#67366,#67367,#67368,#67369,
#67370,#67371,#67372,#67373,#67374,#67375,#67376,#67377,#67378,#67379,#67380,
#67381,#67382,#67383,#67384,#67385,#67386,#67387,#67388,#67389,#67390,#67391,
#67392,#67393,#67394,#67395,#67396,#67397,#67398,#67399,#67400,#67401,#67402,
#67403,#67404,#67405,#67406,#67407,#67408,#67409,#67410,#67411,#67412,#67413,
#67414,#67415,#67416,#67417,#67418,#67419,#67420,#67421,#67422,#67423,#67424,
#67425,#67426,#67427,#67428,#67429,#67430,#67431,#67432,#67433,#67434,#67435,
#67436,#67437,#67438,#67439,#67440,#67441,#67442,#67443,#67444,#67445,#67446,
#67447,#67448,#67449,#67450,#67451,#67452,#67453,#67454,#67455),
 .UNSPECIFIED.,.F.,.F.,(4,3,3,3,3,3,3,3,3,3,3,3,3,3,3,3,3,3,3,3,3,3,3,3,
3,3,3,3,3,3,3,3,3,3,3,3,3,3,3,3,3,3,3,3,3,3,3,3,3,3,3,3,3,3,3,3,3,3,3,3,
3,3,3,4),(19.9661761555104,20.0657577276433,20.1651964120122,20.2645199722879,
20.3637805135757,20.4630086753788,20.5622350573188,20.6615596078517,20.7609309415982,
20.860483049496,20.9579602321843,21.0576524523546,21.1572016396432,21.2570462269977,
21.3564161593729,21.4557532431238,21.5550879273303,21.6553055301174,21.7547847068578,
21.8553715226683,21.9559583384788,22.0556505583573,22.1551997453451,22.2550443327736,
22.3544142648279,22.4537513482509,22.5530860321232,22.6533036352857,22.7527828116792,
22.8533696282262,22.9539564447733,23.0536486651395,23.1531978526233,23.2530424399289,
23.3524123724952,23.4517494564354,23.551084140829,23.6513017433887,23.750780920309,
23.8513677356884,23.9519545510678,24.051646771243,24.1511959585335,24.2510405458871,
24.3504104782565,24.4497475619987,24.5490822461939,24.649299848986,24.7487790257078,
24.849365841535,24.9499526573622,25.0496448775194,25.1491940647909,25.2490386521491,
25.3484085844979,25.4477456682185,25.547080352391,25.6472979552074,25.7467771319055,
25.8473639477811,25.9479507636567,26.0691100425263,26.1886825764541,26.2493614619858),
 .UNSPECIFIED.);
#713=B_SPLINE_CURVE_WITH_KNOTS('',3,(#67457,#67458,#67459,#67460,#67461,
#67462,#67463,#67464,#67465,#67466,#67467,#67468,#67469,#67470,#67471,#67472,
#67473,#67474,#67475,#67476,#67477,#67478,#67479,#67480,#67481,#67482,#67483,
#67484,#67485,#67486,#67487,#67488,#67489,#67490,#67491,#67492,#67493,#67494,
#67495,#67496,#67497,#67498,#67499,#67500,#67501,#67502,#67503,#67504,#67505,
#67506,#67507,#67508,#67509,#67510,#67511,#67512,#67513,#67514,#67515,#67516,
#67517,#67518,#67519,#67520,#67521,#67522,#67523,#67524,#67525,#67526,#67527,
#67528,#67529,#67530,#67531,#67532,#67533,#67534,#67535,#67536,#67537,#67538,
#67539,#67540,#67541,#67542,#67543,#67544,#67545,#67546,#67547,#67548,#67549,
#67550,#67551,#67552,#67553,#67554,#67555,#67556,#67557,#67558,#67559,#67560,
#67561,#67562,#67563,#67564,#67565,#67566,#67567,#67568,#67569,#67570,#67571,
#67572,#67573,#67574,#67575,#67576,#67577,#67578,#67579,#67580,#67581,#67582,
#67583,#67584,#67585,#67586,#67587,#67588,#67589,#67590,#67591,#67592,#67593,
#67594,#67595,#67596,#67597,#67598,#67599,#67600,#67601,#67602,#67603,#67604,
#67605,#67606,#67607,#67608,#67609,#67610,#67611,#67612,#67613,#67614,#67615,
#67616,#67617,#67618,#67619,#67620,#67621,#67622,#67623,#67624,#67625,#67626,
#67627,#67628,#67629,#67630,#67631,#67632,#67633,#67634,#67635,#67636,#67637,
#67638,#67639,#67640,#67641,#67642,#67643,#67644,#67645,#67646),
 .UNSPECIFIED.,.F.,.F.,(4,3,3,3,3,3,3,3,3,3,3,3,3,3,3,3,3,3,3,3,3,3,3,3,
3,3,3,3,3,3,3,3,3,3,3,3,3,3,3,3,3,3,3,3,3,3,3,3,3,3,3,3,3,3,3,3,3,3,3,3,
3,3,3,4),(26.249361462325,26.3481734936058,26.4469506347904,26.5457240082695,
26.6457802236899,26.7446986980816,26.8453237840164,26.9459488699512,27.0456410901392,
27.1451902774423,27.2450348647927,27.3444047971741,27.4437418809282,27.5430765651348,
27.6432941679125,27.7427733446451,27.8433601604454,27.9439469762457,28.0436391964338,
28.1431883837368,28.2430329710872,28.3424029034685,28.4417399872223,28.5410746714285,
28.6412922742064,28.7407714509386,28.8413582667394,28.9419450825402,29.0416373027347,
29.1411864900443,29.2410310773931,29.3404010097813,29.439738093542,29.5390727777552,
29.6392903805251,29.7387695572644,29.8393563730496,29.9399431888347,30.0396354090257,
30.139184596332,30.2390291836816,30.3383991160662,30.4377361998233,30.5370708840328,
30.6372884868069,30.7367676635423,30.8373544793357,30.9379412951292,31.0376335153205,
31.1371827026271,31.2370272899766,31.3363972223614,31.4357343061186,31.5350689903286,
31.6352865931024,31.7347657698382,31.8353525856309,31.9359394014237,32.0371556997279,
32.138214632322,32.2391188409517,32.3399315096669,32.4406844014574,32.5325467695046),
 .UNSPECIFIED.);
#714=B_SPLINE_CURVE_WITH_KNOTS('',3,(#67648,#67649,#67650,#67651,#67652,
#67653,#67654,#67655,#67656,#67657,#67658,#67659,#67660,#67661,#67662,#67663,
#67664,#67665,#67666,#67667,#67668,#67669,#67670,#67671,#67672,#67673,#67674,
#67675,#67676,#67677,#67678,#67679,#67680,#67681,#67682,#67683,#67684,#67685,
#67686,#67687,#67688,#67689,#67690,#67691,#67692,#67693,#67694,#67695,#67696,
#67697,#67698,#67699,#67700,#67701,#67702,#67703,#67704,#67705,#67706,#67707,
#67708,#67709,#67710,#67711,#67712,#67713,#67714,#67715,#67716,#67717,#67718,
#67719,#67720,#67721,#67722,#67723,#67724,#67725,#67726,#67727,#67728,#67729,
#67730,#67731,#67732,#67733,#67734,#67735,#67736,#67737,#67738,#67739,#67740,
#67741,#67742,#67743,#67744,#67745,#67746,#67747,#67748,#67749,#67750,#67751,
#67752,#67753,#67754,#67755,#67756,#67757,#67758,#67759,#67760,#67761,#67762,
#67763,#67764,#67765,#67766,#67767,#67768,#67769,#67770,#67771,#67772,#67773,
#67774,#67775,#67776,#67777,#67778,#67779,#67780,#67781,#67782,#67783,#67784,
#67785,#67786,#67787,#67788,#67789,#67790,#67791,#67792,#67793,#67794,#67795,
#67796,#67797,#67798,#67799,#67800,#67801,#67802,#67803,#67804,#67805,#67806,
#67807,#67808,#67809,#67810,#67811,#67812,#67813,#67814,#67815,#67816,#67817,
#67818,#67819,#67820,#67821,#67822,#67823,#67824,#67825,#67826,#67827,#67828,
#67829,#67830,#67831,#67832,#67833,#67834,#67835,#67836,#67837),
 .UNSPECIFIED.,.F.,.F.,(4,3,3,3,3,3,3,3,3,3,3,3,3,3,3,3,3,3,3,3,3,3,3,3,
3,3,3,3,3,3,3,3,3,3,3,3,3,3,3,3,3,3,3,3,3,3,3,3,3,3,3,3,3,3,3,3,3,3,3,3,
3,3,3,4),(32.5325467697112,32.642251979765,32.7523332142757,32.8629430985259,
32.9339375077182,33.0336297279098,33.1331789152162,33.2330235025658,33.3323934349508,
33.4317305187085,33.5310652029185,33.6312828056921,33.7307619824281,33.8313487982204,
33.9319356140127,34.0316278342047,34.1311770215117,34.2310216088611,34.3303915412466,
34.4297286250046,34.529063309215,34.629280911988,34.7287600887245,34.8293469045158,
34.9299337203071,35.0296259404984,35.1291751278049,35.2290197151545,35.3283896475393,
35.4277267312967,35.5270614155066,35.6272790182804,35.7267581950163,35.827345010809,
35.9279318266017,36.0276240467927,36.1271732340988,36.2270178214484,36.3263877538329,
36.42572483759,36.5250595217995,36.6252771245737,36.7247563013092,36.8253431171027,
36.9259299328961,37.0256221530908,37.1251713404006,37.2250159277493,37.3243858601375,
37.4237229438982,37.5230576281115,37.6232752308812,37.7227544076204,37.8233412234055,
37.9239280391906,38.0223327314332,38.1215076495607,38.2196568051179,38.3177465254137,
38.4158087531075,38.5157895839441,38.6139437328095,38.7148379046316,38.8157320764536),
 .UNSPECIFIED.);
#715=B_SPLINE_CURVE_WITH_KNOTS('',3,(#67839,#67840,#67841,#67842,#67843,
#67844,#67845,#67846,#67847,#67848,#67849,#67850,#67851,#67852,#67853,#67854,
#67855,#67856,#67857,#67858,#67859,#67860,#67861,#67862,#67863,#67864,#67865,
#67866,#67867,#67868,#67869,#67870,#67871,#67872,#67873,#67874,#67875,#67876,
#67877,#67878,#67879,#67880,#67881,#67882,#67883,#67884,#67885,#67886,#67887,
#67888,#67889,#67890,#67891,#67892,#67893,#67894,#67895,#67896,#67897,#67898,
#67899,#67900,#67901,#67902,#67903,#67904,#67905,#67906,#67907,#67908,#67909,
#67910,#67911,#67912,#67913,#67914,#67915,#67916,#67917,#67918,#67919,#67920,
#67921,#67922,#67923,#67924,#67925,#67926,#67927,#67928,#67929,#67930,#67931,
#67932,#67933,#67934,#67935,#67936,#67937,#67938,#67939,#67940,#67941,#67942,
#67943,#67944,#67945,#67946,#67947,#67948,#67949,#67950,#67951,#67952,#67953,
#67954,#67955,#67956,#67957,#67958,#67959,#67960,#67961,#67962,#67963,#67964,
#67965,#67966,#67967,#67968,#67969,#67970,#67971,#67972,#67973,#67974,#67975,
#67976,#67977,#67978,#67979,#67980,#67981,#67982,#67983,#67984,#67985,#67986,
#67987,#67988,#67989,#67990,#67991,#67992,#67993,#67994,#67995,#67996,#67997,
#67998,#67999,#68000,#68001,#68002,#68003,#68004,#68005,#68006,#68007,#68008,
#68009,#68010,#68011,#68012,#68013,#68014,#68015,#68016,#68017,#68018,#68019,
#68020,#68021,#68022,#68023,#68024,#68025,#68026,#68027,#68028),
 .UNSPECIFIED.,.F.,.F.,(4,3,3,3,3,3,3,3,3,3,3,3,3,3,3,3,3,3,3,3,3,3,3,3,
3,3,3,3,3,3,3,3,3,3,3,3,3,3,3,3,3,3,3,3,3,3,3,3,3,3,3,3,3,3,3,3,3,3,3,3,
3,3,3,4),(38.8157320766842,38.9219261454851,39.0216183656735,39.121167552977,
39.2210121403273,39.320382072709,39.4197191564632,39.5190538406699,39.6192714434473,
39.71875062018,39.8193374359798,39.9199242517796,40.0196164719951,40.1191656593257,
40.2190102466693,40.3183801790783,40.4177172628598,40.5170519470937,40.6172695498388,
40.7167487265982,40.8173355423361,40.9179223580741,41.0176145782277,41.1171637654965,
41.2170083528555,41.3163782852032,41.4157153689238,41.5150500530972,41.615267655915,
41.7147468326156,41.8153336484921,41.9159204643686,42.0156126845468,42.1151618718396,
42.2150064591925,42.3143763915628,42.4137134753053,42.5130481594999,42.6132657622907,
42.7127449390108,42.8133317548369,42.9139185706631,43.0136107910374,43.1131599785273,
43.2130045658311,43.3123744983996,43.4117115823403,43.5110462667328,43.611263869289,
43.7107430462041,43.8113298615808,43.9119166769576,44.0116088968064,44.1111580837707,
44.2110026712059,44.3103726032525,44.4097096866739,44.5090443705503,44.6092619737258,
44.7087411501379,44.809327966695,44.9099147832521,45.0568405353361,45.0989173838637),
 .UNSPECIFIED.);
#716=B_SPLINE_CURVE_WITH_KNOTS('',3,(#68030,#68031,#68032,#68033,#68034,
#68035,#68036,#68037,#68038,#68039,#68040,#68041,#68042,#68043,#68044,#68045,
#68046,#68047,#68048,#68049,#68050,#68051,#68052,#68053,#68054,#68055,#68056,
#68057,#68058,#68059,#68060,#68061,#68062,#68063,#68064,#68065,#68066,#68067,
#68068,#68069,#68070,#68071,#68072,#68073,#68074,#68075,#68076,#68077,#68078,
#68079,#68080,#68081,#68082,#68083,#68084,#68085,#68086,#68087,#68088,#68089,
#68090,#68091,#68092,#68093,#68094,#68095,#68096,#68097,#68098,#68099,#68100,
#68101,#68102,#68103,#68104,#68105,#68106,#68107,#68108,#68109,#68110,#68111,
#68112,#68113,#68114,#68115,#68116,#68117,#68118,#68119,#68120,#68121,#68122,
#68123,#68124,#68125,#68126,#68127,#68128,#68129,#68130,#68131,#68132,#68133,
#68134,#68135,#68136,#68137,#68138,#68139,#68140,#68141,#68142,#68143,#68144,
#68145,#68146,#68147,#68148,#68149,#68150,#68151,#68152,#68153,#68154,#68155,
#68156,#68157,#68158,#68159,#68160,#68161,#68162,#68163,#68164,#68165,#68166,
#68167,#68168,#68169,#68170,#68171,#68172,#68173,#68174,#68175,#68176,#68177,
#68178,#68179,#68180,#68181,#68182,#68183,#68184,#68185,#68186,#68187,#68188,
#68189,#68190,#68191,#68192,#68193,#68194,#68195,#68196,#68197,#68198,#68199,
#68200,#68201,#68202,#68203,#68204,#68205,#68206,#68207,#68208,#68209,#68210,
#68211,#68212,#68213,#68214,#68215,#68216,#68217,#68218,#68219,#68220,#68221,
#68222),.UNSPECIFIED.,.F.,.F.,(4,3,3,3,3,3,3,3,3,3,3,3,3,3,3,3,3,3,3,3,
3,3,3,3,3,3,3,3,3,3,3,3,3,3,3,3,3,3,3,3,3,3,3,3,3,3,3,3,3,3,3,3,3,3,3,3,
3,3,3,3,3,3,3,3,4),(45.0989173840905,45.2000418222725,45.2980012309023,
45.3959090948093,45.4937975009913,45.5916985068107,45.6897025308092,45.7877690184893,
45.885989317891,45.9079128895465,46.0076051110968,46.1071542997675,46.2069988867767,
46.3063688205293,46.4057059056527,46.5050405912249,46.6052581923789,46.7047373704543,
46.8053241831477,46.905910995841,47.0056032130355,47.1051523973474,47.2049969854459,
47.3043669148636,47.4037039956706,47.5030386769507,47.6032562832469,47.702735457133,
47.8033222796342,47.9039091021355,48.0036013233754,48.1031505117032,48.202995098794,
48.3023650321276,48.4017021168047,48.5010368019041,48.6012544035356,48.7007335810783,
48.8013203947542,48.90190720843,49.0015994384125,49.1011486355596,49.2009932204552,
49.3003631627289,49.3997002563714,49.4990349504489,49.5992525415178,49.6987317279782,
49.7993185213514,49.8999053147245,49.9995975093961,50.0991466711844,50.1989912649137,
50.298361171968,50.397698230521,50.4970328896857,50.597250522519,50.6967296748532,
50.7973165479361,50.897903421019,51.0034366957994,51.1086517278921,51.2136734259997,
51.3184380308843,51.3821026907301),.UNSPECIFIED.);
#717=B_SPLINE_CURVE_WITH_KNOTS('',3,(#68224,#68225,#68226,#68227,#68228,
#68229,#68230,#68231,#68232,#68233,#68234,#68235,#68236,#68237,#68238,#68239,
#68240,#68241,#68242,#68243,#68244,#68245,#68246,#68247,#68248,#68249,#68250,
#68251,#68252,#68253,#68254,#68255,#68256,#68257,#68258,#68259,#68260,#68261,
#68262,#68263,#68264,#68265,#68266,#68267,#68268,#68269,#68270,#68271,#68272,
#68273,#68274,#68275,#68276,#68277,#68278,#68279,#68280,#68281,#68282,#68283,
#68284,#68285,#68286,#68287,#68288,#68289,#68290,#68291,#68292,#68293,#68294,
#68295,#68296,#68297,#68298,#68299,#68300,#68301,#68302,#68303,#68304,#68305,
#68306,#68307,#68308,#68309,#68310,#68311,#68312,#68313,#68314,#68315,#68316,
#68317,#68318,#68319,#68320,#68321,#68322,#68323,#68324,#68325,#68326,#68327,
#68328,#68329,#68330,#68331,#68332,#68333,#68334,#68335,#68336,#68337,#68338,
#68339,#68340,#68341,#68342,#68343,#68344,#68345,#68346,#68347,#68348,#68349,
#68350,#68351,#68352,#68353,#68354,#68355,#68356,#68357,#68358,#68359,#68360,
#68361,#68362,#68363,#68364,#68365,#68366,#68367,#68368,#68369,#68370,#68371,
#68372,#68373,#68374,#68375,#68376,#68377,#68378,#68379,#68380,#68381,#68382,
#68383,#68384,#68385,#68386,#68387,#68388,#68389,#68390,#68391,#68392,#68393,
#68394,#68395,#68396,#68397,#68398,#68399,#68400,#68401,#68402,#68403,#68404,
#68405,#68406,#68407,#68408,#68409,#68410,#68411,#68412,#68413),
 .UNSPECIFIED.,.F.,.F.,(4,3,3,3,3,3,3,3,3,3,3,3,3,3,3,3,3,3,3,3,3,3,3,3,
3,3,3,3,3,3,3,3,3,3,3,3,3,3,3,3,3,3,3,3,3,3,3,3,3,3,3,3,3,3,3,3,3,3,3,3,
3,3,3,4),(51.3821026910433,51.4855307958723,51.5892117397779,51.6930192770188,
51.797104292293,51.8959015273135,51.9955938152988,52.095143070835,52.1949876411816,
52.2943576423501,52.3936947949456,52.4930295479546,52.593247069368,52.692726314102,
52.793312973855,52.893899633608,52.9935916415485,53.093140616474,53.1929852569026,
53.2923549781269,53.3916918516459,53.491026326818,53.5912441800891,53.6907231528435,
53.791310446373,53.8918977399025,53.9915901487866,54.0911395233135,54.1909840636739,
54.2903541783941,54.3896914422614,54.4890263041265,54.5892436896441,54.6887230362615,
54.7893094412292,54.8898958461969,54.9895885107553,55.0891381461562,55.1889826219481,
55.2883530081394,55.3876905468306,55.4870256864775,55.587242752981,55.6867223817006,
55.787308167096,55.8878939524914,55.9875844461522,56.0871319047493,56.1869769240039,
56.28634513493,56.3856805037378,56.4850134817863,56.5852331260362,56.6847106354235,
56.7853013471047,56.8858920587859,56.9841948130386,57.0823705698818,57.1804515428413,
57.2784698224436,57.3764943428403,57.4745156851681,57.5726368200333,57.6652879979023),
 .UNSPECIFIED.);
#718=B_SPLINE_CURVE_WITH_KNOTS('',3,(#68415,#68416,#68417,#68418,#68419,
#68420,#68421,#68422,#68423,#68424,#68425,#68426,#68427,#68428,#68429,#68430,
#68431,#68432,#68433,#68434,#68435,#68436,#68437,#68438,#68439,#68440,#68441,
#68442,#68443,#68444,#68445,#68446,#68447,#68448,#68449,#68450,#68451,#68452,
#68453,#68454,#68455,#68456,#68457,#68458,#68459,#68460,#68461,#68462,#68463,
#68464,#68465,#68466,#68467,#68468,#68469,#68470,#68471,#68472,#68473,#68474,
#68475,#68476,#68477,#68478,#68479,#68480,#68481,#68482,#68483,#68484,#68485,
#68486,#68487,#68488,#68489,#68490,#68491,#68492,#68493,#68494,#68495,#68496,
#68497,#68498,#68499,#68500,#68501,#68502,#68503,#68504,#68505,#68506,#68507,
#68508,#68509,#68510,#68511,#68512,#68513,#68514,#68515,#68516,#68517,#68518,
#68519,#68520,#68521,#68522,#68523,#68524,#68525,#68526,#68527,#68528,#68529,
#68530,#68531,#68532,#68533,#68534,#68535,#68536,#68537,#68538,#68539,#68540,
#68541,#68542,#68543,#68544,#68545,#68546,#68547,#68548,#68549,#68550,#68551,
#68552,#68553,#68554,#68555,#68556,#68557,#68558,#68559,#68560,#68561,#68562,
#68563,#68564,#68565,#68566,#68567,#68568,#68569,#68570,#68571,#68572,#68573,
#68574,#68575,#68576,#68577,#68578,#68579,#68580,#68581,#68582,#68583,#68584,
#68585,#68586,#68587,#68588,#68589,#68590,#68591,#68592,#68593,#68594,#68595,
#68596,#68597,#68598,#68599,#68600,#68601,#68602,#68603,#68604),
 .UNSPECIFIED.,.F.,.F.,(4,3,3,3,3,3,3,3,3,3,3,3,3,3,3,3,3,3,3,3,3,3,3,3,
3,3,3,3,3,3,3,3,3,3,3,3,3,3,3,3,3,3,3,3,3,3,3,3,3,3,3,3,3,3,3,3,3,3,3,3,
3,3,3,4),(57.6652879982229,57.8019872101644,57.8838901650804,57.9835850616989,
58.0831369565666,58.1829808709176,58.2823535660295,58.3816934269835,58.4810308989979,
58.5812452420922,58.6807272037328,58.7813077375538,58.8818882713749,58.9815667546959,
59.0811021788842,59.1809502037324,59.2803064091976,59.3796298098178,59.478950872875,
59.5791847490736,59.6786505945985,59.779268486134,59.8798863776694,59.9795977204589,
60.0791659622596,60.1790057774726,60.2783944630306,60.3777501459646,60.4771032511164,
60.5772985593283,60.6767955357196,60.7773400098417,60.8778844839639,60.9775904742664,
61.0771536862424,61.1769947992444,61.276379265716,61.3757310414051,61.4750805543747,
61.5752810633456,61.6747752481323,61.7753289191953,61.8758825902584,61.9754681206924,
62.0749103463045,62.1747816400855,62.2740447196494,62.3732752234771,62.4725037407329,
62.5728479796879,62.6722230732196,62.7730518848863,62.8738806965529,62.9737506217514,
63.0734770927308,63.1732773064954,63.2728222045018,63.372332990656,63.471839880485,
63.5718496110756,63.6714955828981,63.7716871928727,63.8718788028474,63.9484733054025),
 .UNSPECIFIED.);
#719=B_SPLINE_CURVE_WITH_KNOTS('',3,(#68606,#68607,#68608,#68609,#68610,
#68611,#68612,#68613,#68614,#68615,#68616,#68617,#68618,#68619,#68620,#68621,
#68622,#68623,#68624,#68625,#68626,#68627,#68628,#68629,#68630,#68631,#68632,
#68633),.UNSPECIFIED.,.F.,.F.,(4,3,3,3,3,3,3,3,3,4),(63.9484733057947,64.045833445615,
64.1430501669001,64.240187491038,64.3372781596142,64.4343548402426,64.5315110163484,
64.6287070047887,64.7260617590684,64.7992696555444),.UNSPECIFIED.);
#720=B_SPLINE_CURVE_WITH_KNOTS('',3,(#68639,#68640,#68641,#68642,#68643,
#68644,#68645,#68646,#68647,#68648),.UNSPECIFIED.,.F.,.F.,(4,1,1,1,1,1,
1,4),(-66.8658731217308,-65.8689611914061,-64.8720492610814,-63.8751373307567,
-62.878225400432,-61.8813134701072,-60.8844015397825,-60.6402388355142),
 .UNSPECIFIED.);
#721=B_SPLINE_CURVE_WITH_KNOTS('',3,(#68650,#68651,#68652,#68653,#68654,
#68655,#68656,#68657,#68658,#68659,#68660,#68661,#68662,#68663,#68664,#68665,
#68666,#68667,#68668,#68669,#68670,#68671,#68672,#68673,#68674,#68675,#68676,
#68677,#68678,#68679,#68680,#68681,#68682,#68683,#68684,#68685,#68686,#68687,
#68688,#68689,#68690,#68691,#68692,#68693,#68694,#68695,#68696,#68697,#68698,
#68699,#68700,#68701,#68702,#68703,#68704,#68705,#68706,#68707,#68708,#68709,
#68710,#68711,#68712,#68713,#68714,#68715,#68716,#68717,#68718,#68719,#68720,
#68721,#68722,#68723,#68724,#68725,#68726,#68727,#68728,#68729,#68730,#68731,
#68732,#68733,#68734,#68735,#68736,#68737,#68738,#68739,#68740,#68741,#68742,
#68743,#68744,#68745,#68746,#68747,#68748,#68749,#68750,#68751,#68752,#68753,
#68754,#68755,#68756,#68757,#68758,#68759,#68760,#68761,#68762,#68763,#68764,
#68765,#68766,#68767,#68768,#68769,#68770,#68771,#68772,#68773,#68774,#68775,
#68776,#68777,#68778,#68779,#68780,#68781,#68782,#68783,#68784,#68785,#68786,
#68787,#68788,#68789,#68790,#68791,#68792,#68793,#68794,#68795,#68796,#68797,
#68798,#68799,#68800,#68801,#68802,#68803,#68804,#68805,#68806,#68807,#68808,
#68809,#68810,#68811,#68812,#68813,#68814,#68815,#68816,#68817,#68818,#68819,
#68820,#68821,#68822,#68823,#68824,#68825,#68826,#68827,#68828,#68829,#68830,
#68831,#68832,#68833,#68834,#68835,#68836,#68837,#68838,#68839,#68840,#68841,
#68842),.UNSPECIFIED.,.F.,.F.,(4,3,3,3,3,3,3,3,3,3,3,3,3,3,3,3,3,3,3,3,
3,3,3,3,3,3,3,3,3,3,3,3,3,3,3,3,3,3,3,3,3,3,3,3,3,3,3,3,3,3,3,3,3,3,3,3,
3,3,3,3,3,3,3,3,4),(-60.6402378352238,-60.541941212625,-60.4437069664625,
-60.3455032818595,-60.2472983849303,-60.1489962635298,-60.0506424675455,
-59.9521211484188,-59.8874896094578,-59.7877964476612,-59.688246214181,
-59.5885376473,-59.4891664171286,-59.389827997839,-59.290491942401,-59.190513376584,
-59.0910331601191,-58.9908054196261,-58.8905776791331,-58.7908689547546,
-58.6913029540899,-58.5915983034297,-58.492210925325,-58.3928562507879,
-58.2935038548443,-58.1935443283353,-58.0940477288565,-57.9938567388324,
-57.8936657488084,-57.7939580819579,-57.6943931146846,-57.5946882026595,
-57.4953017907731,-57.3959480548088,-57.2965965683636,-57.1966358808936,
-57.0971401095801,-56.9969469640319,-56.8967538184837,-56.797049434805,
-56.6974878144905,-56.5977820736991,-56.4983991394847,-56.3990489227396,
-56.2997009923592,-56.1997362163091,-56.1002440555365,-56.0000429718477,
-55.899841888159,-55.8001354687304,-55.7005717841839,-55.6008665558901,
-55.5014815034612,-55.4021291529011,-55.3027790759983,-55.2028167964573,
-55.1033224798672,-55.0031262188507,-54.9029299578342,-54.8000855684324,
-54.6974202396436,-54.5949536053784,-54.4926049980164,-54.3903737338144,
-54.3570525280442),.UNSPECIFIED.);
#722=B_SPLINE_CURVE_WITH_KNOTS('',3,(#68844,#68845,#68846,#68847,#68848,
#68849,#68850,#68851,#68852,#68853,#68854,#68855,#68856,#68857,#68858,#68859,
#68860,#68861,#68862,#68863,#68864,#68865,#68866,#68867,#68868,#68869,#68870,
#68871,#68872,#68873,#68874,#68875,#68876,#68877,#68878,#68879,#68880,#68881,
#68882,#68883,#68884,#68885,#68886,#68887,#68888,#68889,#68890,#68891,#68892,
#68893,#68894,#68895,#68896,#68897,#68898,#68899,#68900,#68901,#68902,#68903,
#68904,#68905,#68906,#68907,#68908,#68909,#68910,#68911,#68912,#68913,#68914,
#68915,#68916,#68917,#68918,#68919,#68920,#68921,#68922,#68923,#68924,#68925,
#68926,#68927,#68928,#68929,#68930,#68931,#68932,#68933,#68934,#68935,#68936,
#68937,#68938,#68939,#68940,#68941,#68942,#68943,#68944,#68945,#68946,#68947,
#68948,#68949,#68950,#68951,#68952,#68953,#68954,#68955,#68956,#68957,#68958,
#68959,#68960,#68961,#68962,#68963,#68964,#68965,#68966,#68967,#68968,#68969,
#68970,#68971,#68972,#68973,#68974,#68975,#68976,#68977,#68978,#68979,#68980,
#68981,#68982,#68983,#68984,#68985,#68986,#68987,#68988,#68989,#68990,#68991,
#68992,#68993,#68994,#68995,#68996,#68997,#68998,#68999,#69000,#69001,#69002,
#69003,#69004,#69005,#69006,#69007,#69008,#69009,#69010,#69011,#69012,#69013,
#69014,#69015,#69016,#69017,#69018,#69019,#69020,#69021,#69022,#69023,#69024,
#69025,#69026,#69027,#69028,#69029,#69030,#69031,#69032,#69033,#69034,#69035,
#69036),.UNSPECIFIED.,.F.,.F.,(4,3,3,3,3,3,3,3,3,3,3,3,3,3,3,3,3,3,3,3,
3,3,3,3,3,3,3,3,3,3,3,3,3,3,3,3,3,3,3,3,3,3,3,3,3,3,3,3,3,3,3,3,3,3,3,3,
3,3,3,3,3,3,3,3,4),(-54.3570525278076,-54.2507043889139,-54.1439444211688,
-54.0369627416244,-53.9296600714483,-53.9060180275095,-53.8063122441195,
-53.7067492024809,-53.6070438143189,-53.5076594166994,-53.4083077239587,
-53.3089583069853,-53.2089952545352,-53.1095015962846,-53.0093038467347,
-52.9091060971848,-52.8094000541278,-52.7098367489929,-52.6101314262263,
-52.5107467577453,-52.4113947919731,-52.3120451001678,-52.2120823668409,
-52.1125884321395,-52.0123912994998,-51.9121941668601,-51.8124881776674,
-51.7129249266653,-51.613219590399,-51.5138349762923,-51.4144830648616,
-51.3151334272894,-51.2151706296009,-51.1156767483046,-51.01547949242,-50.9152822365354,
-50.8155762825399,-50.7160130675383,-50.6163077223724,-50.5169231459594,
-50.4175712727776,-50.3182216739587,-50.2182588320217,-50.118764990327,
-50.0185676482688,-49.9183703062107,-49.8186643198593,-49.7191010720012,
-49.6193957349868,-49.5200111247426,-49.4206592174378,-49.3213095842503,
-49.2213467821592,-49.1218529058425,-49.0216556408642,-48.9214583758859,
-48.8232165413679,-48.7251385007468,-48.6271523335141,-48.529225872404,
-48.4313270291267,-48.333374301944,-48.2353942142858,-48.1372843483312,
-48.0738672212483),.UNSPECIFIED.);
#723=B_SPLINE_CURVE_WITH_KNOTS('',3,(#69038,#69039,#69040,#69041,#69042,
#69043,#69044,#69045,#69046,#69047,#69048,#69049,#69050,#69051,#69052,#69053,
#69054,#69055,#69056,#69057,#69058,#69059,#69060,#69061,#69062,#69063,#69064,
#69065,#69066,#69067,#69068,#69069,#69070,#69071,#69072,#69073,#69074,#69075,
#69076,#69077,#69078,#69079,#69080,#69081,#69082,#69083,#69084,#69085,#69086,
#69087,#69088,#69089,#69090,#69091,#69092,#69093,#69094,#69095,#69096,#69097,
#69098,#69099,#69100,#69101,#69102,#69103,#69104,#69105,#69106,#69107,#69108,
#69109,#69110,#69111,#69112,#69113,#69114,#69115,#69116,#69117,#69118,#69119,
#69120,#69121,#69122,#69123,#69124,#69125,#69126,#69127,#69128,#69129,#69130,
#69131,#69132,#69133,#69134,#69135,#69136,#69137,#69138,#69139,#69140,#69141,
#69142,#69143,#69144,#69145,#69146,#69147,#69148,#69149,#69150,#69151,#69152,
#69153,#69154,#69155,#69156,#69157,#69158,#69159,#69160,#69161,#69162,#69163,
#69164,#69165,#69166,#69167,#69168,#69169,#69170,#69171,#69172,#69173,#69174,
#69175,#69176,#69177,#69178,#69179,#69180,#69181,#69182,#69183,#69184,#69185,
#69186,#69187,#69188,#69189,#69190,#69191,#69192,#69193,#69194,#69195,#69196,
#69197,#69198,#69199,#69200,#69201,#69202,#69203,#69204,#69205,#69206,#69207,
#69208,#69209,#69210,#69211,#69212,#69213,#69214,#69215,#69216,#69217,#69218,
#69219,#69220,#69221,#69222,#69223,#69224),.UNSPECIFIED.,.F.,.F.,(4,3,3,
3,3,3,3,3,3,3,3,3,3,3,3,3,3,3,3,3,3,3,3,3,3,3,3,3,3,3,3,3,3,3,3,3,3,3,3,
3,3,3,3,3,3,3,3,3,3,3,3,3,3,3,3,3,3,3,3,3,3,3,4),(-48.0738672208646,-47.9245464455612,
-47.824840471252,-47.725277235593,-47.6255718955484,-47.5261872977941,-47.4268354030607,
-47.327485782509,-47.2275229656908,-47.128029102039,-47.0278318086377,-46.9276345152365,
-46.8279285369865,-46.7283652973229,-46.6286599582715,-46.5292753563869,
-46.4299234574851,-46.3305738327324,-46.2306110207772,-46.1311171528873,
-46.0309198688996,-45.9307225849118,-45.8310166079799,-45.7314533696477,
-45.6317480302652,-45.5323634297345,-45.433011532192,-45.3336619088021,
-45.2336990952484,-45.1342052287161,-45.0340079416516,-44.9338106545871,
-44.8341046779189,-44.734541439859,-44.6348361004094,-44.53545150017,-44.4360996029253,
-44.3367499798393,-44.2367871659451,-44.1372932997287,-44.0370960119956,
-43.9368987242624,-43.8371927471253,-43.7376295085886,-43.6379241692572,
-43.5385395685251,-43.4391876707829,-43.3398380471953,-43.2398752338809,
-43.1403813671576,-43.0401840805477,-42.9399867939377,-42.8402808169886,
-42.7407175786422,-42.6410122392635,-42.5416276387255,-42.4422757411784,
-42.3429261177866,-42.2429633042431,-42.1434694377156,-42.0432721506642,
-41.9430748636129,-41.790681913685),.UNSPECIFIED.);
#724=B_SPLINE_CURVE_WITH_KNOTS('',3,(#69226,#69227,#69228,#69229,#69230,
#69231,#69232,#69233,#69234,#69235,#69236,#69237,#69238,#69239,#69240,#69241,
#69242,#69243,#69244,#69245,#69246,#69247,#69248,#69249,#69250,#69251,#69252,
#69253,#69254,#69255,#69256,#69257,#69258,#69259,#69260,#69261,#69262,#69263,
#69264,#69265,#69266,#69267,#69268,#69269,#69270,#69271,#69272,#69273,#69274,
#69275,#69276,#69277,#69278,#69279,#69280,#69281,#69282,#69283,#69284,#69285,
#69286,#69287,#69288,#69289,#69290,#69291,#69292,#69293,#69294,#69295,#69296,
#69297,#69298,#69299,#69300,#69301,#69302,#69303,#69304,#69305,#69306,#69307,
#69308,#69309,#69310,#69311,#69312,#69313,#69314,#69315,#69316,#69317,#69318,
#69319,#69320,#69321,#69322,#69323,#69324,#69325,#69326,#69327,#69328,#69329,
#69330,#69331,#69332,#69333,#69334,#69335,#69336,#69337,#69338,#69339,#69340,
#69341,#69342,#69343,#69344,#69345,#69346,#69347,#69348,#69349,#69350,#69351,
#69352,#69353,#69354,#69355,#69356,#69357,#69358,#69359,#69360,#69361,#69362,
#69363,#69364,#69365,#69366,#69367,#69368,#69369,#69370,#69371,#69372,#69373,
#69374,#69375,#69376,#69377,#69378,#69379,#69380,#69381,#69382,#69383,#69384,
#69385,#69386,#69387,#69388,#69389,#69390,#69391,#69392,#69393,#69394,#69395,
#69396,#69397,#69398,#69399,#69400,#69401,#69402,#69403,#69404,#69405,#69406,
#69407,#69408,#69409,#69410,#69411,#69412,#69413,#69414,#69415,#69416,#69417,
#69418),.UNSPECIFIED.,.F.,.F.,(4,3,3,3,3,3,3,3,3,3,3,3,3,3,3,3,3,3,3,3,
3,3,3,3,3,3,3,3,3,3,3,3,3,3,3,3,3,3,3,3,3,3,3,3,3,3,3,3,3,3,3,3,3,3,3,3,
3,3,3,3,3,3,3,3,4),(-41.7906819133136,-41.6925640062099,-41.5945653582671,
-41.4966311262791,-41.3987292076811,-41.3008275445918,-41.2028311665152,
-41.104783880033,-41.0065724507144,-40.9461629332882,-40.8464569562993,
-40.7468937179126,-40.647188378544,-40.5478037779658,-40.4484518803784,
-40.3491022569467,-40.2491394434509,-40.149645576884,-40.0494482899238,
-39.9492510029635,-39.8495450260004,-39.7499817876397,-39.6502764482646,
-39.5508918477131,-39.4515399501526,-39.3521903267478,-39.2522275132206,
-39.1527336466808,-39.0525363596598,-38.9523390726388,-38.8526330956752,
-38.7530698573145,-38.6533645179394,-38.5539799173876,-38.4546280198271,
-38.355278396422,-38.255315582895,-38.1558217163552,-38.0556244293346,-37.9554271423141,
-37.8557211653444,-37.7561579269774,-37.6564525876039,-37.5570679870457,
-37.4577160894784,-37.3583664660668,-37.2584036525475,-37.158909786001,
-37.0587124989952,-36.9585152119894,-36.8588092350233,-36.75924599666,-36.6595406572856,
-36.5601560567309,-36.4608041591676,-36.3614545357598,-36.261491722236,
-36.1619978556932,-36.0618005686789,-35.9616032816647,-35.8544601488088,
-35.7476875248841,-35.6411508212861,-35.5349368592938,-35.5074966067279),
 .UNSPECIFIED.);
#725=B_SPLINE_CURVE_WITH_KNOTS('',3,(#69420,#69421,#69422,#69423,#69424,
#69425,#69426,#69427,#69428,#69429,#69430,#69431,#69432,#69433,#69434,#69435,
#69436,#69437,#69438,#69439,#69440,#69441,#69442,#69443,#69444,#69445,#69446,
#69447,#69448,#69449,#69450,#69451,#69452,#69453,#69454,#69455,#69456,#69457,
#69458,#69459,#69460,#69461,#69462,#69463,#69464,#69465,#69466,#69467,#69468,
#69469,#69470,#69471,#69472,#69473,#69474,#69475,#69476,#69477,#69478,#69479,
#69480,#69481,#69482,#69483,#69484,#69485,#69486,#69487,#69488,#69489,#69490,
#69491,#69492,#69493,#69494,#69495,#69496,#69497,#69498,#69499,#69500,#69501,
#69502,#69503,#69504,#69505,#69506,#69507,#69508,#69509,#69510,#69511,#69512,
#69513,#69514,#69515,#69516,#69517,#69518,#69519,#69520,#69521,#69522,#69523,
#69524,#69525,#69526,#69527,#69528,#69529,#69530,#69531,#69532,#69533,#69534,
#69535,#69536,#69537,#69538,#69539,#69540,#69541,#69542,#69543,#69544,#69545,
#69546,#69547,#69548,#69549,#69550,#69551,#69552,#69553,#69554,#69555,#69556,
#69557,#69558,#69559,#69560,#69561,#69562,#69563,#69564,#69565,#69566,#69567,
#69568,#69569,#69570,#69571,#69572,#69573,#69574,#69575,#69576,#69577,#69578,
#69579,#69580,#69581,#69582,#69583,#69584,#69585,#69586,#69587,#69588,#69589,
#69590,#69591,#69592,#69593,#69594,#69595,#69596,#69597,#69598,#69599,#69600,
#69601,#69602,#69603,#69604,#69605,#69606,#69607,#69608,#69609,#69610,#69611,
#69612),.UNSPECIFIED.,.F.,.F.,(4,3,3,3,3,3,3,3,3,3,3,3,3,3,3,3,3,3,3,3,
3,3,3,3,3,3,3,3,3,3,3,3,3,3,3,3,3,3,3,3,3,3,3,3,3,3,3,3,3,3,3,3,3,3,3,3,
3,3,3,3,3,3,3,3,4),(-35.5074966065053,-35.4051595705186,-35.3027289474575,
-35.2000975899008,-35.0973517910919,-34.9943911189887,-34.9646913513399,
-34.8649853743722,-34.7654221360073,-34.6657167966333,-34.5663321960772,
-34.4669802985123,-34.367630675103,-34.267667861581,-34.1681739950367,-34.067976708026,
-33.9677794210152,-33.8680734440487,-33.768510205685,-33.6688048663107,
-33.5694202657559,-33.4700683681921,-33.370718744784,-33.2707559312606,
-33.1712620647175,-33.071064777704,-32.9708674906905,-32.8711615137242,
-32.7715982753605,-32.6718929359862,-32.5725083354315,-32.4731564378678,
-32.37380681446,-32.2738440009364,-32.1743501343935,-32.0741528473796,-31.9739555603658,
-31.8742495833959,-31.7746863450287,-31.6749810056553,-31.5755964050969,
-31.4762445075297,-31.3768948841183,-31.276932070599,-31.1774382040526,
-31.0772409170468,-30.9770436300411,-30.877337653078,-30.7777744147177,
-30.6780690753425,-30.5786844747909,-30.4793325772303,-30.3799829538252,
-30.280020140298,-30.180526273758,-30.0803289867372,-29.9801316997164,-29.8816680285451,
-29.7833326010158,-29.6850933512488,-29.5869183344749,-29.4887449677475,
-29.3905760088001,-29.2923247508768,-29.2243112993258),.UNSPECIFIED.);
#726=B_SPLINE_CURVE_WITH_KNOTS('',3,(#69614,#69615,#69616,#69617,#69618,
#69619,#69620,#69621,#69622,#69623,#69624,#69625,#69626,#69627,#69628,#69629,
#69630,#69631,#69632,#69633,#69634,#69635,#69636,#69637,#69638,#69639,#69640,
#69641,#69642,#69643,#69644,#69645,#69646,#69647,#69648,#69649,#69650,#69651,
#69652,#69653,#69654,#69655,#69656,#69657,#69658,#69659,#69660,#69661,#69662,
#69663,#69664,#69665,#69666,#69667,#69668,#69669,#69670,#69671,#69672,#69673,
#69674,#69675,#69676,#69677,#69678,#69679,#69680,#69681,#69682,#69683,#69684,
#69685,#69686,#69687,#69688,#69689,#69690,#69691,#69692,#69693,#69694,#69695,
#69696,#69697,#69698,#69699,#69700,#69701,#69702,#69703,#69704,#69705,#69706,
#69707,#69708,#69709,#69710,#69711,#69712,#69713,#69714,#69715,#69716,#69717,
#69718,#69719,#69720,#69721,#69722,#69723,#69724,#69725,#69726,#69727,#69728,
#69729,#69730,#69731,#69732,#69733,#69734,#69735,#69736,#69737,#69738,#69739,
#69740,#69741,#69742,#69743,#69744,#69745,#69746,#69747,#69748,#69749,#69750,
#69751,#69752,#69753,#69754,#69755,#69756,#69757,#69758,#69759,#69760,#69761,
#69762,#69763,#69764,#69765,#69766,#69767,#69768,#69769,#69770,#69771,#69772,
#69773,#69774,#69775,#69776,#69777,#69778,#69779,#69780,#69781,#69782,#69783,
#69784,#69785,#69786,#69787,#69788,#69789,#69790,#69791,#69792,#69793,#69794,
#69795,#69796,#69797,#69798,#69799,#69800,#69801,#69802,#69803),
 .UNSPECIFIED.,.F.,.F.,(4,3,3,3,3,3,3,3,3,3,3,3,3,3,3,3,3,3,3,3,3,3,3,3,
3,3,3,3,3,3,3,3,3,3,3,3,3,3,3,3,3,3,3,3,3,3,3,3,3,3,3,3,3,3,3,3,3,3,3,3,
3,3,3,4),(-29.2243112990037,-29.0935052524198,-28.9832197693916,-28.8835137924016,
-28.7839505540141,-28.6842452146457,-28.5848606140673,-28.4855087164801,
-28.3861590930487,-28.2861962795532,-28.1867024129872,-28.086505126027,
-27.9863078390669,-27.8866018621359,-27.7870386238074,-27.6873332844243,
-27.5879486839043,-27.4885967863751,-27.3892471630013,-27.2892843494365,
-27.1897904829265,-27.0895931958344,-26.9893959087422,-26.8896899317904,
-26.7901266934417,-26.6904213540637,-26.5910367535249,-26.4916848559776,
-26.3923352325861,-26.292372419044,-26.192878552518,-26.0926812654677,-25.9924839784175,
-25.8927780012723,-25.7932147627291,-25.6935094233996,-25.5941248226654,
-25.4947729249228,-25.3954233013364,-25.2954604880255,-25.1959666213074,
-25.0957693347001,-24.9955720480928,-24.8958660714534,-24.796302833416,
-24.69659749396,-24.5972128937279,-24.4978609964848,-24.3985113733948,-24.2985485594881,
-24.1990546932537,-24.0988574055109,-23.9986601177681,-23.8989541408065,
-23.7993909024511,-23.6996855630751,-23.6003009625368,-23.5009490649927,
-23.4015994416071,-23.3016366280662,-23.2021427615525,-23.101945474498,
-23.0017481874434,-22.9411259921462),.UNSPECIFIED.);
#727=B_SPLINE_CURVE_WITH_KNOTS('',3,(#69805,#69806,#69807,#69808,#69809,
#69810,#69811,#69812,#69813,#69814,#69815,#69816,#69817,#69818,#69819,#69820,
#69821,#69822,#69823,#69824,#69825,#69826,#69827,#69828,#69829,#69830,#69831,
#69832,#69833,#69834,#69835,#69836,#69837,#69838,#69839,#69840,#69841,#69842,
#69843,#69844,#69845,#69846,#69847,#69848,#69849,#69850,#69851,#69852,#69853,
#69854,#69855,#69856,#69857,#69858,#69859,#69860,#69861,#69862,#69863,#69864,
#69865,#69866,#69867,#69868,#69869,#69870,#69871,#69872,#69873,#69874,#69875,
#69876,#69877,#69878,#69879,#69880,#69881,#69882,#69883,#69884,#69885,#69886,
#69887,#69888,#69889,#69890,#69891,#69892,#69893,#69894,#69895,#69896,#69897,
#69898,#69899,#69900,#69901,#69902,#69903,#69904,#69905,#69906,#69907,#69908,
#69909,#69910,#69911,#69912,#69913,#69914,#69915,#69916,#69917,#69918,#69919,
#69920,#69921,#69922,#69923,#69924,#69925,#69926,#69927,#69928,#69929,#69930,
#69931,#69932,#69933,#69934,#69935,#69936,#69937,#69938,#69939,#69940,#69941,
#69942,#69943,#69944,#69945,#69946,#69947,#69948,#69949,#69950,#69951,#69952,
#69953,#69954,#69955,#69956,#69957,#69958,#69959,#69960,#69961,#69962,#69963,
#69964,#69965,#69966,#69967,#69968,#69969,#69970,#69971,#69972,#69973,#69974,
#69975,#69976,#69977,#69978,#69979,#69980,#69981,#69982,#69983,#69984,#69985,
#69986,#69987,#69988,#69989,#69990,#69991,#69992,#69993,#69994,#69995,#69996,
#69997),.UNSPECIFIED.,.F.,.F.,(4,3,3,3,3,3,3,3,3,3,3,3,3,3,3,3,3,3,3,3,
3,3,3,3,3,3,3,3,3,3,3,3,3,3,3,3,3,3,3,3,3,3,3,3,3,3,3,3,3,3,3,3,3,3,3,3,
3,3,3,3,3,3,3,3,4),(-22.9411259917771,-22.8423298884581,-22.7436701923909,
-22.6451152123133,-22.5466155817799,-22.4481397693788,-22.3496562767237,
-22.2510711285813,-22.1524289845342,-22.0536236607553,-22.0048362571186,
-21.9051302830416,-21.8055670475646,-21.7058617074683,-21.6064771097735,
-21.5071252150533,-21.4077755944685,-21.3078127775499,-21.2083189137523,
-21.1081216202731,-21.0079243267939,-20.9082183489098,-20.8086551096547,
-20.7089497705065,-20.6095651691311,-20.5102132707748,-20.4108636466031,
-20.3109008340696,-20.2114069668409,-20.111209681655,-20.0110123964692,
-19.9113064098326,-19.8117431617508,-19.7120378248,-19.6126532144827,-19.5133013071616,
-19.4139516740144,-19.3139888720469,-19.2144949959087,-19.1142977310266,
-19.0141004661445,-18.9143945139796,-18.8148313004146,-18.7151259548402,
-18.6157413788972,-18.5163895058211,-18.4170399067437,-18.3170770640127,
-18.2175832211708,-18.1173858784953,-18.0171885358198,-17.917482543784,
-17.8179192905504,-17.7182139549185,-17.6188293400818,-17.5194774284872,
-17.420127791317,-17.3201649948615,-17.2206711153469,-17.120473860421,-17.0202766054951,
-16.9063917652444,-16.7929807702555,-16.6803704353785,-16.6579406851942),
 .UNSPECIFIED.);
#728=B_SPLINE_CURVE_WITH_KNOTS('',3,(#69999,#70000,#70001,#70002,#70003,
#70004,#70005,#70006,#70007,#70008,#70009,#70010,#70011,#70012,#70013,#70014,
#70015,#70016,#70017,#70018,#70019,#70020,#70021,#70022,#70023,#70024,#70025,
#70026,#70027,#70028,#70029,#70030,#70031,#70032,#70033,#70034,#70035,#70036,
#70037,#70038,#70039,#70040,#70041,#70042,#70043,#70044,#70045,#70046,#70047,
#70048,#70049,#70050,#70051,#70052,#70053,#70054,#70055,#70056,#70057,#70058,
#70059,#70060,#70061,#70062,#70063,#70064,#70065,#70066,#70067,#70068,#70069,
#70070,#70071,#70072,#70073,#70074,#70075,#70076,#70077,#70078,#70079,#70080,
#70081,#70082,#70083,#70084,#70085,#70086,#70087,#70088,#70089,#70090,#70091,
#70092,#70093,#70094,#70095,#70096,#70097,#70098,#70099,#70100,#70101,#70102,
#70103,#70104,#70105,#70106,#70107,#70108,#70109,#70110,#70111,#70112,#70113,
#70114,#70115,#70116,#70117,#70118,#70119,#70120,#70121,#70122,#70123,#70124,
#70125,#70126,#70127,#70128,#70129,#70130,#70131,#70132,#70133,#70134,#70135,
#70136,#70137,#70138,#70139,#70140,#70141,#70142,#70143,#70144,#70145,#70146,
#70147,#70148,#70149,#70150,#70151,#70152,#70153,#70154,#70155,#70156,#70157,
#70158,#70159,#70160,#70161,#70162,#70163,#70164,#70165,#70166,#70167,#70168,
#70169,#70170,#70171,#70172,#70173,#70174,#70175,#70176,#70177,#70178,#70179,
#70180,#70181,#70182,#70183,#70184,#70185,#70186,#70187,#70188,#70189,#70190,
#70191),.UNSPECIFIED.,.F.,.F.,(4,3,3,3,3,3,3,3,3,3,3,3,3,3,3,3,3,3,3,3,
3,3,3,3,3,3,3,3,3,3,3,3,3,3,3,3,3,3,3,3,3,3,3,3,3,3,3,3,3,3,3,3,3,3,3,3,
3,3,3,3,3,3,3,3,4),(-16.6579406849666,-16.5580934344199,-16.4582422444312,
-16.3583577075461,-16.258342944254,-16.1582524650089,-16.0579861672984,
-16.0233646751703,-15.923658905856,-15.8240958752626,-15.7243904839604,
-15.625006089955,-15.5256543980263,-15.4263049790649,-15.3263419205101,
-15.2268482534387,-15.1266504991422,-15.0264527448456,-14.9267465864787,
-14.8271831681702,-14.727477873964,-14.6280930982588,-14.5287410277233,
-14.4293912337434,-14.3294286289377,-14.2299345993823,-14.1297377069516,
-14.0295408145209,-13.9298343947855,-13.8302707099986,-13.7305654817733,
-13.6311804292655,-13.5318280786876,-13.4324780018285,-13.3325157224204,
-13.2330214060225,-13.1328251451094,-13.0326288841962,-12.9329246058058,
-12.833363068111,-12.7336573038311,-12.6342743966511,-12.5349241859803,
-12.4355762407301,-12.3356114190155,-12.2361191922637,-12.1359180730676,
-12.0357169538715,-11.9360090584454,-11.8364439118102,-11.7367390507773,
-11.6373525802036,-11.5379988310565,-11.4386473768989,-11.3386867885609,
-11.2391911604896,-11.1389980920182,-11.0388050235468,-10.9391546302479,
-10.8396437149114,-10.740241606817,-10.6409133704535,-10.5416298901773,
-10.4423315635812,-10.374755377787),.UNSPECIFIED.);
#729=B_SPLINE_CURVE_WITH_KNOTS('',3,(#70192,#70193,#70194,#70195,#70196,
#70197,#70198,#70199,#70200,#70201,#70202,#70203,#70204,#70205,#70206,#70207,
#70208,#70209,#70210,#70211,#70212,#70213,#70214,#70215,#70216,#70217,#70218,
#70219,#70220,#70221,#70222,#70223,#70224,#70225,#70226,#70227,#70228,#70229,
#70230,#70231,#70232,#70233,#70234,#70235,#70236,#70237,#70238,#70239,#70240,
#70241,#70242,#70243,#70244,#70245,#70246,#70247,#70248,#70249,#70250,#70251,
#70252,#70253,#70254,#70255,#70256,#70257,#70258,#70259,#70260,#70261,#70262,
#70263,#70264,#70265,#70266,#70267,#70268,#70269,#70270,#70271,#70272,#70273,
#70274,#70275,#70276,#70277,#70278,#70279,#70280,#70281,#70282,#70283,#70284,
#70285,#70286,#70287,#70288,#70289,#70290,#70291,#70292,#70293,#70294,#70295,
#70296,#70297,#70298,#70299,#70300,#70301,#70302,#70303,#70304,#70305,#70306,
#70307,#70308,#70309,#70310,#70311,#70312,#70313,#70314,#70315,#70316,#70317,
#70318,#70319,#70320,#70321,#70322,#70323,#70324,#70325,#70326,#70327,#70328,
#70329,#70330,#70331,#70332,#70333,#70334,#70335,#70336,#70337,#70338,#70339,
#70340,#70341,#70342,#70343,#70344,#70345,#70346,#70347,#70348,#70349,#70350,
#70351,#70352,#70353,#70354,#70355,#70356,#70357,#70358,#70359,#70360,#70361,
#70362,#70363,#70364,#70365,#70366,#70367,#70368,#70369,#70370,#70371,#70372,
#70373,#70374,#70375,#70376,#70377,#70378,#70379,#70380,#70381),
 .UNSPECIFIED.,.F.,.F.,(4,3,3,3,3,3,3,3,3,3,3,3,3,3,3,3,3,3,3,3,3,3,3,3,
3,3,3,3,3,3,3,3,3,3,3,3,3,3,3,3,3,3,3,3,3,3,3,3,3,3,3,3,3,3,3,3,3,3,3,3,
3,3,3,4),(-10.3747553775759,-10.2591101330065,-10.1422757994338,-10.0418930932221,
-9.94220069316546,-9.84265105744093,-9.74294232062298,-9.64357128606953,
-9.54423291077586,-9.44489674782431,-9.34491785159257,-9.24543715783758,
-9.14520916036746,-9.04498116289735,-8.9452563413951,-8.84567432613174,
-8.74597368943685,-8.64657061042831,-8.54720038699816,-8.44783261431723,
-8.34789176888108,-8.24838036694254,-8.14822479975759,-8.04806923257263,
-7.94834950285117,-7.84877225956233,-7.74907038989803,-7.64967128144482,
-7.55030472044975,-7.45094029914482,-7.35099454992059,-7.25148571213079,
-7.15132150718935,-7.05115730224791,-6.95155715616721,-6.85210001837247,
-6.75236818756631,-6.65308957648869,-6.55384339551515,-6.45459907611016,
-6.35451065006342,-6.25512001485721,-6.15468269339021,-6.0542453719232,
-5.95436295273983,-5.85462368971806,-5.75496240870311,-5.65540408598084,
-5.55587972319795,-5.45635912459957,-5.3566027038493,-5.25694323810271,
-5.15710663205714,-5.05733344159848,-4.95810738230795,-4.85902171181877,
-4.76004703457688,-4.66113224957557,-4.56224628842496,-4.46335811984981,
-4.36437074477041,-4.26533216177527,-4.16612178033553,-4.09157041827049),
 .UNSPECIFIED.);
#730=B_SPLINE_CURVE_WITH_KNOTS('',3,(#70384,#70385,#70386,#70387,#70388,
#70389,#70390,#70391,#70392,#70393,#70394,#70395,#70396,#70397,#70398,#70399,
#70400,#70401,#70402,#70403,#70404,#70405,#70406,#70407,#70408,#70409,#70410,
#70411,#70412,#70413,#70414,#70415,#70416,#70417),.UNSPECIFIED.,.F.,.F.,
(4,3,3,3,3,3,3,3,3,3,3,4),(71.1940098997199,71.2987359719931,71.4036584532844,
71.5038828067993,71.607596420869,71.7111684685388,71.8146363092789,71.9180371573734,
72.0214389095813,72.1248428520168,72.2283284120281,72.2566310325653),
 .UNSPECIFIED.);
#731=B_SPLINE_CURVE_WITH_KNOTS('',3,(#70419,#70420,#70421,#70422,#70423,
#70424,#70425,#70426,#70427,#70428,#70429,#70430,#70431,#70432,#70433,#70434,
#70435,#70436,#70437,#70438,#70439,#70440,#70441,#70442,#70443,#70444,#70445,
#70446,#70447,#70448,#70449,#70450,#70451,#70452,#70453,#70454,#70455,#70456,
#70457,#70458,#70459,#70460,#70461,#70462,#70463,#70464,#70465,#70466,#70467,
#70468,#70469,#70470,#70471,#70472,#70473,#70474,#70475,#70476,#70477,#70478,
#70479,#70480,#70481,#70482,#70483,#70484,#70485,#70486,#70487,#70488,#70489,
#70490,#70491,#70492,#70493,#70494,#70495,#70496,#70497,#70498,#70499,#70500,
#70501,#70502,#70503,#70504,#70505,#70506,#70507,#70508,#70509,#70510,#70511,
#70512,#70513,#70514,#70515,#70516,#70517,#70518,#70519,#70520,#70521,#70522,
#70523,#70524,#70525,#70526,#70527,#70528,#70529,#70530,#70531,#70532,#70533,
#70534,#70535,#70536,#70537,#70538,#70539,#70540,#70541,#70542),
 .UNSPECIFIED.,.F.,.F.,(4,3,3,3,3,3,3,3,3,3,3,3,3,3,3,3,3,3,3,3,3,3,3,3,
3,3,3,3,3,3,3,3,3,3,3,3,3,3,3,3,3,4),(72.2566310329874,72.3935845469085,
72.500794737124,72.6057786247621,72.7106055714104,72.8153098988276,72.9199487824371,
73.0245577431498,73.1291722582607,73.233897426931,73.3386840147705,73.4436520658765,
73.4977066674487,73.6025646586816,73.7072651358392,73.8118427580766,73.916354860038,
74.0208371502974,74.1253252938358,74.2299254067418,74.3345874987602,74.4394332502781,
74.4946185977734,74.5997737631742,74.7047712383462,74.8096441674778,74.9144503584131,
75.019225085812,75.1240035792051,75.2288889103067,75.3338337191025,75.4389553227352,
75.4915305280982,75.5954266638067,75.699148837704,75.8027739576774,75.9063390395231,
76.0098810172454,76.1135062214272,76.2171700260122,76.3210160814776,76.4156412590678),
 .UNSPECIFIED.);
#732=B_SPLINE_CURVE_WITH_KNOTS('',3,(#70545,#70546,#70547,#70548,#70549,
#70550,#70551,#70552,#70553,#70554,#70555,#70556,#70557,#70558,#70559,#70560,
#70561,#70562,#70563,#70564,#70565,#70566,#70567,#70568,#70569,#70570,#70571,
#70572,#70573,#70574,#70575,#70576,#70577,#70578,#70579,#70580,#70581,#70582,
#70583,#70584,#70585,#70586,#70587,#70588,#70589,#70590,#70591,#70592,#70593,
#70594,#70595,#70596,#70597,#70598,#70599,#70600,#70601,#70602,#70603,#70604,
#70605,#70606,#70607,#70608,#70609,#70610,#70611,#70612,#70613,#70614,#70615,
#70616,#70617,#70618,#70619,#70620,#70621,#70622,#70623,#70624,#70625,#70626,
#70627,#70628,#70629,#70630,#70631,#70632,#70633,#70634,#70635,#70636,#70637,
#70638,#70639,#70640,#70641,#70642,#70643,#70644,#70645,#70646,#70647,#70648,
#70649,#70650,#70651,#70652,#70653,#70654,#70655,#70656,#70657,#70658),
 .UNSPECIFIED.,.F.,.F.,(4,2,2,2,2,2,2,2,2,2,2,2,2,2,2,2,2,2,2,2,2,2,2,2,
2,2,2,2,2,2,2,2,2,2,2,2,2,2,2,2,2,2,2,2,2,2,2,2,2,2,2,2,2,2,2,2,4),(-1.83983945624295,
-1.83795397537346,-1.83573652513345,-1.82949843462936,-1.79178426308305,
-1.76296147372845,-1.75453667498902,-1.7486351304989,-1.74325086347128,
-1.73439828645192,-1.70725676385421,-1.66626641078697,-1.64910413130173,
-1.64422596375543,-1.64112570463183,-1.63844711672127,-1.63388566353806,
-1.61996621044673,-1.57569789052089,-1.55447720636594,-1.5471665286971,
-1.54207966082191,-1.53689493023208,-1.52907708541865,-1.50552707052677,
-1.46407541746046,-1.45269140278871,-1.444811032953,-1.44124797603105,-1.438683102287,
-1.43521655468152,-1.42867176437277,-1.4021719058181,-1.36984066765876,
-1.35111068785806,-1.343833908549,-1.33852386818394,-1.33287687770572,-1.32380860300783,
-1.27821947713036,-1.259205164698,-1.24799348242959,-1.2437417789513,-1.24073351187944,
-1.23729752844853,-1.23100354292647,-1.19611231183529,-1.16969535698436,
-1.15303889570976,-1.14607155381394,-1.14083464371401,-1.13512337698453,
-1.12562653131419,-1.0813412211916,-1.05133401436251,-1.04567072466869,
-1.0443153183833),.UNSPECIFIED.);
#733=B_SPLINE_CURVE_WITH_KNOTS('',3,(#70931,#70932,#70933,#70934,#70935,
#70936,#70937,#70938,#70939,#70940,#70941,#70942,#70943,#70944,#70945,#70946,
#70947,#70948,#70949,#70950,#70951,#70952,#70953,#70954,#70955,#70956,#70957,
#70958,#70959,#70960,#70961,#70962,#70963,#70964,#70965,#70966,#70967,#70968,
#70969,#70970,#70971,#70972,#70973,#70974,#70975,#70976,#70977,#70978,#70979,
#70980,#70981,#70982,#70983,#70984,#70985,#70986,#70987,#70988,#70989,#70990,
#70991,#70992,#70993,#70994,#70995,#70996,#70997,#70998,#70999,#71000,#71001,
#71002,#71003,#71004,#71005,#71006,#71007,#71008,#71009,#71010,#71011,#71012,
#71013,#71014,#71015),.UNSPECIFIED.,.F.,.F.,(4,3,3,3,3,3,3,3,3,3,3,3,3,
3,3,3,3,3,3,3,3,3,3,3,3,3,3,3,4),(-0.463803050843692,-0.449070703225483,
-0.42735479445911,-0.415189549046521,-0.410496202330004,-0.406058805975524,
-0.383404300327137,-0.364881814729665,-0.357461864595492,-0.352400732469066,
-0.329036435798896,-0.305267012368989,-0.287822011874325,-0.274662752749041,
-0.270903259004613,-0.246475346213267,-0.23536348442085,-0.211528359113113,
-0.187693233805376,-0.183684004614737,-0.159318899344364,-0.134503159343954,
-0.109395145221359,-0.0938232102629364,-0.0899531631052965,-0.0642046403497918,
-0.0384306169102492,-0.0132144355033025,0.),.UNSPECIFIED.);
#734=B_SPLINE_CURVE_WITH_KNOTS('',3,(#71020,#71021,#71022,#71023,#71024,
#71025,#71026,#71027,#71028,#71029,#71030,#71031,#71032,#71033,#71034,#71035,
#71036,#71037,#71038,#71039,#71040,#71041,#71042,#71043,#71044,#71045,#71046,
#71047,#71048,#71049,#71050,#71051,#71052,#71053,#71054,#71055,#71056,#71057,
#71058,#71059,#71060,#71061,#71062,#71063,#71064,#71065,#71066,#71067,#71068,
#71069,#71070,#71071,#71072,#71073,#71074,#71075,#71076,#71077,#71078,#71079,
#71080,#71081,#71082,#71083,#71084,#71085,#71086,#71087,#71088,#71089,#71090,
#71091,#71092,#71093,#71094,#71095,#71096,#71097,#71098,#71099,#71100,#71101,
#71102,#71103,#71104,#71105,#71106,#71107),.UNSPECIFIED.,.F.,.F.,(4,3,3,
3,3,3,3,3,3,3,3,3,3,3,3,3,3,3,3,3,3,3,3,3,3,3,3,3,3,4),(-0.45706977230884,
-0.444522365548672,-0.418899005513524,-0.405945758827233,-0.399313330176187,
-0.394631600643061,-0.369313518144253,-0.344021007921678,-0.340358828086956,
-0.336108374295373,-0.33175454364197,-0.307004890679168,-0.282783792225254,
-0.259078063661601,-0.248631875962901,-0.244428173588767,-0.220936136292426,
-0.211647058532859,-0.187586133721808,-0.164224619203416,-0.15876767775089,
-0.135435698638008,-0.112185513746461,-0.089130325712887,-0.0803330397173641,
-0.0766181939392614,-0.0541584315341221,-0.0320645162777776,-0.0106795002206658,
0.),.UNSPECIFIED.);
#735=B_SPLINE_CURVE_WITH_KNOTS('',3,(#71389,#71390,#71391,#71392),
 .UNSPECIFIED.,.F.,.F.,(4,4),(-0.0469525346883488,0.),.UNSPECIFIED.);
#819=SHAPE_REPRESENTATION_RELATIONSHIP('SRR','None',#81138,#829);
#829=ADVANCED_BREP_SHAPE_REPRESENTATION('',(#849),#81038);
#839=STYLED_ITEM('',(#81197),#849);
#849=MANIFOLD_SOLID_BREP('Body1',#15092);
#1055=CYLINDRICAL_SURFACE('',#16451,1.99475);
#1056=CYLINDRICAL_SURFACE('',#16453,1.99475);
#1057=CYLINDRICAL_SURFACE('',#16455,1.99475);
#1058=CYLINDRICAL_SURFACE('',#16456,1.99475);
#1059=CYLINDRICAL_SURFACE('',#16457,1.99475);
#1060=CYLINDRICAL_SURFACE('',#16458,1.99475);
#1061=CYLINDRICAL_SURFACE('',#16459,1.99475);
#1062=CYLINDRICAL_SURFACE('',#16460,1.99475);
#1063=CYLINDRICAL_SURFACE('',#16461,1.99475);
#1064=CYLINDRICAL_SURFACE('',#16462,1.99475);
#1065=CYLINDRICAL_SURFACE('',#16468,2.4505);
#1066=CYLINDRICAL_SURFACE('',#16471,1.99475);
#1067=CYLINDRICAL_SURFACE('',#16508,4.75);
#1209=FACE_BOUND('',#3174,.T.);
#1583=PLANE('',#16474);
#1584=PLANE('',#16477);
#1585=PLANE('',#16481);
#1586=PLANE('',#16483);
#1587=PLANE('',#16485);
#1588=PLANE('',#16487);
#1589=PLANE('',#16489);
#1590=PLANE('',#16491);
#1591=PLANE('',#16493);
#1592=PLANE('',#16496);
#1593=PLANE('',#16498);
#1594=PLANE('',#16500);
#1595=PLANE('',#16502);
#1596=PLANE('',#16504);
#1597=PLANE('',#16506);
#2285=FACE_OUTER_BOUND('',#3154,.T.);
#2286=FACE_OUTER_BOUND('',#3155,.T.);
#2287=FACE_OUTER_BOUND('',#3156,.T.);
#2288=FACE_OUTER_BOUND('',#3157,.T.);
#2289=FACE_OUTER_BOUND('',#3158,.T.);
#2290=FACE_OUTER_BOUND('',#3159,.T.);
#2291=FACE_OUTER_BOUND('',#3160,.T.);
#2292=FACE_OUTER_BOUND('',#3161,.T.);
#2293=FACE_OUTER_BOUND('',#3162,.T.);
#2294=FACE_OUTER_BOUND('',#3163,.T.);
#2295=FACE_OUTER_BOUND('',#3164,.T.);
#2296=FACE_OUTER_BOUND('',#3165,.T.);
#2297=FACE_OUTER_BOUND('',#3166,.T.);
#2298=FACE_OUTER_BOUND('',#3167,.T.);
#2299=FACE_OUTER_BOUND('',#3168,.T.);
#2300=FACE_OUTER_BOUND('',#3169,.T.);
#2301=FACE_OUTER_BOUND('',#3170,.T.);
#2302=FACE_OUTER_BOUND('',#3171,.T.);
#2303=FACE_OUTER_BOUND('',#3172,.T.);
#2304=FACE_OUTER_BOUND('',#3173,.T.);
#2305=FACE_OUTER_BOUND('',#3175,.T.);
#2306=FACE_OUTER_BOUND('',#3176,.T.);
#2307=FACE_OUTER_BOUND('',#3177,.T.);
#2308=FACE_OUTER_BOUND('',#3178,.T.);
#2309=FACE_OUTER_BOUND('',#3179,.T.);
#2310=FACE_OUTER_BOUND('',#3180,.T.);
#2311=FACE_OUTER_BOUND('',#3181,.T.);
#2312=FACE_OUTER_BOUND('',#3182,.T.);
#2313=FACE_OUTER_BOUND('',#3183,.T.);
#2314=FACE_OUTER_BOUND('',#3184,.T.);
#2315=FACE_OUTER_BOUND('',#3185,.T.);
#2316=FACE_OUTER_BOUND('',#3186,.T.);
#2317=FACE_OUTER_BOUND('',#3187,.T.);
#2318=FACE_OUTER_BOUND('',#3188,.T.);
#2319=FACE_OUTER_BOUND('',#3189,.T.);
#3154=EDGE_LOOP('',(#13764,#13765,#13766));
#3155=EDGE_LOOP('',(#13767,#13768,#13769,#13770,#13771,#13772,#13773));
#3156=EDGE_LOOP('',(#13774,#13775,#13776,#13777,#13778));
#3157=EDGE_LOOP('',(#13779,#13780,#13781,#13782,#13783,#13784));
#3158=EDGE_LOOP('',(#13785,#13786,#13787,#13788,#13789));
#3159=EDGE_LOOP('',(#13790,#13791,#13792,#13793,#13794,#13795));
#3160=EDGE_LOOP('',(#13796,#13797,#13798,#13799,#13800));
#3161=EDGE_LOOP('',(#13801,#13802,#13803,#13804,#13805,#13806));
#3162=EDGE_LOOP('',(#13807,#13808,#13809,#13810,#13811));
#3163=EDGE_LOOP('',(#13812,#13813,#13814,#13815,#13816,#13817));
#3164=EDGE_LOOP('',(#13818,#13819,#13820));
#3165=EDGE_LOOP('',(#13821,#13822,#13823,#13824,#13825));
#3166=EDGE_LOOP('',(#13826,#13827,#13828,#13829,#13830,#13831,#13832,#13833,
#13834,#13835,#13836,#13837,#13838,#13839,#13840,#13841,#13842,#13843,#13844,
#13845,#13846,#13847,#13848,#13849,#13850,#13851));
#3167=EDGE_LOOP('',(#13852,#13853,#13854,#13855,#13856));
#3168=EDGE_LOOP('',(#13857,#13858,#13859,#13860,#13861,#13862,#13863,#13864,
#13865,#13866,#13867,#13868,#13869,#13870,#13871,#13872,#13873,#13874,#13875,
#13876,#13877,#13878,#13879,#13880,#13881,#13882,#13883,#13884,#13885,#13886,
#13887,#13888,#13889,#13890));
#3169=EDGE_LOOP('',(#13891,#13892,#13893,#13894));
#3170=EDGE_LOOP('',(#13895,#13896,#13897,#13898,#13899,#13900,#13901,#13902,
#13903,#13904,#13905,#13906,#13907,#13908,#13909,#13910,#13911,#13912,#13913,
#13914,#13915,#13916,#13917,#13918,#13919,#13920,#13921,#13922,#13923,#13924,
#13925,#13926,#13927));
#3171=EDGE_LOOP('',(#13928,#13929,#13930,#13931,#13932,#13933));
#3172=EDGE_LOOP('',(#13934,#13935,#13936,#13937,#13938,#13939,#13940));
#3173=EDGE_LOOP('',(#13941));
#3174=EDGE_LOOP('',(#13942));
#3175=EDGE_LOOP('',(#13943,#13944));
#3176=EDGE_LOOP('',(#13945,#13946));
#3177=EDGE_LOOP('',(#13947,#13948));
#3178=EDGE_LOOP('',(#13949,#13950));
#3179=EDGE_LOOP('',(#13951,#13952));
#3180=EDGE_LOOP('',(#13953,#13954));
#3181=EDGE_LOOP('',(#13955,#13956,#13957,#13958,#13959,#13960,#13961,#13962));
#3182=EDGE_LOOP('',(#13963,#13964,#13965,#13966));
#3183=EDGE_LOOP('',(#13967,#13968,#13969,#13970));
#3184=EDGE_LOOP('',(#13971,#13972,#13973,#13974));
#3185=EDGE_LOOP('',(#13975,#13976,#13977,#13978));
#3186=EDGE_LOOP('',(#13979,#13980,#13981,#13982));
#3187=EDGE_LOOP('',(#13983,#13984,#13985,#13986));
#3188=EDGE_LOOP('',(#13987,#13988,#13989,#13990));
#3189=EDGE_LOOP('',(#13991,#13992,#13993,#13994,#13995,#13996,#13997,#13998,
#13999));
#4285=LINE('',#63348,#5397);
#4286=LINE('',#63379,#5398);
#4287=LINE('',#63754,#5399);
#4288=LINE('',#64126,#5400);
#4289=LINE('',#64510,#5401);
#4290=LINE('',#64893,#5402);
#4291=LINE('',#65270,#5403);
#4292=LINE('',#65649,#5404);
#4293=LINE('',#65877,#5405);
#4294=LINE('',#66229,#5406);
#4295=LINE('',#66611,#5407);
#4296=LINE('',#71404,#5408);
#4297=LINE('',#71408,#5409);
#4298=LINE('',#71412,#5410);
#4299=LINE('',#71416,#5411);
#4300=LINE('',#71420,#5412);
#4301=LINE('',#71423,#5413);
#4302=LINE('',#71427,#5414);
#4303=LINE('',#71432,#5415);
#4304=LINE('',#71433,#5416);
#4305=LINE('',#71437,#5417);
#4306=LINE('',#71441,#5418);
#4307=LINE('',#71445,#5419);
#4308=LINE('',#71449,#5420);
#4309=LINE('',#71455,#5421);
#5397=VECTOR('',#20179,1.99475);
#5398=VECTOR('',#20184,1.99475);
#5399=VECTOR('',#20189,1.99475);
#5400=VECTOR('',#20192,1.99475);
#5401=VECTOR('',#20195,1.99475);
#5402=VECTOR('',#20198,1.99475);
#5403=VECTOR('',#20201,1.99475);
#5404=VECTOR('',#20204,1.99475);
#5405=VECTOR('',#20207,1.99475);
#5406=VECTOR('',#20210,1.99475);
#5407=VECTOR('',#20213,2.25);
#5408=VECTOR('',#20254,10.);
#5409=VECTOR('',#20259,10.);
#5410=VECTOR('',#20264,10.);
#5411=VECTOR('',#20269,10.);
#5412=VECTOR('',#20274,10.);
#5413=VECTOR('',#20279,10.);
#5414=VECTOR('',#20284,0.866025403784438);
#5415=VECTOR('',#20289,10.);
#5416=VECTOR('',#20290,10.);
#5417=VECTOR('',#20295,10.);
#5418=VECTOR('',#20300,10.);
#5419=VECTOR('',#20305,10.);
#5420=VECTOR('',#20310,10.);
#5421=VECTOR('',#20319,4.75);
#5977=CIRCLE('',#16452,1.99475);
#5978=CIRCLE('',#16454,1.99475);
#5979=CIRCLE('',#16464,2.);
#5980=CIRCLE('',#16466,2.4505);
#5981=CIRCLE('',#16467,2.);
#5982=CIRCLE('',#16469,2.4505);
#5983=CIRCLE('',#16470,2.4505);
#5984=CIRCLE('',#16472,1.99475);
#5985=CIRCLE('',#16475,2.4505);
#5986=CIRCLE('',#16479,2.6505);
#5987=CIRCLE('',#16480,0.2);
#5988=CIRCLE('',#16482,4.75);
#5989=CIRCLE('',#16484,1.73205080756888);
#5990=CIRCLE('',#16486,1.73205080756888);
#5991=CIRCLE('',#16488,1.73205080756888);
#5992=CIRCLE('',#16490,1.73205080756888);
#5993=CIRCLE('',#16492,1.73205080756888);
#5994=CIRCLE('',#16494,1.73205080756888);
#5995=CIRCLE('',#16497,5.86614939355167);
#5996=CIRCLE('',#16499,5.86614939355167);
#5997=CIRCLE('',#16501,5.86614939355168);
#5998=CIRCLE('',#16503,5.86614939355169);
#5999=CIRCLE('',#16505,5.86614939355168);
#6000=CIRCLE('',#16507,5.86614939355169);
#6001=CIRCLE('',#16509,4.75);
#6002=CIRCLE('',#16511,6.05489130434781);
#7375=VERTEX_POINT('',#63346);
#7376=VERTEX_POINT('',#63347);
#7377=VERTEX_POINT('',#63349);
#7378=VERTEX_POINT('',#63377);
#7379=VERTEX_POINT('',#63378);
#7380=VERTEX_POINT('',#63380);
#7381=VERTEX_POINT('',#63569);
#7382=VERTEX_POINT('',#63571);
#7383=VERTEX_POINT('',#63752);
#7384=VERTEX_POINT('',#63753);
#7385=VERTEX_POINT('',#63931);
#7386=VERTEX_POINT('',#64124);
#7387=VERTEX_POINT('',#64125);
#7388=VERTEX_POINT('',#64127);
#7389=VERTEX_POINT('',#64318);
#7390=VERTEX_POINT('',#64508);
#7391=VERTEX_POINT('',#64509);
#7392=VERTEX_POINT('',#64695);
#7393=VERTEX_POINT('',#64891);
#7394=VERTEX_POINT('',#64892);
#7395=VERTEX_POINT('',#64894);
#7396=VERTEX_POINT('',#65075);
#7397=VERTEX_POINT('',#65268);
#7398=VERTEX_POINT('',#65269);
#7399=VERTEX_POINT('',#65457);
#7400=VERTEX_POINT('',#65647);
#7401=VERTEX_POINT('',#65648);
#7402=VERTEX_POINT('',#65650);
#7403=VERTEX_POINT('',#65829);
#7404=VERTEX_POINT('',#65875);
#7405=VERTEX_POINT('',#65876);
#7406=VERTEX_POINT('',#66060);
#7407=VERTEX_POINT('',#66227);
#7408=VERTEX_POINT('',#66228);
#7409=VERTEX_POINT('',#66230);
#7410=VERTEX_POINT('',#66419);
#7411=VERTEX_POINT('',#66609);
#7412=VERTEX_POINT('',#66610);
#7413=VERTEX_POINT('',#66612);
#7414=VERTEX_POINT('',#66643);
#7415=VERTEX_POINT('',#66654);
#7416=VERTEX_POINT('',#66656);
#7417=VERTEX_POINT('',#66673);
#7418=VERTEX_POINT('',#66680);
#7419=VERTEX_POINT('',#66686);
#7420=VERTEX_POINT('',#66877);
#7421=VERTEX_POINT('',#67071);
#7422=VERTEX_POINT('',#67265);
#7423=VERTEX_POINT('',#67456);
#7424=VERTEX_POINT('',#67647);
#7425=VERTEX_POINT('',#67838);
#7426=VERTEX_POINT('',#68029);
#7427=VERTEX_POINT('',#68223);
#7428=VERTEX_POINT('',#68414);
#7429=VERTEX_POINT('',#68605);
#7430=VERTEX_POINT('',#68634);
#7431=VERTEX_POINT('',#68636);
#7432=VERTEX_POINT('',#68638);
#7433=VERTEX_POINT('',#68649);
#7434=VERTEX_POINT('',#68843);
#7435=VERTEX_POINT('',#69037);
#7436=VERTEX_POINT('',#69225);
#7437=VERTEX_POINT('',#69419);
#7438=VERTEX_POINT('',#69613);
#7439=VERTEX_POINT('',#69804);
#7440=VERTEX_POINT('',#69998);
#7441=VERTEX_POINT('',#70383);
#7442=VERTEX_POINT('',#70418);
#7443=VERTEX_POINT('',#70543);
#7444=VERTEX_POINT('',#71018);
#7445=VERTEX_POINT('',#71395);
#7446=VERTEX_POINT('',#71399);
#7447=VERTEX_POINT('',#71402);
#7448=VERTEX_POINT('',#71403);
#7449=VERTEX_POINT('',#71407);
#7450=VERTEX_POINT('',#71411);
#7451=VERTEX_POINT('',#71415);
#7452=VERTEX_POINT('',#71419);
#7453=VERTEX_POINT('',#71426);
#7454=VERTEX_POINT('',#71429);
#7455=VERTEX_POINT('',#71430);
#7456=VERTEX_POINT('',#71435);
#7457=VERTEX_POINT('',#71439);
#7458=VERTEX_POINT('',#71443);
#7459=VERTEX_POINT('',#71447);
#7460=VERTEX_POINT('',#71453);
#9545=EDGE_CURVE('',#7375,#7376,#4285,.T.);
#9546=EDGE_CURVE('',#7377,#7375,#671,.T.);
#9547=EDGE_CURVE('',#7376,#7377,#5977,.T.);
#9548=EDGE_CURVE('',#7378,#7379,#4286,.T.);
#9549=EDGE_CURVE('',#7380,#7378,#672,.F.);
#9550=EDGE_CURVE('',#7375,#7380,#673,.T.);
#9551=EDGE_CURVE('',#7381,#7376,#5978,.T.);
#9552=EDGE_CURVE('',#7381,#7382,#674,.T.);
#9553=EDGE_CURVE('',#7382,#7379,#675,.T.);
#9554=EDGE_CURVE('',#7383,#7384,#4287,.T.);
#9555=EDGE_CURVE('',#7378,#7383,#676,.F.);
#9556=EDGE_CURVE('',#7379,#7385,#677,.T.);
#9557=EDGE_CURVE('',#7385,#7384,#678,.T.);
#9558=EDGE_CURVE('',#7386,#7387,#4288,.T.);
#9559=EDGE_CURVE('',#7388,#7386,#679,.F.);
#9560=EDGE_CURVE('',#7383,#7388,#680,.F.);
#9561=EDGE_CURVE('',#7384,#7389,#681,.T.);
#9562=EDGE_CURVE('',#7389,#7387,#682,.T.);
#9563=EDGE_CURVE('',#7390,#7391,#4289,.T.);
#9564=EDGE_CURVE('',#7386,#7390,#683,.F.);
#9565=EDGE_CURVE('',#7387,#7392,#684,.T.);
#9566=EDGE_CURVE('',#7392,#7391,#685,.T.);
#9567=EDGE_CURVE('',#7393,#7394,#4290,.T.);
#9568=EDGE_CURVE('',#7395,#7393,#686,.F.);
#9569=EDGE_CURVE('',#7390,#7395,#687,.F.);
#9570=EDGE_CURVE('',#7391,#7396,#688,.T.);
#9571=EDGE_CURVE('',#7396,#7394,#689,.T.);
#9572=EDGE_CURVE('',#7397,#7398,#4291,.T.);
#9573=EDGE_CURVE('',#7393,#7397,#690,.F.);
#9574=EDGE_CURVE('',#7394,#7399,#691,.T.);
#9575=EDGE_CURVE('',#7399,#7398,#692,.T.);
#9576=EDGE_CURVE('',#7400,#7401,#4292,.T.);
#9577=EDGE_CURVE('',#7402,#7400,#693,.F.);
#9578=EDGE_CURVE('',#7397,#7402,#694,.F.);
#9579=EDGE_CURVE('',#7398,#7403,#695,.T.);
#9580=EDGE_CURVE('',#7403,#7401,#696,.T.);
#9581=EDGE_CURVE('',#7404,#7405,#4293,.T.);
#9582=EDGE_CURVE('',#7400,#7404,#697,.F.);
#9583=EDGE_CURVE('',#7401,#7406,#698,.T.);
#9584=EDGE_CURVE('',#7406,#7405,#699,.T.);
#9585=EDGE_CURVE('',#7407,#7408,#4294,.T.);
#9586=EDGE_CURVE('',#7409,#7407,#700,.F.);
#9587=EDGE_CURVE('',#7404,#7409,#701,.F.);
#9588=EDGE_CURVE('',#7405,#7410,#702,.T.);
#9589=EDGE_CURVE('',#7410,#7408,#703,.T.);
#9590=EDGE_CURVE('',#7411,#7412,#4295,.T.);
#9591=EDGE_CURVE('',#7411,#7413,#5979,.T.);
#9592=EDGE_CURVE('',#7413,#7412,#704,.T.);
#9593=EDGE_CURVE('',#7412,#7414,#705,.T.);
#9594=EDGE_CURVE('',#7415,#7414,#5980,.T.);
#9595=EDGE_CURVE('',#7415,#7416,#706,.T.);
#9596=EDGE_CURVE('',#7416,#7411,#5981,.T.);
#9597=EDGE_CURVE('',#7417,#7415,#707,.T.);
#9598=EDGE_CURVE('',#7414,#7418,#708,.T.);
#9599=EDGE_CURVE('',#7418,#7419,#709,.T.);
#9600=EDGE_CURVE('',#7419,#7420,#710,.T.);
#9601=EDGE_CURVE('',#7420,#7421,#711,.T.);
#9602=EDGE_CURVE('',#7421,#7422,#712,.T.);
#9603=EDGE_CURVE('',#7422,#7423,#713,.T.);
#9604=EDGE_CURVE('',#7423,#7424,#714,.T.);
#9605=EDGE_CURVE('',#7424,#7425,#715,.T.);
#9606=EDGE_CURVE('',#7425,#7426,#716,.T.);
#9607=EDGE_CURVE('',#7426,#7427,#717,.T.);
#9608=EDGE_CURVE('',#7427,#7428,#718,.T.);
#9609=EDGE_CURVE('',#7428,#7429,#719,.T.);
#9610=EDGE_CURVE('',#7430,#7429,#5982,.T.);
#9611=EDGE_CURVE('',#7431,#7430,#5983,.T.);
#9612=EDGE_CURVE('',#7431,#7432,#720,.T.);
#9613=EDGE_CURVE('',#7432,#7433,#721,.T.);
#9614=EDGE_CURVE('',#7433,#7434,#722,.T.);
#9615=EDGE_CURVE('',#7434,#7435,#723,.T.);
#9616=EDGE_CURVE('',#7435,#7436,#724,.T.);
#9617=EDGE_CURVE('',#7436,#7437,#725,.T.);
#9618=EDGE_CURVE('',#7437,#7438,#726,.T.);
#9619=EDGE_CURVE('',#7438,#7439,#727,.T.);
#9620=EDGE_CURVE('',#7439,#7440,#728,.T.);
#9621=EDGE_CURVE('',#7440,#7417,#729,.T.);
#9622=EDGE_CURVE('',#7408,#7441,#730,.T.);
#9623=EDGE_CURVE('',#7441,#7442,#731,.T.);
#9624=EDGE_CURVE('',#7443,#7442,#5984,.T.);
#9625=EDGE_CURVE('',#7407,#7443,#732,.F.);
#9626=EDGE_CURVE('',#7442,#7431,#733,.T.);
#9627=EDGE_CURVE('',#7416,#7381,#400,.T.);
#9628=EDGE_CURVE('',#7444,#7431,#5985,.T.);
#9629=EDGE_CURVE('',#7444,#7443,#734,.T.);
#9630=EDGE_CURVE('',#7377,#7413,#401,.T.);
#9631=EDGE_CURVE('',#7429,#7444,#735,.T.);
#9632=EDGE_CURVE('',#7445,#7445,#5986,.T.);
#9633=EDGE_CURVE('',#7445,#7430,#5987,.T.);
#9634=EDGE_CURVE('',#7446,#7446,#5988,.T.);
#9635=EDGE_CURVE('',#7447,#7448,#4296,.T.);
#9636=EDGE_CURVE('',#7448,#7447,#5989,.T.);
#9637=EDGE_CURVE('',#7448,#7449,#4297,.T.);
#9638=EDGE_CURVE('',#7449,#7448,#5990,.T.);
#9639=EDGE_CURVE('',#7449,#7450,#4298,.T.);
#9640=EDGE_CURVE('',#7450,#7449,#5991,.T.);
#9641=EDGE_CURVE('',#7450,#7451,#4299,.T.);
#9642=EDGE_CURVE('',#7451,#7450,#5992,.T.);
#9643=EDGE_CURVE('',#7451,#7452,#4300,.T.);
#9644=EDGE_CURVE('',#7452,#7451,#5993,.T.);
#9645=EDGE_CURVE('',#7452,#7447,#4301,.T.);
#9646=EDGE_CURVE('',#7447,#7452,#5994,.T.);
#9647=EDGE_CURVE('',#7453,#7448,#4302,.T.);
#9648=EDGE_CURVE('',#7454,#7455,#5995,.T.);
#9649=EDGE_CURVE('',#7454,#7447,#4303,.T.);
#9650=EDGE_CURVE('',#7455,#7448,#4304,.T.);
#9651=EDGE_CURVE('',#7455,#7456,#5996,.T.);
#9652=EDGE_CURVE('',#7456,#7449,#4305,.T.);
#9653=EDGE_CURVE('',#7456,#7457,#5997,.T.);
#9654=EDGE_CURVE('',#7457,#7450,#4306,.T.);
#9655=EDGE_CURVE('',#7457,#7458,#5998,.T.);
#9656=EDGE_CURVE('',#7458,#7451,#4307,.T.);
#9657=EDGE_CURVE('',#7459,#7454,#5999,.T.);
#9658=EDGE_CURVE('',#7459,#7452,#4308,.T.);
#9659=EDGE_CURVE('',#7458,#7459,#6000,.T.);
#9660=EDGE_CURVE('',#7460,#7460,#6001,.T.);
#9661=EDGE_CURVE('',#7460,#7446,#4309,.T.);
#9662=EDGE_CURVE('',#7455,#7460,#6002,.T.);
#13764=ORIENTED_EDGE('',*,*,#9545,.F.);
#13765=ORIENTED_EDGE('',*,*,#9546,.F.);
#13766=ORIENTED_EDGE('',*,*,#9547,.F.);
#13767=ORIENTED_EDGE('',*,*,#9548,.F.);
#13768=ORIENTED_EDGE('',*,*,#9549,.F.);
#13769=ORIENTED_EDGE('',*,*,#9550,.F.);
#13770=ORIENTED_EDGE('',*,*,#9545,.T.);
#13771=ORIENTED_EDGE('',*,*,#9551,.F.);
#13772=ORIENTED_EDGE('',*,*,#9552,.T.);
#13773=ORIENTED_EDGE('',*,*,#9553,.T.);
#13774=ORIENTED_EDGE('',*,*,#9554,.F.);
#13775=ORIENTED_EDGE('',*,*,#9555,.F.);
#13776=ORIENTED_EDGE('',*,*,#9548,.T.);
#13777=ORIENTED_EDGE('',*,*,#9556,.T.);
#13778=ORIENTED_EDGE('',*,*,#9557,.T.);
#13779=ORIENTED_EDGE('',*,*,#9558,.F.);
#13780=ORIENTED_EDGE('',*,*,#9559,.F.);
#13781=ORIENTED_EDGE('',*,*,#9560,.F.);
#13782=ORIENTED_EDGE('',*,*,#9554,.T.);
#13783=ORIENTED_EDGE('',*,*,#9561,.T.);
#13784=ORIENTED_EDGE('',*,*,#9562,.T.);
#13785=ORIENTED_EDGE('',*,*,#9563,.F.);
#13786=ORIENTED_EDGE('',*,*,#9564,.F.);
#13787=ORIENTED_EDGE('',*,*,#9558,.T.);
#13788=ORIENTED_EDGE('',*,*,#9565,.T.);
#13789=ORIENTED_EDGE('',*,*,#9566,.T.);
#13790=ORIENTED_EDGE('',*,*,#9567,.F.);
#13791=ORIENTED_EDGE('',*,*,#9568,.F.);
#13792=ORIENTED_EDGE('',*,*,#9569,.F.);
#13793=ORIENTED_EDGE('',*,*,#9563,.T.);
#13794=ORIENTED_EDGE('',*,*,#9570,.T.);
#13795=ORIENTED_EDGE('',*,*,#9571,.T.);
#13796=ORIENTED_EDGE('',*,*,#9572,.F.);
#13797=ORIENTED_EDGE('',*,*,#9573,.F.);
#13798=ORIENTED_EDGE('',*,*,#9567,.T.);
#13799=ORIENTED_EDGE('',*,*,#9574,.T.);
#13800=ORIENTED_EDGE('',*,*,#9575,.T.);
#13801=ORIENTED_EDGE('',*,*,#9576,.F.);
#13802=ORIENTED_EDGE('',*,*,#9577,.F.);
#13803=ORIENTED_EDGE('',*,*,#9578,.F.);
#13804=ORIENTED_EDGE('',*,*,#9572,.T.);
#13805=ORIENTED_EDGE('',*,*,#9579,.T.);
#13806=ORIENTED_EDGE('',*,*,#9580,.T.);
#13807=ORIENTED_EDGE('',*,*,#9581,.F.);
#13808=ORIENTED_EDGE('',*,*,#9582,.F.);
#13809=ORIENTED_EDGE('',*,*,#9576,.T.);
#13810=ORIENTED_EDGE('',*,*,#9583,.T.);
#13811=ORIENTED_EDGE('',*,*,#9584,.T.);
#13812=ORIENTED_EDGE('',*,*,#9585,.F.);
#13813=ORIENTED_EDGE('',*,*,#9586,.F.);
#13814=ORIENTED_EDGE('',*,*,#9587,.F.);
#13815=ORIENTED_EDGE('',*,*,#9581,.T.);
#13816=ORIENTED_EDGE('',*,*,#9588,.T.);
#13817=ORIENTED_EDGE('',*,*,#9589,.T.);
#13818=ORIENTED_EDGE('',*,*,#9590,.F.);
#13819=ORIENTED_EDGE('',*,*,#9591,.T.);
#13820=ORIENTED_EDGE('',*,*,#9592,.T.);
#13821=ORIENTED_EDGE('',*,*,#9590,.T.);
#13822=ORIENTED_EDGE('',*,*,#9593,.T.);
#13823=ORIENTED_EDGE('',*,*,#9594,.F.);
#13824=ORIENTED_EDGE('',*,*,#9595,.T.);
#13825=ORIENTED_EDGE('',*,*,#9596,.T.);
#13826=ORIENTED_EDGE('',*,*,#9597,.T.);
#13827=ORIENTED_EDGE('',*,*,#9594,.T.);
#13828=ORIENTED_EDGE('',*,*,#9598,.T.);
#13829=ORIENTED_EDGE('',*,*,#9599,.T.);
#13830=ORIENTED_EDGE('',*,*,#9600,.T.);
#13831=ORIENTED_EDGE('',*,*,#9601,.T.);
#13832=ORIENTED_EDGE('',*,*,#9602,.T.);
#13833=ORIENTED_EDGE('',*,*,#9603,.T.);
#13834=ORIENTED_EDGE('',*,*,#9604,.T.);
#13835=ORIENTED_EDGE('',*,*,#9605,.T.);
#13836=ORIENTED_EDGE('',*,*,#9606,.T.);
#13837=ORIENTED_EDGE('',*,*,#9607,.T.);
#13838=ORIENTED_EDGE('',*,*,#9608,.T.);
#13839=ORIENTED_EDGE('',*,*,#9609,.T.);
#13840=ORIENTED_EDGE('',*,*,#9610,.F.);
#13841=ORIENTED_EDGE('',*,*,#9611,.F.);
#13842=ORIENTED_EDGE('',*,*,#9612,.T.);
#13843=ORIENTED_EDGE('',*,*,#9613,.T.);
#13844=ORIENTED_EDGE('',*,*,#9614,.T.);
#13845=ORIENTED_EDGE('',*,*,#9615,.T.);
#13846=ORIENTED_EDGE('',*,*,#9616,.T.);
#13847=ORIENTED_EDGE('',*,*,#9617,.T.);
#13848=ORIENTED_EDGE('',*,*,#9618,.T.);
#13849=ORIENTED_EDGE('',*,*,#9619,.T.);
#13850=ORIENTED_EDGE('',*,*,#9620,.T.);
#13851=ORIENTED_EDGE('',*,*,#9621,.T.);
#13852=ORIENTED_EDGE('',*,*,#9585,.T.);
#13853=ORIENTED_EDGE('',*,*,#9622,.T.);
#13854=ORIENTED_EDGE('',*,*,#9623,.T.);
#13855=ORIENTED_EDGE('',*,*,#9624,.F.);
#13856=ORIENTED_EDGE('',*,*,#9625,.F.);
#13857=ORIENTED_EDGE('',*,*,#9595,.F.);
#13858=ORIENTED_EDGE('',*,*,#9597,.F.);
#13859=ORIENTED_EDGE('',*,*,#9621,.F.);
#13860=ORIENTED_EDGE('',*,*,#9620,.F.);
#13861=ORIENTED_EDGE('',*,*,#9619,.F.);
#13862=ORIENTED_EDGE('',*,*,#9618,.F.);
#13863=ORIENTED_EDGE('',*,*,#9617,.F.);
#13864=ORIENTED_EDGE('',*,*,#9616,.F.);
#13865=ORIENTED_EDGE('',*,*,#9615,.F.);
#13866=ORIENTED_EDGE('',*,*,#9614,.F.);
#13867=ORIENTED_EDGE('',*,*,#9613,.F.);
#13868=ORIENTED_EDGE('',*,*,#9612,.F.);
#13869=ORIENTED_EDGE('',*,*,#9626,.F.);
#13870=ORIENTED_EDGE('',*,*,#9623,.F.);
#13871=ORIENTED_EDGE('',*,*,#9622,.F.);
#13872=ORIENTED_EDGE('',*,*,#9589,.F.);
#13873=ORIENTED_EDGE('',*,*,#9588,.F.);
#13874=ORIENTED_EDGE('',*,*,#9584,.F.);
#13875=ORIENTED_EDGE('',*,*,#9583,.F.);
#13876=ORIENTED_EDGE('',*,*,#9580,.F.);
#13877=ORIENTED_EDGE('',*,*,#9579,.F.);
#13878=ORIENTED_EDGE('',*,*,#9575,.F.);
#13879=ORIENTED_EDGE('',*,*,#9574,.F.);
#13880=ORIENTED_EDGE('',*,*,#9571,.F.);
#13881=ORIENTED_EDGE('',*,*,#9570,.F.);
#13882=ORIENTED_EDGE('',*,*,#9566,.F.);
#13883=ORIENTED_EDGE('',*,*,#9565,.F.);
#13884=ORIENTED_EDGE('',*,*,#9562,.F.);
#13885=ORIENTED_EDGE('',*,*,#9561,.F.);
#13886=ORIENTED_EDGE('',*,*,#9557,.F.);
#13887=ORIENTED_EDGE('',*,*,#9556,.F.);
#13888=ORIENTED_EDGE('',*,*,#9553,.F.);
#13889=ORIENTED_EDGE('',*,*,#9552,.F.);
#13890=ORIENTED_EDGE('',*,*,#9627,.F.);
#13891=ORIENTED_EDGE('',*,*,#9628,.F.);
#13892=ORIENTED_EDGE('',*,*,#9629,.T.);
#13893=ORIENTED_EDGE('',*,*,#9624,.T.);
#13894=ORIENTED_EDGE('',*,*,#9626,.T.);
#13895=ORIENTED_EDGE('',*,*,#9592,.F.);
#13896=ORIENTED_EDGE('',*,*,#9630,.F.);
#13897=ORIENTED_EDGE('',*,*,#9546,.T.);
#13898=ORIENTED_EDGE('',*,*,#9550,.T.);
#13899=ORIENTED_EDGE('',*,*,#9549,.T.);
#13900=ORIENTED_EDGE('',*,*,#9555,.T.);
#13901=ORIENTED_EDGE('',*,*,#9560,.T.);
#13902=ORIENTED_EDGE('',*,*,#9559,.T.);
#13903=ORIENTED_EDGE('',*,*,#9564,.T.);
#13904=ORIENTED_EDGE('',*,*,#9569,.T.);
#13905=ORIENTED_EDGE('',*,*,#9568,.T.);
#13906=ORIENTED_EDGE('',*,*,#9573,.T.);
#13907=ORIENTED_EDGE('',*,*,#9578,.T.);
#13908=ORIENTED_EDGE('',*,*,#9577,.T.);
#13909=ORIENTED_EDGE('',*,*,#9582,.T.);
#13910=ORIENTED_EDGE('',*,*,#9587,.T.);
#13911=ORIENTED_EDGE('',*,*,#9586,.T.);
#13912=ORIENTED_EDGE('',*,*,#9625,.T.);
#13913=ORIENTED_EDGE('',*,*,#9629,.F.);
#13914=ORIENTED_EDGE('',*,*,#9631,.F.);
#13915=ORIENTED_EDGE('',*,*,#9609,.F.);
#13916=ORIENTED_EDGE('',*,*,#9608,.F.);
#13917=ORIENTED_EDGE('',*,*,#9607,.F.);
#13918=ORIENTED_EDGE('',*,*,#9606,.F.);
#13919=ORIENTED_EDGE('',*,*,#9605,.F.);
#13920=ORIENTED_EDGE('',*,*,#9604,.F.);
#13921=ORIENTED_EDGE('',*,*,#9603,.F.);
#13922=ORIENTED_EDGE('',*,*,#9602,.F.);
#13923=ORIENTED_EDGE('',*,*,#9601,.F.);
#13924=ORIENTED_EDGE('',*,*,#9600,.F.);
#13925=ORIENTED_EDGE('',*,*,#9599,.F.);
#13926=ORIENTED_EDGE('',*,*,#9598,.F.);
#13927=ORIENTED_EDGE('',*,*,#9593,.F.);
#13928=ORIENTED_EDGE('',*,*,#9627,.T.);
#13929=ORIENTED_EDGE('',*,*,#9551,.T.);
#13930=ORIENTED_EDGE('',*,*,#9547,.T.);
#13931=ORIENTED_EDGE('',*,*,#9630,.T.);
#13932=ORIENTED_EDGE('',*,*,#9591,.F.);
#13933=ORIENTED_EDGE('',*,*,#9596,.F.);
#13934=ORIENTED_EDGE('',*,*,#9632,.T.);
#13935=ORIENTED_EDGE('',*,*,#9633,.T.);
#13936=ORIENTED_EDGE('',*,*,#9610,.T.);
#13937=ORIENTED_EDGE('',*,*,#9631,.T.);
#13938=ORIENTED_EDGE('',*,*,#9628,.T.);
#13939=ORIENTED_EDGE('',*,*,#9611,.T.);
#13940=ORIENTED_EDGE('',*,*,#9633,.F.);
#13941=ORIENTED_EDGE('',*,*,#9634,.F.);
#13942=ORIENTED_EDGE('',*,*,#9632,.F.);
#13943=ORIENTED_EDGE('',*,*,#9635,.F.);
#13944=ORIENTED_EDGE('',*,*,#9636,.F.);
#13945=ORIENTED_EDGE('',*,*,#9637,.F.);
#13946=ORIENTED_EDGE('',*,*,#9638,.F.);
#13947=ORIENTED_EDGE('',*,*,#9639,.F.);
#13948=ORIENTED_EDGE('',*,*,#9640,.F.);
#13949=ORIENTED_EDGE('',*,*,#9641,.F.);
#13950=ORIENTED_EDGE('',*,*,#9642,.F.);
#13951=ORIENTED_EDGE('',*,*,#9643,.F.);
#13952=ORIENTED_EDGE('',*,*,#9644,.F.);
#13953=ORIENTED_EDGE('',*,*,#9645,.F.);
#13954=ORIENTED_EDGE('',*,*,#9646,.F.);
#13955=ORIENTED_EDGE('',*,*,#9647,.T.);
#13956=ORIENTED_EDGE('',*,*,#9636,.T.);
#13957=ORIENTED_EDGE('',*,*,#9646,.T.);
#13958=ORIENTED_EDGE('',*,*,#9644,.T.);
#13959=ORIENTED_EDGE('',*,*,#9642,.T.);
#13960=ORIENTED_EDGE('',*,*,#9640,.T.);
#13961=ORIENTED_EDGE('',*,*,#9638,.T.);
#13962=ORIENTED_EDGE('',*,*,#9647,.F.);
#13963=ORIENTED_EDGE('',*,*,#9648,.F.);
#13964=ORIENTED_EDGE('',*,*,#9649,.T.);
#13965=ORIENTED_EDGE('',*,*,#9635,.T.);
#13966=ORIENTED_EDGE('',*,*,#9650,.F.);
#13967=ORIENTED_EDGE('',*,*,#9651,.F.);
#13968=ORIENTED_EDGE('',*,*,#9650,.T.);
#13969=ORIENTED_EDGE('',*,*,#9637,.T.);
#13970=ORIENTED_EDGE('',*,*,#9652,.F.);
#13971=ORIENTED_EDGE('',*,*,#9653,.F.);
#13972=ORIENTED_EDGE('',*,*,#9652,.T.);
#13973=ORIENTED_EDGE('',*,*,#9639,.T.);
#13974=ORIENTED_EDGE('',*,*,#9654,.F.);
#13975=ORIENTED_EDGE('',*,*,#9655,.F.);
#13976=ORIENTED_EDGE('',*,*,#9654,.T.);
#13977=ORIENTED_EDGE('',*,*,#9641,.T.);
#13978=ORIENTED_EDGE('',*,*,#9656,.F.);
#13979=ORIENTED_EDGE('',*,*,#9657,.F.);
#13980=ORIENTED_EDGE('',*,*,#9658,.T.);
#13981=ORIENTED_EDGE('',*,*,#9645,.T.);
#13982=ORIENTED_EDGE('',*,*,#9649,.F.);
#13983=ORIENTED_EDGE('',*,*,#9659,.F.);
#13984=ORIENTED_EDGE('',*,*,#9656,.T.);
#13985=ORIENTED_EDGE('',*,*,#9643,.T.);
#13986=ORIENTED_EDGE('',*,*,#9658,.F.);
#13987=ORIENTED_EDGE('',*,*,#9660,.F.);
#13988=ORIENTED_EDGE('',*,*,#9661,.T.);
#13989=ORIENTED_EDGE('',*,*,#9634,.T.);
#13990=ORIENTED_EDGE('',*,*,#9661,.F.);
#13991=ORIENTED_EDGE('',*,*,#9651,.T.);
#13992=ORIENTED_EDGE('',*,*,#9653,.T.);
#13993=ORIENTED_EDGE('',*,*,#9655,.T.);
#13994=ORIENTED_EDGE('',*,*,#9659,.T.);
#13995=ORIENTED_EDGE('',*,*,#9657,.T.);
#13996=ORIENTED_EDGE('',*,*,#9648,.T.);
#13997=ORIENTED_EDGE('',*,*,#9662,.T.);
#13998=ORIENTED_EDGE('',*,*,#9660,.T.);
#13999=ORIENTED_EDGE('',*,*,#9662,.F.);
#14335=CONICAL_SURFACE('',#16463,2.25,0.785398163397448);
#14336=CONICAL_SURFACE('',#16465,2.25,0.785398163397448);
#14337=CONICAL_SURFACE('',#16495,0.866025403784438,1.02974425867665);
#15020=ADVANCED_FACE('',(#2285),#1055,.T.);
#15021=ADVANCED_FACE('',(#2286),#1056,.T.);
#15022=ADVANCED_FACE('',(#2287),#1057,.T.);
#15023=ADVANCED_FACE('',(#2288),#1058,.T.);
#15024=ADVANCED_FACE('',(#2289),#1059,.T.);
#15025=ADVANCED_FACE('',(#2290),#1060,.T.);
#15026=ADVANCED_FACE('',(#2291),#1061,.T.);
#15027=ADVANCED_FACE('',(#2292),#1062,.T.);
#15028=ADVANCED_FACE('',(#2293),#1063,.T.);
#15029=ADVANCED_FACE('',(#2294),#1064,.T.);
#15030=ADVANCED_FACE('',(#2295),#14335,.F.);
#15031=ADVANCED_FACE('',(#2296),#14336,.F.);
#15032=ADVANCED_FACE('',(#2297),#1065,.T.);
#15033=ADVANCED_FACE('',(#2298),#1066,.T.);
#15034=ADVANCED_FACE('',(#2299),#368,.F.);
#15035=ADVANCED_FACE('',(#2300),#1583,.F.);
#15036=ADVANCED_FACE('',(#2301),#369,.F.);
#15037=ADVANCED_FACE('',(#2302),#1584,.T.);
#15038=ADVANCED_FACE('',(#2303),#362,.F.);
#15039=ADVANCED_FACE('',(#2304,#1209),#1585,.T.);
#15040=ADVANCED_FACE('',(#2305),#1586,.F.);
#15041=ADVANCED_FACE('',(#2306),#1587,.F.);
#15042=ADVANCED_FACE('',(#2307),#1588,.F.);
#15043=ADVANCED_FACE('',(#2308),#1589,.F.);
#15044=ADVANCED_FACE('',(#2309),#1590,.F.);
#15045=ADVANCED_FACE('',(#2310),#1591,.F.);
#15046=ADVANCED_FACE('',(#2311),#14337,.F.);
#15047=ADVANCED_FACE('',(#2312),#1592,.F.);
#15048=ADVANCED_FACE('',(#2313),#1593,.F.);
#15049=ADVANCED_FACE('',(#2314),#1594,.F.);
#15050=ADVANCED_FACE('',(#2315),#1595,.F.);
#15051=ADVANCED_FACE('',(#2316),#1596,.F.);
#15052=ADVANCED_FACE('',(#2317),#1597,.F.);
#15053=ADVANCED_FACE('',(#2318),#1067,.T.);
#15054=ADVANCED_FACE('',(#2319),#259,.T.);
#15092=CLOSED_SHELL('',(#15020,#15021,#15022,#15023,#15024,#15025,#15026,
#15027,#15028,#15029,#15030,#15031,#15032,#15033,#15034,#15035,#15036,#15037,
#15038,#15039,#15040,#15041,#15042,#15043,#15044,#15045,#15046,#15047,#15048,
#15049,#15050,#15051,#15052,#15053,#15054));
#16450=AXIS2_PLACEMENT_3D('',#63344,#20175,#20176);
#16451=AXIS2_PLACEMENT_3D('',#63345,#20177,#20178);
#16452=AXIS2_PLACEMENT_3D('',#63375,#20180,#20181);
#16453=AXIS2_PLACEMENT_3D('',#63376,#20182,#20183);
#16454=AXIS2_PLACEMENT_3D('',#63570,#20185,#20186);
#16455=AXIS2_PLACEMENT_3D('',#63751,#20187,#20188);
#16456=AXIS2_PLACEMENT_3D('',#64123,#20190,#20191);
#16457=AXIS2_PLACEMENT_3D('',#64507,#20193,#20194);
#16458=AXIS2_PLACEMENT_3D('',#64890,#20196,#20197);
#16459=AXIS2_PLACEMENT_3D('',#65267,#20199,#20200);
#16460=AXIS2_PLACEMENT_3D('',#65646,#20202,#20203);
#16461=AXIS2_PLACEMENT_3D('',#65874,#20205,#20206);
#16462=AXIS2_PLACEMENT_3D('',#66226,#20208,#20209);
#16463=AXIS2_PLACEMENT_3D('',#66608,#20211,#20212);
#16464=AXIS2_PLACEMENT_3D('',#66613,#20214,#20215);
#16465=AXIS2_PLACEMENT_3D('',#66642,#20216,#20217);
#16466=AXIS2_PLACEMENT_3D('',#66655,#20218,#20219);
#16467=AXIS2_PLACEMENT_3D('',#66671,#20220,#20221);
#16468=AXIS2_PLACEMENT_3D('',#66672,#20222,#20223);
#16469=AXIS2_PLACEMENT_3D('',#68635,#20224,#20225);
#16470=AXIS2_PLACEMENT_3D('',#68637,#20226,#20227);
#16471=AXIS2_PLACEMENT_3D('',#70382,#20228,#20229);
#16472=AXIS2_PLACEMENT_3D('',#70544,#20230,#20231);
#16473=AXIS2_PLACEMENT_3D('',#71016,#20232,#20233);
#16474=AXIS2_PLACEMENT_3D('',#71017,#20234,#20235);
#16475=AXIS2_PLACEMENT_3D('',#71019,#20236,#20237);
#16476=AXIS2_PLACEMENT_3D('',#71388,#20238,#20239);
#16477=AXIS2_PLACEMENT_3D('',#71393,#20240,#20241);
#16478=AXIS2_PLACEMENT_3D('',#71394,#20242,#20243);
#16479=AXIS2_PLACEMENT_3D('',#71396,#20244,#20245);
#16480=AXIS2_PLACEMENT_3D('',#71397,#20246,#20247);
#16481=AXIS2_PLACEMENT_3D('',#71398,#20248,#20249);
#16482=AXIS2_PLACEMENT_3D('',#71400,#20250,#20251);
#16483=AXIS2_PLACEMENT_3D('',#71401,#20252,#20253);
#16484=AXIS2_PLACEMENT_3D('',#71405,#20255,#20256);
#16485=AXIS2_PLACEMENT_3D('',#71406,#20257,#20258);
#16486=AXIS2_PLACEMENT_3D('',#71409,#20260,#20261);
#16487=AXIS2_PLACEMENT_3D('',#71410,#20262,#20263);
#16488=AXIS2_PLACEMENT_3D('',#71413,#20265,#20266);
#16489=AXIS2_PLACEMENT_3D('',#71414,#20267,#20268);
#16490=AXIS2_PLACEMENT_3D('',#71417,#20270,#20271);
#16491=AXIS2_PLACEMENT_3D('',#71418,#20272,#20273);
#16492=AXIS2_PLACEMENT_3D('',#71421,#20275,#20276);
#16493=AXIS2_PLACEMENT_3D('',#71422,#20277,#20278);
#16494=AXIS2_PLACEMENT_3D('',#71424,#20280,#20281);
#16495=AXIS2_PLACEMENT_3D('',#71425,#20282,#20283);
#16496=AXIS2_PLACEMENT_3D('',#71428,#20285,#20286);
#16497=AXIS2_PLACEMENT_3D('',#71431,#20287,#20288);
#16498=AXIS2_PLACEMENT_3D('',#71434,#20291,#20292);
#16499=AXIS2_PLACEMENT_3D('',#71436,#20293,#20294);
#16500=AXIS2_PLACEMENT_3D('',#71438,#20296,#20297);
#16501=AXIS2_PLACEMENT_3D('',#71440,#20298,#20299);
#16502=AXIS2_PLACEMENT_3D('',#71442,#20301,#20302);
#16503=AXIS2_PLACEMENT_3D('',#71444,#20303,#20304);
#16504=AXIS2_PLACEMENT_3D('',#71446,#20306,#20307);
#16505=AXIS2_PLACEMENT_3D('',#71448,#20308,#20309);
#16506=AXIS2_PLACEMENT_3D('',#71450,#20311,#20312);
#16507=AXIS2_PLACEMENT_3D('',#71451,#20313,#20314);
#16508=AXIS2_PLACEMENT_3D('',#71452,#20315,#20316);
#16509=AXIS2_PLACEMENT_3D('',#71454,#20317,#20318);
#16510=AXIS2_PLACEMENT_3D('',#71456,#20320,#20321);
#16511=AXIS2_PLACEMENT_3D('',#71457,#20322,#20323);
#20175=DIRECTION('axis',(0.,0.,1.));
#20176=DIRECTION('refdir',(1.,0.,0.));
#20177=DIRECTION('center_axis',(0.,0.,1.));
#20178=DIRECTION('ref_axis',(0.487024915847047,-0.873388076025873,0.));
#20179=DIRECTION('',(0.,0.,-1.));
#20180=DIRECTION('center_axis',(0.,0.,-1.));
#20181=DIRECTION('ref_axis',(1.,6.23361216984672E-14,0.));
#20182=DIRECTION('center_axis',(0.,0.,1.));
#20183=DIRECTION('ref_axis',(0.487024915847047,-0.873388076025873,0.));
#20184=DIRECTION('',(0.,0.,-1.));
#20185=DIRECTION('center_axis',(0.,0.,-1.));
#20186=DIRECTION('ref_axis',(1.,6.23361216984672E-14,0.));
#20187=DIRECTION('center_axis',(0.,0.,1.));
#20188=DIRECTION('ref_axis',(0.487024915847047,-0.873388076025873,0.));
#20189=DIRECTION('',(0.,0.,-1.));
#20190=DIRECTION('center_axis',(0.,0.,1.));
#20191=DIRECTION('ref_axis',(0.487024915847047,-0.873388076025873,0.));
#20192=DIRECTION('',(0.,0.,-1.));
#20193=DIRECTION('center_axis',(0.,0.,1.));
#20194=DIRECTION('ref_axis',(0.487024915847047,-0.873388076025873,0.));
#20195=DIRECTION('',(0.,0.,-1.));
#20196=DIRECTION('center_axis',(0.,0.,1.));
#20197=DIRECTION('ref_axis',(0.487024915847047,-0.873388076025873,0.));
#20198=DIRECTION('',(0.,0.,-1.));
#20199=DIRECTION('center_axis',(0.,0.,1.));
#20200=DIRECTION('ref_axis',(0.487024915847047,-0.873388076025873,0.));
#20201=DIRECTION('',(0.,0.,-1.));
#20202=DIRECTION('center_axis',(0.,0.,1.));
#20203=DIRECTION('ref_axis',(0.487024915847047,-0.873388076025873,0.));
#20204=DIRECTION('',(0.,0.,-1.));
#20205=DIRECTION('center_axis',(0.,0.,1.));
#20206=DIRECTION('ref_axis',(0.487024915847047,-0.873388076025873,0.));
#20207=DIRECTION('',(0.,0.,-1.));
#20208=DIRECTION('center_axis',(0.,0.,1.));
#20209=DIRECTION('ref_axis',(0.487024915847047,-0.873388076025873,0.));
#20210=DIRECTION('',(0.,0.,-1.));
#20211=DIRECTION('center_axis',(0.,0.,-1.));
#20212=DIRECTION('ref_axis',(1.,0.,0.));
#20213=DIRECTION('',(-0.707106781186547,8.65956056235493E-17,-0.707106781186548));
#20214=DIRECTION('center_axis',(0.,0.,1.));
#20215=DIRECTION('ref_axis',(1.,0.,0.));
#20216=DIRECTION('center_axis',(0.,0.,-1.));
#20217=DIRECTION('ref_axis',(1.,0.,0.));
#20218=DIRECTION('center_axis',(0.,0.,1.));
#20219=DIRECTION('ref_axis',(1.,0.,0.));
#20220=DIRECTION('center_axis',(0.,0.,1.));
#20221=DIRECTION('ref_axis',(1.,0.,0.));
#20222=DIRECTION('center_axis',(0.,0.,1.));
#20223=DIRECTION('ref_axis',(1.,0.,0.));
#20224=DIRECTION('center_axis',(0.,0.,1.));
#20225=DIRECTION('ref_axis',(1.,0.,0.));
#20226=DIRECTION('center_axis',(0.,0.,1.));
#20227=DIRECTION('ref_axis',(1.,0.,0.));
#20228=DIRECTION('center_axis',(0.,0.,1.));
#20229=DIRECTION('ref_axis',(0.487024915847047,-0.873388076025873,0.));
#20230=DIRECTION('center_axis',(0.,0.,1.));
#20231=DIRECTION('ref_axis',(1.,6.23361216984672E-14,0.));
#20232=DIRECTION('center_axis',(-4.0203604687501E-11,3.07178135510889E-11,
-1.));
#20233=DIRECTION('ref_axis',(0.523940213008024,0.85175504295138,5.09976739692055E-12));
#20234=DIRECTION('center_axis',(0.,0.,1.));
#20235=DIRECTION('ref_axis',(1.,0.,0.));
#20236=DIRECTION('center_axis',(0.,0.,1.));
#20237=DIRECTION('ref_axis',(1.,0.,0.));
#20238=DIRECTION('center_axis',(6.22475379338965E-12,5.06217749195052E-11,
-1.));
#20239=DIRECTION('ref_axis',(0.946205103506986,-0.323567461431668,-1.04896653964898E-11));
#20240=DIRECTION('center_axis',(0.,0.,-1.));
#20241=DIRECTION('ref_axis',(-1.,0.,0.));
#20242=DIRECTION('center_axis',(0.,0.,1.));
#20243=DIRECTION('ref_axis',(1.,0.,0.));
#20244=DIRECTION('center_axis',(0.,0.,-1.));
#20245=DIRECTION('ref_axis',(1.,0.,0.));
#20246=DIRECTION('center_axis',(0.,1.,0.));
#20247=DIRECTION('ref_axis',(-1.,0.,0.));
#20248=DIRECTION('center_axis',(0.,0.,-1.));
#20249=DIRECTION('ref_axis',(-1.,0.,0.));
#20250=DIRECTION('center_axis',(0.,0.,1.));
#20251=DIRECTION('ref_axis',(1.,0.,0.));
#20252=DIRECTION('center_axis',(0.,0.,1.));
#20253=DIRECTION('ref_axis',(1.,0.,0.));
#20254=DIRECTION('',(-0.499999999999998,0.86602540378444,0.));
#20255=DIRECTION('center_axis',(0.,0.,1.));
#20256=DIRECTION('ref_axis',(1.,0.,0.));
#20257=DIRECTION('center_axis',(0.,0.,1.));
#20258=DIRECTION('ref_axis',(1.,0.,0.));
#20259=DIRECTION('',(0.5,0.866025403784439,0.));
#20260=DIRECTION('center_axis',(0.,0.,1.));
#20261=DIRECTION('ref_axis',(1.,0.,0.));
#20262=DIRECTION('center_axis',(0.,0.,1.));
#20263=DIRECTION('ref_axis',(1.,0.,0.));
#20264=DIRECTION('',(1.,0.,0.));
#20265=DIRECTION('center_axis',(0.,0.,1.));
#20266=DIRECTION('ref_axis',(1.,0.,0.));
#20267=DIRECTION('center_axis',(0.,0.,1.));
#20268=DIRECTION('ref_axis',(1.,0.,0.));
#20269=DIRECTION('',(0.5,-0.866025403784439,0.));
#20270=DIRECTION('center_axis',(0.,0.,1.));
#20271=DIRECTION('ref_axis',(1.,0.,0.));
#20272=DIRECTION('center_axis',(0.,0.,1.));
#20273=DIRECTION('ref_axis',(1.,0.,0.));
#20274=DIRECTION('',(-0.499999999999999,-0.866025403784439,0.));
#20275=DIRECTION('center_axis',(0.,0.,1.));
#20276=DIRECTION('ref_axis',(1.,0.,0.));
#20277=DIRECTION('center_axis',(0.,0.,1.));
#20278=DIRECTION('ref_axis',(1.,0.,0.));
#20279=DIRECTION('',(-1.,0.,0.));
#20280=DIRECTION('center_axis',(0.,0.,1.));
#20281=DIRECTION('ref_axis',(1.,0.,0.));
#20282=DIRECTION('center_axis',(0.,0.,1.));
#20283=DIRECTION('ref_axis',(1.,0.,0.));
#20284=DIRECTION('',(-0.85716730070211,-1.04972719113862E-16,0.515038074910058));
#20285=DIRECTION('center_axis',(-0.86602540378444,-0.499999999999998,0.));
#20286=DIRECTION('ref_axis',(-0.499999999999998,0.86602540378444,0.));
#20287=DIRECTION('center_axis',(-0.86602540378444,-0.499999999999998,0.));
#20288=DIRECTION('ref_axis',(0.,0.,-1.));
#20289=DIRECTION('',(0.,0.,-1.));
#20290=DIRECTION('',(0.,0.,-1.));
#20291=DIRECTION('center_axis',(-0.866025403784439,0.5,0.));
#20292=DIRECTION('ref_axis',(0.5,0.866025403784439,0.));
#20293=DIRECTION('center_axis',(-0.866025403784439,0.5,0.));
#20294=DIRECTION('ref_axis',(0.,0.,-1.));
#20295=DIRECTION('',(0.,0.,-1.));
#20296=DIRECTION('center_axis',(0.,1.,0.));
#20297=DIRECTION('ref_axis',(1.,0.,0.));
#20298=DIRECTION('center_axis',(0.,1.,0.));
#20299=DIRECTION('ref_axis',(0.,0.,-1.));
#20300=DIRECTION('',(0.,0.,-1.));
#20301=DIRECTION('center_axis',(0.866025403784439,0.5,0.));
#20302=DIRECTION('ref_axis',(0.5,-0.866025403784439,0.));
#20303=DIRECTION('center_axis',(0.866025403784439,0.5,0.));
#20304=DIRECTION('ref_axis',(0.,0.,-1.));
#20305=DIRECTION('',(0.,0.,-1.));
#20306=DIRECTION('center_axis',(0.,-1.,0.));
#20307=DIRECTION('ref_axis',(-1.,0.,0.));
#20308=DIRECTION('center_axis',(0.,-1.,0.));
#20309=DIRECTION('ref_axis',(0.,0.,1.));
#20310=DIRECTION('',(0.,0.,-1.));
#20311=DIRECTION('center_axis',(0.866025403784439,-0.5,0.));
#20312=DIRECTION('ref_axis',(-0.5,-0.866025403784439,0.));
#20313=DIRECTION('center_axis',(0.866025403784439,-0.5,0.));
#20314=DIRECTION('ref_axis',(0.,0.,1.));
#20315=DIRECTION('center_axis',(0.,0.,1.));
#20316=DIRECTION('ref_axis',(1.,0.,0.));
#20317=DIRECTION('center_axis',(0.,0.,1.));
#20318=DIRECTION('ref_axis',(1.,0.,0.));
#20319=DIRECTION('',(0.,0.,-1.));
#20320=DIRECTION('center_axis',(0.,0.,1.));
#20321=DIRECTION('ref_axis',(1.,0.,0.));
#20322=DIRECTION('center_axis',(0.,-1.,0.));
#20323=DIRECTION('ref_axis',(-1.,0.,0.));
#63344=CARTESIAN_POINT('',(0.,0.,0.));
#63345=CARTESIAN_POINT('Origin',(30.,21.,34.5704548813952));
#63346=CARTESIAN_POINT('',(29.0285070491141,22.7421908646526,36.5933647280801));
#63347=CARTESIAN_POINT('',(29.0285070491141,22.7421908646526,36.5));
#63348=CARTESIAN_POINT('',(29.0285070491141,22.7421908646526,34.5704548813952));
#63349=CARTESIAN_POINT('',(30.4423314238756,22.9450888087571,36.5));
#63350=CARTESIAN_POINT('Ctrl Pts',(30.4423314238756,22.9450888087571,36.5));
#63351=CARTESIAN_POINT('Ctrl Pts',(30.3662355841702,22.9623937158526,36.5049600370302));
#63352=CARTESIAN_POINT('Ctrl Pts',(30.2892837013555,22.975192508028,36.5099200740605));
#63353=CARTESIAN_POINT('Ctrl Pts',(30.2119875644214,22.9834537642785,36.5148801110907));
#63354=CARTESIAN_POINT('Ctrl Pts',(30.1343618519812,22.9917502448989,36.5198612967421));
#63355=CARTESIAN_POINT('Ctrl Pts',(30.0563892228182,22.9954704906302,36.5248424823934));
#63356=CARTESIAN_POINT('Ctrl Pts',(29.9785820065602,22.9946350122408,36.5298236680448));
#63357=CARTESIAN_POINT('Ctrl Pts',(29.9003694249949,22.9937951811196,36.5348308050147));
#63358=CARTESIAN_POINT('Ctrl Pts',(29.8223242552552,22.9883521111826,36.5398379419846));
#63359=CARTESIAN_POINT('Ctrl Pts',(29.7449566415887,22.9783782367966,36.5448450789545));
#63360=CARTESIAN_POINT('Ctrl Pts',(29.7246537813463,22.9757608860973,36.5461590551429));
#63361=CARTESIAN_POINT('Ctrl Pts',(29.7043975141738,22.9728317941917,36.5474730313313));
#63362=CARTESIAN_POINT('Ctrl Pts',(29.6841969077652,22.9695928435682,36.5487870075198));
#63363=CARTESIAN_POINT('Ctrl Pts',(29.6157197224541,22.9586132611944,36.5532412000885));
#63364=CARTESIAN_POINT('Ctrl Pts',(29.5476810636523,22.9440366831893,36.5576953926573));
#63365=CARTESIAN_POINT('Ctrl Pts',(29.4804876480764,22.9259113371853,36.5621495852261));
#63366=CARTESIAN_POINT('Ctrl Pts',(29.4133823824009,22.9078097695147,36.5665979344153));
#63367=CARTESIAN_POINT('Ctrl Pts',(29.3471206295807,22.8861687907933,36.5710462836045));
#63368=CARTESIAN_POINT('Ctrl Pts',(29.2821008695718,22.8610879616586,36.5754946327937));
#63369=CARTESIAN_POINT('Ctrl Pts',(29.2171555459823,22.8360358457507,36.5799378893897));
#63370=CARTESIAN_POINT('Ctrl Pts',(29.1534498458602,22.8075518748946,36.5843811459858));
#63371=CARTESIAN_POINT('Ctrl Pts',(29.091367063864,22.7757853895865,36.5888244025818));
#63372=CARTESIAN_POINT('Ctrl Pts',(29.0702207093069,22.7649652339852,36.5903378444146));
#63373=CARTESIAN_POINT('Ctrl Pts',(29.0492624937621,22.7537646643879,36.5918512862474));
#63374=CARTESIAN_POINT('Ctrl Pts',(29.0285070491141,22.7421908646526,36.5933647280801));
#63375=CARTESIAN_POINT('Origin',(30.,21.,36.5));
#63376=CARTESIAN_POINT('Origin',(30.,21.,34.5704548813952));
#63377=CARTESIAN_POINT('',(29.0285070711969,22.7421908769666,37.3944594262182));
#63378=CARTESIAN_POINT('',(29.0285070491141,22.7421908646526,37.2352940441794));
#63379=CARTESIAN_POINT('',(29.0285070491141,22.7421908646526,34.5704548813952));
#63380=CARTESIAN_POINT('',(28.0052502061177,21.0009068111524,36.728545118564));
#63381=CARTESIAN_POINT('Ctrl Pts',(29.0285070711969,22.7421908769666,37.3944594262182));
#63382=CARTESIAN_POINT('Ctrl Pts',(29.0505519466918,22.7544836980017,37.3929589895291));
#63383=CARTESIAN_POINT('Ctrl Pts',(29.0728387999716,22.766362930873,37.3914477881055));
#63384=CARTESIAN_POINT('Ctrl Pts',(29.1324581808279,22.7967002305002,37.3874118803961));
#63385=CARTESIAN_POINT('Ctrl Pts',(29.1701396501316,22.8144122904256,37.3848676333455));
#63386=CARTESIAN_POINT('Ctrl Pts',(29.2275108683841,22.8392183322913,37.3809871994448));
#63387=CARTESIAN_POINT('Ctrl Pts',(29.246804328479,22.8472032266414,37.3796811885625));
#63388=CARTESIAN_POINT('Ctrl Pts',(29.2821472466523,22.861184676385,37.3772850067571));
#63389=CARTESIAN_POINT('Ctrl Pts',(29.2981555580911,22.8672801944376,37.3761982996956));
#63390=CARTESIAN_POINT('Ctrl Pts',(29.333266665734,22.8801342392277,37.373810887938));
#63391=CARTESIAN_POINT('Ctrl Pts',(29.3523977597723,22.8868093132904,37.3725075377884));
#63392=CARTESIAN_POINT('Ctrl Pts',(29.407980165528,22.9052577907491,37.3687121581381));
#63393=CARTESIAN_POINT('Ctrl Pts',(29.4446714541357,22.9162736252472,37.3661958590089));
#63394=CARTESIAN_POINT('Ctrl Pts',(29.635229488006,22.9675525454124,37.3530655267716));
#63395=CARTESIAN_POINT('Ctrl Pts',(29.793176987161,22.9903591309445,37.3419125284843));
#63396=CARTESIAN_POINT('Ctrl Pts',(30.029961120004,22.9960442174414,37.3254471308986));
#63397=CARTESIAN_POINT('Ctrl Pts',(30.1078522927262,22.9933540726519,37.3200846017565));
#63398=CARTESIAN_POINT('Ctrl Pts',(30.2028333987317,22.9844880897592,37.3137505736092));
#63399=CARTESIAN_POINT('Ctrl Pts',(30.2202519211021,22.9826304516262,37.3125976114903));
#63400=CARTESIAN_POINT('Ctrl Pts',(30.2480971807814,22.9792893130701,37.3107706968631));
#63401=CARTESIAN_POINT('Ctrl Pts',(30.2585401479286,22.9779523250387,37.3100892024933));
#63402=CARTESIAN_POINT('Ctrl Pts',(30.2790498946707,22.9751612989511,37.3087586224246));
#63403=CARTESIAN_POINT('Ctrl Pts',(30.2891169863597,22.97371284027,37.3081092880351));
#63404=CARTESIAN_POINT('Ctrl Pts',(30.3148167709357,22.9698142883536,37.3064602947617));
#63405=CARTESIAN_POINT('Ctrl Pts',(30.3304325917298,22.9672550087523,37.3054665301816));
#63406=CARTESIAN_POINT('Ctrl Pts',(30.3996070685703,22.9550710363641,37.3010942466117));
#63407=CARTESIAN_POINT('Ctrl Pts',(30.452793525566,22.9434422161982,37.2978119933293));
#63408=CARTESIAN_POINT('Ctrl Pts',(30.6311337769079,22.8967287651445,37.2868768608316));
#63409=CARTESIAN_POINT('Ctrl Pts',(30.7533113326398,22.8516032905373,37.2794866753651));
#63410=CARTESIAN_POINT('Ctrl Pts',(30.9406893224414,22.7607559590314,37.2672543835919));
#63411=CARTESIAN_POINT('Ctrl Pts',(31.0090633444993,22.7224828646665,37.2625825347371));
#63412=CARTESIAN_POINT('Ctrl Pts',(31.0971119316904,22.6661517324684,37.2561570018365));
#63413=CARTESIAN_POINT('Ctrl Pts',(31.1189347184272,22.6515753637005,37.2545291011719));
#63414=CARTESIAN_POINT('Ctrl Pts',(31.1536583496348,22.6273778453901,37.2518774502933));
#63415=CARTESIAN_POINT('Ctrl Pts',(31.1667418288865,22.6180233989853,37.2508638535942));
#63416=CARTESIAN_POINT('Ctrl Pts',(31.1939282878908,22.5980843805586,37.2487262022977));
#63417=CARTESIAN_POINT('Ctrl Pts',(31.2080068435841,22.5874690160563,37.2476010075383));
#63418=CARTESIAN_POINT('Ctrl Pts',(31.2416639771832,22.5613842202759,37.2448656346279));
#63419=CARTESIAN_POINT('Ctrl Pts',(31.2610961916772,22.5457316769473,37.2432482838986));
#63420=CARTESIAN_POINT('Ctrl Pts',(31.3340048303601,22.4847141091252,37.2370301152855));
#63421=CARTESIAN_POINT('Ctrl Pts',(31.3853642558693,22.4369094783557,37.2323317138618));
#63422=CARTESIAN_POINT('Ctrl Pts',(31.5317835643389,22.2854643951884,37.2179546765141));
#63423=CARTESIAN_POINT('Ctrl Pts',(31.6185167005224,22.1743842133166,37.2080245036292));
#63424=CARTESIAN_POINT('Ctrl Pts',(31.7214981722948,22.0091607820043,37.1946117744597));
#63425=CARTESIAN_POINT('Ctrl Pts',(31.7482674785112,21.9620412104783,37.1909272696723));
#63426=CARTESIAN_POINT('Ctrl Pts',(31.7805148931126,21.8994760183349,37.1862656040438));
#63427=CARTESIAN_POINT('Ctrl Pts',(31.7877667007291,21.8849749468603,37.1852007429291));
#63428=CARTESIAN_POINT('Ctrl Pts',(31.7988719160402,21.8620746638501,37.1835452895328));
#63429=CARTESIAN_POINT('Ctrl Pts',(31.8028449648706,21.8537346996225,37.1829477806362));
#63430=CARTESIAN_POINT('Ctrl Pts',(31.8110648534309,21.8361667534254,37.1817008774943));
#63431=CARTESIAN_POINT('Ctrl Pts',(31.8152994023827,21.8269333886907,37.1810523074144));
#63432=CARTESIAN_POINT('Ctrl Pts',(31.8259253998944,21.8032885663352,37.1794076986467));
#63433=CARTESIAN_POINT('Ctrl Pts',(31.8322170402126,21.788832581248,37.1784174934755));
#63434=CARTESIAN_POINT('Ctrl Pts',(31.8592010672664,21.7247675677668,37.1740896785286));
#63435=CARTESIAN_POINT('Ctrl Pts',(31.8780564899883,21.6744045382354,37.1708459485977));
#63436=CARTESIAN_POINT('Ctrl Pts',(31.9342600914459,21.5035536178957,37.1601724553701));
#63437=CARTESIAN_POINT('Ctrl Pts',(31.9622189134631,21.3802999894884,37.1529920685108));
#63438=CARTESIAN_POINT('Ctrl Pts',(31.9887832957447,21.174390176544,37.1408187830289));
#63439=CARTESIAN_POINT('Ctrl Pts',(31.9942467866017,21.0929979291003,37.1359662941121));
#63440=CARTESIAN_POINT('Ctrl Pts',(31.9948719384502,20.98461136241,37.1293100692708));
#63441=CARTESIAN_POINT('Ctrl Pts',(31.994483143454,20.9577182779882,37.1276430535329));
#63442=CARTESIAN_POINT('Ctrl Pts',(31.9929893253837,20.9146572834782,37.1249451018273));
#63443=CARTESIAN_POINT('Ctrl Pts',(31.9922307922341,20.8984801697109,37.1239250418011));
#63444=CARTESIAN_POINT('Ctrl Pts',(31.990240848714,20.8648097157594,37.1217875138603));
#63445=CARTESIAN_POINT('Ctrl Pts',(31.9889755627939,20.8473198536811,37.1206690704946));
#63446=CARTESIAN_POINT('Ctrl Pts',(31.9853988037762,20.8055407685583,37.1179769552282));
#63447=CARTESIAN_POINT('Ctrl Pts',(31.9828719958702,20.781273314384,37.116396664224));
#63448=CARTESIAN_POINT('Ctrl Pts',(31.97195288093,20.692285535213,37.1105382221356));
#63449=CARTESIAN_POINT('Ctrl Pts',(31.9608319140613,20.6279475723352,37.1061767578868));
#63450=CARTESIAN_POINT('Ctrl Pts',(31.9205636100355,20.4480506722101,37.0936333132178));
#63451=CARTESIAN_POINT('Ctrl Pts',(31.8841920908289,20.3343961034967,37.0852793466902));
#63452=CARTESIAN_POINT('Ctrl Pts',(31.8071560880185,20.1517821235621,37.0714968516894));
#63453=CARTESIAN_POINT('Ctrl Pts',(31.7720930043362,20.0807744846037,37.0660448691127));
#63454=CARTESIAN_POINT('Ctrl Pts',(31.7242059054002,19.9967803011711,37.0596245336309));
#63455=CARTESIAN_POINT('Ctrl Pts',(31.715309472373,19.981643857447,37.0584688617362));
#63456=CARTESIAN_POINT('Ctrl Pts',(31.7007560212544,19.9576145053395,37.0566387384929));
#63457=CARTESIAN_POINT('Ctrl Pts',(31.695226577374,19.9486459079006,37.0559566996931));
#63458=CARTESIAN_POINT('Ctrl Pts',(31.6842242702422,19.9311129836435,37.0546260433189));
#63459=CARTESIAN_POINT('Ctrl Pts',(31.6787565686178,19.9225459469477,37.0539771650629));
#63460=CARTESIAN_POINT('Ctrl Pts',(31.6646282428951,19.900777712684,37.0523307958152));
#63461=CARTESIAN_POINT('Ctrl Pts',(31.6558757092233,19.8876365267462,37.0513391626404));
#63462=CARTESIAN_POINT('Ctrl Pts',(31.6164950702593,19.8300048831308,37.0469937855974));
#63463=CARTESIAN_POINT('Ctrl Pts',(31.5842208842064,19.786661583213,37.0437348576022));
#63464=CARTESIAN_POINT('Ctrl Pts',(31.46993776086,19.645530844033,37.0329600549671));
#63465=CARTESIAN_POINT('Ctrl Pts',(31.3803225844935,19.5543112020049,37.025698680878));
#63466=CARTESIAN_POINT('Ctrl Pts',(31.2213033017395,19.4208063667873,37.013516124595));
#63467=CARTESIAN_POINT('Ctrl Pts',(31.1569650209088,19.3730813660352,37.0087469674915));
#63468=CARTESIAN_POINT('Ctrl Pts',(31.0675314425625,19.3147344556502,37.002187845244));
#63469=CARTESIAN_POINT('Ctrl Pts',(31.0448334806621,19.3005688517418,37.0005292251542));
#63470=CARTESIAN_POINT('Ctrl Pts',(31.0079697451104,19.2785802147049,36.997841158744));
#63471=CARTESIAN_POINT('Ctrl Pts',(30.9939813000039,19.2704653126584,36.996822430059));
#63472=CARTESIAN_POINT('Ctrl Pts',(30.9646036750718,19.2538970384935,36.9946847698269));
#63473=CARTESIAN_POINT('Ctrl Pts',(30.9491985141791,19.2454750072078,36.993564827598));
#63474=CARTESIAN_POINT('Ctrl Pts',(30.9120204002801,19.2257826048474,36.9908634274208));
#63475=CARTESIAN_POINT('Ctrl Pts',(30.8901473580621,19.2147083801958,36.9892752349388));
#63476=CARTESIAN_POINT('Ctrl Pts',(30.8084305949921,19.1752106044216,36.983343311587));
#63477=CARTESIAN_POINT('Ctrl Pts',(30.7473916484745,19.1493729524247,36.9789134720229));
#63478=CARTESIAN_POINT('Ctrl Pts',(30.5696717075202,19.084372100307,36.9660294515073));
#63479=CARTESIAN_POINT('Ctrl Pts',(30.4505033572301,19.05290000393,36.9573901538706));
#63480=CARTESIAN_POINT('Ctrl Pts',(30.2559420711087,19.020343548509,36.9436898968894));
#63481=CARTESIAN_POINT('Ctrl Pts',(30.1820392630783,19.0121846476817,36.9385825419192));
#63482=CARTESIAN_POINT('Ctrl Pts',(30.0904986835374,19.0072282110943,36.9324971381318));
#63483=CARTESIAN_POINT('Ctrl Pts',(30.0731379592029,19.0065155374074,36.9313537796742));
#63484=CARTESIAN_POINT('Ctrl Pts',(30.0452754435835,19.0057362493949,36.9295383293677));
#63485=CARTESIAN_POINT('Ctrl Pts',(30.0347789939,19.0055255813799,36.9288588541997));
#63486=CARTESIAN_POINT('Ctrl Pts',(30.0140837766536,19.005273650292,36.9275285836808));
#63487=CARTESIAN_POINT('Ctrl Pts',(30.0038854874693,19.0052277138254,36.9268775826602));
#63488=CARTESIAN_POINT('Ctrl Pts',(29.9777397174193,19.0053104592963,36.9252192026252));
#63489=CARTESIAN_POINT('Ctrl Pts',(29.9617929176046,19.0055521714252,36.9242178474603));
#63490=CARTESIAN_POINT('Ctrl Pts',(29.8899994323436,19.0075018093649,36.9197483962374));
#63491=CARTESIAN_POINT('Ctrl Pts',(29.8342318638349,19.0113644823723,36.916381884886));
#63492=CARTESIAN_POINT('Ctrl Pts',(29.6405289045097,19.0329880599958,36.9048330082955));
#63493=CARTESIAN_POINT('Ctrl Pts',(29.5043510713071,19.0628137583321,36.8969455773903));
#63494=CARTESIAN_POINT('Ctrl Pts',(29.306573983947,19.1283713713343,36.8846476268788));
#63495=CARTESIAN_POINT('Ctrl Pts',(29.2419584534486,19.1535967474226,36.8804906917809));
#63496=CARTESIAN_POINT('Ctrl Pts',(29.1556456019692,19.1925879697277,36.8746606160187));
#63497=CARTESIAN_POINT('Ctrl Pts',(29.1327028425009,19.2034844431534,36.8730833353602));
#63498=CARTESIAN_POINT('Ctrl Pts',(29.094279685868,19.2226407633797,36.8703913119002));
#63499=CARTESIAN_POINT('Ctrl Pts',(29.0786885194952,19.2306723685026,36.8692845890791));
#63500=CARTESIAN_POINT('Ctrl Pts',(29.0472320849437,19.2474052902033,36.867021256783));
#63501=CARTESIAN_POINT('Ctrl Pts',(29.0313752935115,19.2561189664718,36.8658642851627));
#63502=CARTESIAN_POINT('Ctrl Pts',(28.9918131296237,19.2785653517224,36.8629359513471));
#63503=CARTESIAN_POINT('Ctrl Pts',(28.9682686622855,19.2925725968994,36.8611548424468));
#63504=CARTESIAN_POINT('Ctrl Pts',(28.8590692792431,19.3606216889673,36.8527076378899));
#63505=CARTESIAN_POINT('Ctrl Pts',(28.7773337549541,19.4206437661393,36.845824652764));
#63506=CARTESIAN_POINT('Ctrl Pts',(28.5919030991364,19.5798642614653,36.8289010611239));
#63507=CARTESIAN_POINT('Ctrl Pts',(28.4936435258082,19.684547782622,36.8187645711298));
#63508=CARTESIAN_POINT('Ctrl Pts',(28.3924323754014,19.8187402428948,36.8074754861495));
#63509=CARTESIAN_POINT('Ctrl Pts',(28.3778032665314,19.8389116428921,36.8058198795782));
#63510=CARTESIAN_POINT('Ctrl Pts',(28.3566819727408,19.8692135930201,36.8033994341084));
#63511=CARTESIAN_POINT('Ctrl Pts',(28.3498978380449,19.8791365338724,36.8026171413259));
#63512=CARTESIAN_POINT('Ctrl Pts',(28.3377998356182,19.8971798289228,36.8012140966905));
#63513=CARTESIAN_POINT('Ctrl Pts',(28.3324550802124,19.9052782706601,36.800591408918));
#63514=CARTESIAN_POINT('Ctrl Pts',(28.3202544760473,19.9240614891959,36.7991631418085));
#63515=CARTESIAN_POINT('Ctrl Pts',(28.3134412459352,19.9347731257423,36.7983603058982));
#63516=CARTESIAN_POINT('Ctrl Pts',(28.2915224937793,19.9699709380131,36.7957576078963));
#63517=CARTESIAN_POINT('Ctrl Pts',(28.2768436795831,19.9947200654301,36.7939828145033));
#63518=CARTESIAN_POINT('Ctrl Pts',(28.2417000832152,20.0570068758419,36.7896295976838));
#63519=CARTESIAN_POINT('Ctrl Pts',(28.2218963417669,20.0949019781294,36.7870805022924));
#63520=CARTESIAN_POINT('Ctrl Pts',(28.1552996583477,20.2329743084075,36.7780417660263));
#63521=CARTESIAN_POINT('Ctrl Pts',(28.1156336597192,20.3363640582666,36.7717205270939));
#63522=CARTESIAN_POINT('Ctrl Pts',(28.0605293921342,20.5256754378019,36.7601816624638));
#63523=CARTESIAN_POINT('Ctrl Pts',(28.0417667170985,20.610320602388,36.7550359031402));
#63524=CARTESIAN_POINT('Ctrl Pts',(28.0244772296112,20.7224099562335,36.7480704341553));
#63525=CARTESIAN_POINT('Ctrl Pts',(28.0209247192546,20.7489873005574,36.7464084049198));
#63526=CARTESIAN_POINT('Ctrl Pts',(28.0160898839718,20.7916978437649,36.7437168309782));
#63527=CARTESIAN_POINT('Ctrl Pts',(28.0144662497862,20.8077895977779,36.7426980830205));
#63528=CARTESIAN_POINT('Ctrl Pts',(28.0115968167425,20.8401656270264,36.740638199966));
#63529=CARTESIAN_POINT('Ctrl Pts',(28.0103549747104,20.8564489876068,36.7395970233493));
#63530=CARTESIAN_POINT('Ctrl Pts',(28.0080226188934,20.8929348103733,36.7372517647791));
#63531=CARTESIAN_POINT('Ctrl Pts',(28.0070392649365,20.9131420696515,36.7359444286128));
#63532=CARTESIAN_POINT('Ctrl Pts',(28.0056098626701,20.9559049249684,36.7331590673407));
#63533=CARTESIAN_POINT('Ctrl Pts',(28.0052387767564,20.9784598849025,36.7316789202021));
#63534=CARTESIAN_POINT('Ctrl Pts',(28.0052502584425,21.0010154093453,36.7301874407357));
#63535=CARTESIAN_POINT('Ctrl Pts',(29.0285070491141,22.7421908646526,36.5933647280801));
#63536=CARTESIAN_POINT('Ctrl Pts',(28.9676176456079,22.7082372792619,36.5978046508089));
#63537=CARTESIAN_POINT('Ctrl Pts',(28.9084752835363,22.6710682151059,36.6022445735377));
#63538=CARTESIAN_POINT('Ctrl Pts',(28.8514330820545,22.6308959493178,36.6066844962665));
#63539=CARTESIAN_POINT('Ctrl Pts',(28.7944006664215,22.5907305752643,36.6111236573064));
#63540=CARTESIAN_POINT('Ctrl Pts',(28.7394680955456,22.5475633047902,36.6155628183463));
#63541=CARTESIAN_POINT('Ctrl Pts',(28.6869589491316,22.501649346963,36.6200019793861));
#63542=CARTESIAN_POINT('Ctrl Pts',(28.6319025478678,22.4535080714257,36.6246564871848));
#63543=CARTESIAN_POINT('Ctrl Pts',(28.5795111414156,22.4023472009318,36.6293109949835));
#63544=CARTESIAN_POINT('Ctrl Pts',(28.5301161934672,22.3485062690965,36.6339655027822));
#63545=CARTESIAN_POINT('Ctrl Pts',(28.4829441605491,22.2970883343813,36.6384105443141));
#63546=CARTESIAN_POINT('Ctrl Pts',(28.4385049568665,22.2432268115348,36.642855585846));
#63547=CARTESIAN_POINT('Ctrl Pts',(28.3970458829366,22.1872513049432,36.6473006273779));
#63548=CARTESIAN_POINT('Ctrl Pts',(28.355557612108,22.1312363784844,36.6517487992602));
#63549=CARTESIAN_POINT('Ctrl Pts',(28.3170539153061,22.0731049144069,36.6561969711424));
#63550=CARTESIAN_POINT('Ctrl Pts',(28.2817379201812,22.0132141864171,36.6606451430247));
#63551=CARTESIAN_POINT('Ctrl Pts',(28.2463644782723,21.9532260371397,36.6651005505284));
#63552=CARTESIAN_POINT('Ctrl Pts',(28.2141893024353,21.8914733502745,36.669555958032));
#63553=CARTESIAN_POINT('Ctrl Pts',(28.1853684355378,21.8283355888512,36.6740113655357));
#63554=CARTESIAN_POINT('Ctrl Pts',(28.1813907920867,21.8196217807573,36.6746262680139));
#63555=CARTESIAN_POINT('Ctrl Pts',(28.1774769626901,21.8108816159094,36.6752411704921));
#63556=CARTESIAN_POINT('Ctrl Pts',(28.1736272830851,21.8021161146672,36.6758560729703));
#63557=CARTESIAN_POINT('Ctrl Pts',(28.1429611739475,21.7322911304302,36.6807543160555));
#63558=CARTESIAN_POINT('Ctrl Pts',(28.116265697656,21.6606202638874,36.6856525591407));
#63559=CARTESIAN_POINT('Ctrl Pts',(28.0937438469357,21.5875500331072,36.6905508022258));
#63560=CARTESIAN_POINT('Ctrl Pts',(28.0712891522905,21.514697684506,36.6954344396383));
#63561=CARTESIAN_POINT('Ctrl Pts',(28.0529833994963,21.4404545853452,36.7003180770508));
#63562=CARTESIAN_POINT('Ctrl Pts',(28.0389815215822,21.365286312095,36.7052017144632));
#63563=CARTESIAN_POINT('Ctrl Pts',(28.0250482095369,21.2904861307532,36.7100614371662));
#63564=CARTESIAN_POINT('Ctrl Pts',(28.0153768565579,21.2147701145771,36.7149211598692));
#63565=CARTESIAN_POINT('Ctrl Pts',(28.0100720374931,21.1386155349627,36.7197808825722));
#63566=CARTESIAN_POINT('Ctrl Pts',(28.0068830567618,21.0928353709229,36.7227022945695));
#63567=CARTESIAN_POINT('Ctrl Pts',(28.0052711132345,21.0468970559952,36.7256237065667));
#63568=CARTESIAN_POINT('Ctrl Pts',(28.0052502061177,21.0009068111524,36.728545118564));
#63569=CARTESIAN_POINT('',(28.29025763663,22.0275229169844,36.501576848773));
#63570=CARTESIAN_POINT('Origin',(30.,21.,36.5));
#63571=CARTESIAN_POINT('',(28.0052500270373,21.000328428416,36.5704549034975));
#63572=CARTESIAN_POINT('Ctrl Pts',(28.2902566323839,22.0275238096476,36.5015864635853));
#63573=CARTESIAN_POINT('Ctrl Pts',(28.2530535621634,21.9656199374772,36.5061693646417));
#63574=CARTESIAN_POINT('Ctrl Pts',(28.2192474515991,21.9017453975362,36.510752265698));
#63575=CARTESIAN_POINT('Ctrl Pts',(28.1890241385836,21.8362977889886,36.5153351667544));
#63576=CARTESIAN_POINT('Ctrl Pts',(28.1587307817518,21.7706985028179,36.5199286888793));
#63577=CARTESIAN_POINT('Ctrl Pts',(28.1320369926429,21.7035192682946,36.5245222110042));
#63578=CARTESIAN_POINT('Ctrl Pts',(28.1090803750041,21.6351775612419,36.5291157331292));
#63579=CARTESIAN_POINT('Ctrl Pts',(28.0860958385404,21.5667527400224,36.5337148416929));
#63580=CARTESIAN_POINT('Ctrl Pts',(28.066857645781,21.497163054947,36.5383139502567));
#63581=CARTESIAN_POINT('Ctrl Pts',(28.0514526602536,21.4268381745663,36.5429130588204));
#63582=CARTESIAN_POINT('Ctrl Pts',(28.0360074155949,21.3563295083206,36.5475241866175));
#63583=CARTESIAN_POINT('Ctrl Pts',(28.0244154684101,21.2850822436007,36.5521353144146));
#63584=CARTESIAN_POINT('Ctrl Pts',(28.0167120719566,21.2135335031729,36.5567464422117));
#63585=CARTESIAN_POINT('Ctrl Pts',(28.0112867761488,21.1631436415273,36.5599939360227));
#63586=CARTESIAN_POINT('Ctrl Pts',(28.0077891046199,21.1126043416051,36.5632414298337));
#63587=CARTESIAN_POINT('Ctrl Pts',(28.0062158685675,21.0620677029381,36.5664889236447));
#63588=CARTESIAN_POINT('Ctrl Pts',(28.0055754375071,21.0414953081962,36.5678109095616));
#63589=CARTESIAN_POINT('Ctrl Pts',(28.0052534198484,21.0209135090081,36.5691328954784));
#63590=CARTESIAN_POINT('Ctrl Pts',(28.005250027094,21.0003287725725,36.5704548813952));
#63591=CARTESIAN_POINT('Ctrl Pts',(28.0052500269806,21.0003280842595,36.5704549255998));
#63592=CARTESIAN_POINT('Ctrl Pts',(28.0052386714972,20.9312868256578,36.574888869682));
#63593=CARTESIAN_POINT('Ctrl Pts',(28.0088160317775,20.8621028756339,36.5793228137642));
#63594=CARTESIAN_POINT('Ctrl Pts',(28.0160004941859,20.7931823909103,36.5837567578465));
#63595=CARTESIAN_POINT('Ctrl Pts',(28.0234042602584,20.7221581280657,36.588326046806));
#63596=CARTESIAN_POINT('Ctrl Pts',(28.0346390301168,20.651414201514,36.5928953357655));
#63597=CARTESIAN_POINT('Ctrl Pts',(28.0496669166672,20.5813970538116,36.5974646247251));
#63598=CARTESIAN_POINT('Ctrl Pts',(28.0642105588504,20.5136360722889,36.6018866772496));
#63599=CARTESIAN_POINT('Ctrl Pts',(28.0823064725704,20.4465562705405,36.6063087297742));
#63600=CARTESIAN_POINT('Ctrl Pts',(28.1038678101182,20.3805564747339,36.6107307822988));
#63601=CARTESIAN_POINT('Ctrl Pts',(28.1254162281456,20.3145962259038,36.6151501851362));
#63602=CARTESIAN_POINT('Ctrl Pts',(28.1504257983438,20.249715168508,36.6195695879737));
#63603=CARTESIAN_POINT('Ctrl Pts',(28.1787594529453,20.1862983149435,36.6239889908111));
#63604=CARTESIAN_POINT('Ctrl Pts',(28.2070859824803,20.1228974088203,36.628407282301));
#63605=CARTESIAN_POINT('Ctrl Pts',(28.2387347352602,20.0609604267976,36.6328255737909));
#63606=CARTESIAN_POINT('Ctrl Pts',(28.2735207007135,20.0008519671064,36.6372438652808));
#63607=CARTESIAN_POINT('Ctrl Pts',(28.3083100144199,19.9407377217963,36.6416625820444));
#63608=CARTESIAN_POINT('Ctrl Pts',(28.3462368897675,19.8824527744823,36.6460812988081));
#63609=CARTESIAN_POINT('Ctrl Pts',(28.3870715365556,19.8263350843146,36.6505000155717));
#63610=CARTESIAN_POINT('Ctrl Pts',(28.4279494873314,19.770157882924,36.6549234182595));
#63611=CARTESIAN_POINT('Ctrl Pts',(28.4717410687165,19.7161529232429,36.6593468209473));
#63612=CARTESIAN_POINT('Ctrl Pts',(28.5181751866023,19.6646263500807,36.6637702236351));
#63613=CARTESIAN_POINT('Ctrl Pts',(28.5646391040617,19.6130667092093,36.6681964650871));
#63614=CARTESIAN_POINT('Ctrl Pts',(28.6137485814085,19.5639889673164,36.6726227065391));
#63615=CARTESIAN_POINT('Ctrl Pts',(28.6651965229941,19.5176615635177,36.6770489479911));
#63616=CARTESIAN_POINT('Ctrl Pts',(28.7167278672448,19.4712590579981,36.6814823648582));
#63617=CARTESIAN_POINT('Ctrl Pts',(28.7706048521435,19.4276160918823,36.6859157817252));
#63618=CARTESIAN_POINT('Ctrl Pts',(28.8264891705401,19.3869594252964,36.6903491985923));
#63619=CARTESIAN_POINT('Ctrl Pts',(28.8393906176858,19.3775734320494,36.6913726966867));
#63620=CARTESIAN_POINT('Ctrl Pts',(28.8523989386336,19.3683464074629,36.6923961947811));
#63621=CARTESIAN_POINT('Ctrl Pts',(28.8655097834363,19.3592807945839,36.6934196928754));
#63622=CARTESIAN_POINT('Ctrl Pts',(28.9226695512531,19.3197571532715,36.6978818701277));
#63623=CARTESIAN_POINT('Ctrl Pts',(28.9820056711569,19.2831490561882,36.70234404738));
#63624=CARTESIAN_POINT('Ctrl Pts',(29.0431890178685,19.2497027946739,36.7068062246323));
#63625=CARTESIAN_POINT('Ctrl Pts',(29.1042829228631,19.2163054270369,36.7112618787894));
#63626=CARTESIAN_POINT('Ctrl Pts',(29.1672182698099,19.1860609517794,36.7157175329465));
#63627=CARTESIAN_POINT('Ctrl Pts',(29.2316367156414,19.159172624674,36.7201731871036));
#63628=CARTESIAN_POINT('Ctrl Pts',(29.2959823945075,19.1323146705766,36.7246238081614));
#63629=CARTESIAN_POINT('Ctrl Pts',(29.3618073968103,19.1088055213526,36.7290744292193));
#63630=CARTESIAN_POINT('Ctrl Pts',(29.4287300887424,19.0888018807586,36.7335250502771));
#63631=CARTESIAN_POINT('Ctrl Pts',(29.4956125476592,19.0688102660823,36.7379729956819));
#63632=CARTESIAN_POINT('Ctrl Pts',(29.5635909208368,19.0523201179599,36.7424209410867));
#63633=CARTESIAN_POINT('Ctrl Pts',(29.6322663951171,19.0394389684736,36.7468688864915));
#63634=CARTESIAN_POINT('Ctrl Pts',(29.7009236688492,19.0265612327822,36.7513156530905));
#63635=CARTESIAN_POINT('Ctrl Pts',(29.7702771979811,19.0172906864354,36.7557624196896));
#63636=CARTESIAN_POINT('Ctrl Pts',(29.8399176209918,19.0116838293594,36.7602091862886));
#63637=CARTESIAN_POINT('Ctrl Pts',(29.9095629973759,19.0060765734797,36.7646562691765));
#63638=CARTESIAN_POINT('Ctrl Pts',(29.9794948221041,19.0041335609959,36.7691033520645));
#63639=CARTESIAN_POINT('Ctrl Pts',(30.0493000077049,19.0058593149579,36.7735504349525));
#63640=CARTESIAN_POINT('Ctrl Pts',(30.1191800615645,19.0075869198453,36.7780022874768));
#63641=CARTESIAN_POINT('Ctrl Pts',(30.1889327169807,19.0129911325344,36.7824541400012));
#63642=CARTESIAN_POINT('Ctrl Pts',(30.2581472309743,19.0220243758731,36.7869059925255));
#63643=CARTESIAN_POINT('Ctrl Pts',(30.3274030821619,19.031063014163,36.7913605038432));
#63644=CARTESIAN_POINT('Ctrl Pts',(30.3961196727158,19.0437349089237,36.795815015161));
#63645=CARTESIAN_POINT('Ctrl Pts',(30.4638964470654,19.0599413284903,36.8002695264787));
#63646=CARTESIAN_POINT('Ctrl Pts',(30.5317904704488,19.0761757840184,36.8047317437864));
#63647=CARTESIAN_POINT('Ctrl Pts',(30.5987409649366,19.0959568315954,36.8091939610942));
#63648=CARTESIAN_POINT('Ctrl Pts',(30.6643632856274,19.1191361061442,36.813656178402));
#63649=CARTESIAN_POINT('Ctrl Pts',(30.6971791408953,19.1307274017705,36.8158876063034));
#63650=CARTESIAN_POINT('Ctrl Pts',(30.7296631820897,19.1431677458785,36.8181190342048));
#63651=CARTESIAN_POINT('Ctrl Pts',(30.761769523972,19.1564342282285,36.8203504621062));
#63652=CARTESIAN_POINT('Ctrl Pts',(30.8258050956774,19.1828940094428,36.824801008416));
#63653=CARTESIAN_POINT('Ctrl Pts',(30.8885889960873,19.2127472807336,36.8292515547259));
#63654=CARTESIAN_POINT('Ctrl Pts',(30.9497368226418,19.2458541878686,36.8337021010357));
#63655=CARTESIAN_POINT('Ctrl Pts',(31.0107920689531,19.2789109698283,36.8381459090413));
#63656=CARTESIAN_POINT('Ctrl Pts',(31.0702157298272,19.3152113794572,36.8425897170468));
#63657=CARTESIAN_POINT('Ctrl Pts',(31.1276433749924,19.3545675397222,36.8470335250524));
#63658=CARTESIAN_POINT('Ctrl Pts',(31.1850026111637,19.3938768181184,36.8514720395023));
#63659=CARTESIAN_POINT('Ctrl Pts',(31.2403701512933,19.436234341885,36.8559105539523));
#63660=CARTESIAN_POINT('Ctrl Pts',(31.2934077780998,19.4814072691959,36.8603490684022));
#63661=CARTESIAN_POINT('Ctrl Pts',(31.3464115884187,19.5265513945067,36.8647847528807));
#63662=CARTESIAN_POINT('Ctrl Pts',(31.3970880597347,19.5745070452748,36.8692204373592));
#63663=CARTESIAN_POINT('Ctrl Pts',(31.4451307387815,19.625000105335,36.8736561218377));
#63664=CARTESIAN_POINT('Ctrl Pts',(31.4931591819423,19.6754782034183,36.8780904919453));
#63665=CARTESIAN_POINT('Ctrl Pts',(31.5385550441581,19.728491863154,36.8825248620529));
#63666=CARTESIAN_POINT('Ctrl Pts',(31.5810488507624,19.7837302544242,36.8869592321605));
#63667=CARTESIAN_POINT('Ctrl Pts',(31.6235445674886,19.838971128693,36.8913938015957));
#63668=CARTESIAN_POINT('Ctrl Pts',(31.6631376725093,19.8964365428245,36.8958283710309));
#63669=CARTESIAN_POINT('Ctrl Pts',(31.6996002142036,19.9557841820873,36.9002629404661));
#63670=CARTESIAN_POINT('Ctrl Pts',(31.7361012208808,20.015194428229,36.9047021880074));
#63671=CARTESIAN_POINT('Ctrl Pts',(31.7694648155461,20.0764904438482,36.9091414355486));
#63672=CARTESIAN_POINT('Ctrl Pts',(31.7995080072554,20.1393034830303,36.9135806830899));
#63673=CARTESIAN_POINT('Ctrl Pts',(31.8295687154451,20.2021531449316,36.9180225189045));
#63674=CARTESIAN_POINT('Ctrl Pts',(31.8563049794955,20.2665211377134,36.9224643547192));
#63675=CARTESIAN_POINT('Ctrl Pts',(31.8795822660123,20.3320194106172,36.9269061905338));
#63676=CARTESIAN_POINT('Ctrl Pts',(31.9029000655277,20.3976316801177,36.9313557571502));
#63677=CARTESIAN_POINT('Ctrl Pts',(31.9227467310129,20.4643776864229,36.9358053237667));
#63678=CARTESIAN_POINT('Ctrl Pts',(31.9390380341855,20.531855722579,36.9402548903831));
#63679=CARTESIAN_POINT('Ctrl Pts',(31.9476132701235,20.567374064761,36.9425970040344));
#63680=CARTESIAN_POINT('Ctrl Pts',(31.9552043041219,20.6030950764752,36.9449391176857));
#63681=CARTESIAN_POINT('Ctrl Pts',(31.9618046223388,20.6389595780662,36.947281231337));
#63682=CARTESIAN_POINT('Ctrl Pts',(31.9743612682226,20.7071892954034,36.9517369394972));
#63683=CARTESIAN_POINT('Ctrl Pts',(31.983378916413,20.7762090129602,36.9561926476574));
#63684=CARTESIAN_POINT('Ctrl Pts',(31.9887669676629,20.8456189427659,36.9606483558175));
#63685=CARTESIAN_POINT('Ctrl Pts',(31.9941469496941,20.9149249233175,36.9650973910486));
#63686=CARTESIAN_POINT('Ctrl Pts',(31.995908086141,20.9846194724866,36.9695464262797));
#63687=CARTESIAN_POINT('Ctrl Pts',(31.9940109741103,21.0542936241897,36.9739954615108));
#63688=CARTESIAN_POINT('Ctrl Pts',(31.9921160888979,21.1238859928087,36.9784392744922));
#63689=CARTESIAN_POINT('Ctrl Pts',(31.9865714971795,21.1934575249014,36.9828830874735));
#63690=CARTESIAN_POINT('Ctrl Pts',(31.9773897947127,21.2625969578388,36.9873269004548));
#63691=CARTESIAN_POINT('Ctrl Pts',(31.9682138543114,21.3316930016611,36.9917679246786));
#63692=CARTESIAN_POINT('Ctrl Pts',(31.9554053955368,21.4003570005243,36.9962089489025));
#63693=CARTESIAN_POINT('Ctrl Pts',(31.9390289146708,21.4681820485352,37.0006499731263));
#63694=CARTESIAN_POINT('Ctrl Pts',(31.9226571582324,21.5359875297947,37.0050897161654));
#63695=CARTESIAN_POINT('Ctrl Pts',(31.902719537934,21.6029540654654,37.0095294592044));
#63696=CARTESIAN_POINT('Ctrl Pts',(31.879331443147,21.6686859422024,37.0139692022435));
#63697=CARTESIAN_POINT('Ctrl Pts',(31.8559421655853,21.734421143109,37.0184091698077));
#63698=CARTESIAN_POINT('Ctrl Pts',(31.8291022333342,21.7989211011065,37.0228491373719));
#63699=CARTESIAN_POINT('Ctrl Pts',(31.7989760009868,21.8618079312547,37.0272891049362));
#63700=CARTESIAN_POINT('Ctrl Pts',(31.7688180178141,21.9247610394802,37.0317337518985));
#63701=CARTESIAN_POINT('Ctrl Pts',(31.7353670334275,21.9860971845992,37.0361783988608));
#63702=CARTESIAN_POINT('Ctrl Pts',(31.6988339900007,22.0454619251405,37.0406230458231));
#63703=CARTESIAN_POINT('Ctrl Pts',(31.6622795997693,22.1048613533888,37.0450702898592));
#63704=CARTESIAN_POINT('Ctrl Pts',(31.6226398438709,22.162286681586,37.0495175338953));
#63705=CARTESIAN_POINT('Ctrl Pts',(31.5801681727807,22.2174136964199,37.0539647779315));
#63706=CARTESIAN_POINT('Ctrl Pts',(31.5376230902326,22.2726359972274,37.0584197089424));
#63707=CARTESIAN_POINT('Ctrl Pts',(31.4922366400443,22.3255516837158,37.0628746399534));
#63708=CARTESIAN_POINT('Ctrl Pts',(31.444301042517,22.3758713824644,37.0673295709644));
#63709=CARTESIAN_POINT('Ctrl Pts',(31.4196157836681,22.4017843751646,37.0696237141655));
#63710=CARTESIAN_POINT('Ctrl Pts',(31.3942550895449,22.4270095608114,37.0719178573667));
#63711=CARTESIAN_POINT('Ctrl Pts',(31.3682622464784,22.4515116215043,37.0742120005678));
#63712=CARTESIAN_POINT('Ctrl Pts',(31.3177777071752,22.4991006921917,37.078667794892));
#63713=CARTESIAN_POINT('Ctrl Pts',(31.2647084104482,22.5441461487519,37.0831235892161));
#63714=CARTESIAN_POINT('Ctrl Pts',(31.2093410011878,22.5863549115334,37.0875793835403));
#63715=CARTESIAN_POINT('Ctrl Pts',(31.1540562981378,22.6285006241042,37.0920285219298));
#63716=CARTESIAN_POINT('Ctrl Pts',(31.0964806819931,22.6678177591639,37.0964776603192));
#63717=CARTESIAN_POINT('Ctrl Pts',(31.0369362891096,22.7040512594484,37.1009267987086));
#63718=CARTESIAN_POINT('Ctrl Pts',(30.9774614551959,22.7402424322385,37.1053707396736));
#63719=CARTESIAN_POINT('Ctrl Pts',(30.9160228283773,22.773356871914,37.1098146806386));
#63720=CARTESIAN_POINT('Ctrl Pts',(30.8529726938128,22.8031819503616,37.1142586216036));
#63721=CARTESIAN_POINT('Ctrl Pts',(30.789961908263,22.8329884152493,37.1186997891455));
#63722=CARTESIAN_POINT('Ctrl Pts',(30.7253420513037,22.8595093828041,37.1231409566874));
#63723=CARTESIAN_POINT('Ctrl Pts',(30.6594899134094,22.8825781833993,37.1275821242293));
#63724=CARTESIAN_POINT('Ctrl Pts',(30.5936565478156,22.9056404078306,37.132022025739));
#63725=CARTESIAN_POINT('Ctrl Pts',(30.5265920600452,22.9252522573811,37.1364619272486));
#63726=CARTESIAN_POINT('Ctrl Pts',(30.4586914576963,22.9412958839745,37.1409018287583));
#63727=CARTESIAN_POINT('Ctrl Pts',(30.3907871924322,22.9573403760455,37.1453419697795));
#63728=CARTESIAN_POINT('Ctrl Pts',(30.3220471995847,22.9698161528819,37.1497821108008));
#63729=CARTESIAN_POINT('Ctrl Pts',(30.2528780842132,22.9786561694809,37.154222251822));
#63730=CARTESIAN_POINT('Ctrl Pts',(30.183635734459,22.9875055456496,37.1586670939441));
#63731=CARTESIAN_POINT('Ctrl Pts',(30.1139638414636,22.9927114163849,37.1631119360662));
#63732=CARTESIAN_POINT('Ctrl Pts',(30.0442746033641,22.9942585895508,37.1675567781883));
#63733=CARTESIAN_POINT('Ctrl Pts',(29.9745444485121,22.9958066711109,37.1720042300176));
#63734=CARTESIAN_POINT('Ctrl Pts',(29.9047974172846,22.9936917942619,37.1764516818469));
#63735=CARTESIAN_POINT('Ctrl Pts',(29.8354433862942,22.9879508754961,37.1808991336762));
#63736=CARTESIAN_POINT('Ctrl Pts',(29.7659692095172,22.9822000114223,37.1853542900699));
#63737=CARTESIAN_POINT('Ctrl Pts',(29.6968898764961,22.9728106325431,37.1898094464635));
#63738=CARTESIAN_POINT('Ctrl Pts',(29.6286070416676,22.9598711266308,37.1942646028572));
#63739=CARTESIAN_POINT('Ctrl Pts',(29.5934671800723,22.9532121698372,37.196557325171));
#63740=CARTESIAN_POINT('Ctrl Pts',(29.5585380467932,22.9456138345229,37.1988500474848));
#63741=CARTESIAN_POINT('Ctrl Pts',(29.5238726929801,22.9370932734409,37.2011427697985));
#63742=CARTESIAN_POINT('Ctrl Pts',(29.4565256301231,22.9205397206959,37.2055970186896));
#63743=CARTESIAN_POINT('Ctrl Pts',(29.3899099067316,22.9004371101155,37.2100512675806));
#63744=CARTESIAN_POINT('Ctrl Pts',(29.3244270369207,22.8768667331636,37.2145055164717));
#63745=CARTESIAN_POINT('Ctrl Pts',(29.2590489305348,22.8533340655153,37.218952639188));
#63746=CARTESIAN_POINT('Ctrl Pts',(29.1948005354634,22.8263448123012,37.2233997619044));
#63747=CARTESIAN_POINT('Ctrl Pts',(29.1320706273667,22.7960306697327,37.2278468846207));
#63748=CARTESIAN_POINT('Ctrl Pts',(29.0970547557198,22.7791092974962,37.2303292711403));
#63749=CARTESIAN_POINT('Ctrl Pts',(29.06251179142,22.7611528326649,37.2328116576599));
#63750=CARTESIAN_POINT('Ctrl Pts',(29.0285070491141,22.7421908646526,37.2352940441794));
#63751=CARTESIAN_POINT('Origin',(30.,21.,34.5704548813952));
#63752=CARTESIAN_POINT('',(29.0285070492154,22.7421908647091,38.1915268296408));
#63753=CARTESIAN_POINT('',(29.0285070491141,22.7421908646526,38.0351948256389));
#63754=CARTESIAN_POINT('',(29.0285070491141,22.7421908646526,34.5704548813952));
#63755=CARTESIAN_POINT('Ctrl Pts',(29.0285070492154,22.7421908647091,38.1915268296408));
#63756=CARTESIAN_POINT('Ctrl Pts',(29.0365800098479,22.7466925668505,38.1909595153784));
#63757=CARTESIAN_POINT('Ctrl Pts',(29.04468452496,22.7511383037825,38.1903948448985));
#63758=CARTESIAN_POINT('Ctrl Pts',(29.17424040473,22.8210390713102,38.1814406805563));
#63759=CARTESIAN_POINT('Ctrl Pts',(29.3021415357132,22.8737832221873,38.1735891043926));
#63760=CARTESIAN_POINT('Ctrl Pts',(29.5114982215156,22.9356768422155,38.1608674012811));
#63761=CARTESIAN_POINT('Ctrl Pts',(29.5898222654284,22.9537736424879,38.1561393308334));
#63762=CARTESIAN_POINT('Ctrl Pts',(29.706476237995,22.9734016687763,38.148975413452));
#63763=CARTESIAN_POINT('Ctrl Pts',(29.7441040460161,22.9786326899555,38.1466469977521));
#63764=CARTESIAN_POINT('Ctrl Pts',(29.8019359873461,22.9849952835544,38.1430291420011));
#63765=CARTESIAN_POINT('Ctrl Pts',(29.8220472691853,22.986899193958,38.1417638477182));
#63766=CARTESIAN_POINT('Ctrl Pts',(29.8592611977757,22.9898526677302,38.1394076556626));
#63767=CARTESIAN_POINT('Ctrl Pts',(29.8763552645962,22.9909879455026,38.1383195636265));
#63768=CARTESIAN_POINT('Ctrl Pts',(29.9143811365715,22.9930217910881,38.1358853082497));
#63769=CARTESIAN_POINT('Ctrl Pts',(29.9353165000315,22.9938110338678,38.1345358384149));
#63770=CARTESIAN_POINT('Ctrl Pts',(29.9968882439604,22.9951614838551,38.1305381587301));
#63771=CARTESIAN_POINT('Ctrl Pts',(30.0375318190381,22.9948107671914,38.1278621632728));
#63772=CARTESIAN_POINT('Ctrl Pts',(30.2258584634346,22.9874283790031,38.1152852304615));
#63773=CARTESIAN_POINT('Ctrl Pts',(30.3724640935126,22.9652333253242,38.1049404294473));
#63774=CARTESIAN_POINT('Ctrl Pts',(30.570741395996,22.9122190722138,38.0906530865214));
#63775=CARTESIAN_POINT('Ctrl Pts',(30.6255735345576,22.894989709113,38.0866755334977));
#63776=CARTESIAN_POINT('Ctrl Pts',(30.7125786403059,22.86346197472,38.0803899137055));
#63777=CARTESIAN_POINT('Ctrl Pts',(30.7452503010156,22.8506380458435,38.0780358611323));
#63778=CARTESIAN_POINT('Ctrl Pts',(30.7901627955289,22.831626967783,38.0748245414112));
#63779=CARTESIAN_POINT('Ctrl Pts',(30.8027021492279,22.8261664429801,38.0739306968194));
#63780=CARTESIAN_POINT('Ctrl Pts',(30.824126600144,22.8165733941425,38.0724094441732));
#63781=CARTESIAN_POINT('Ctrl Pts',(30.8330390066345,22.8125036769592,38.071778439769));
#63782=CARTESIAN_POINT('Ctrl Pts',(30.8522186885074,22.8035741962733,38.0704247585852));
#63783=CARTESIAN_POINT('Ctrl Pts',(30.8624749173958,22.7986921933208,38.0697034188892));
#63784=CARTESIAN_POINT('Ctrl Pts',(30.8914706320288,22.7845850817138,38.0676697497463));
#63785=CARTESIAN_POINT('Ctrl Pts',(30.9101082760709,22.7751526152732,38.0663693225785));
#63786=CARTESIAN_POINT('Ctrl Pts',(31.0575902165645,22.697578813938,38.0561059090748));
#63787=CARTESIAN_POINT('Ctrl Pts',(31.1787770002033,22.6157867233193,38.0478142623707));
#63788=CARTESIAN_POINT('Ctrl Pts',(31.3696085324446,22.4539941518065,38.0332522327653));
#63789=CARTESIAN_POINT('Ctrl Pts',(31.4438070964583,22.3803419914948,38.0271035197814));
#63790=CARTESIAN_POINT('Ctrl Pts',(31.5298650756104,22.2803511528691,38.0190096932702));
#63791=CARTESIAN_POINT('Ctrl Pts',(31.5473975758435,22.2591055760042,38.0173037397508));
#63792=CARTESIAN_POINT('Ctrl Pts',(31.5757246577007,22.2232937776063,38.0144461502316));
#63793=CARTESIAN_POINT('Ctrl Pts',(31.586770925177,22.2089308745206,38.0133047009676));
#63794=CARTESIAN_POINT('Ctrl Pts',(31.6081048038498,22.1803953265292,38.0110447796811));
#63795=CARTESIAN_POINT('Ctrl Pts',(31.6184044794508,22.1662337225799,38.0099269219977));
#63796=CARTESIAN_POINT('Ctrl Pts',(31.6431048365196,22.1313143914951,38.0071784874097));
#63797=CARTESIAN_POINT('Ctrl Pts',(31.6572998571073,22.1104156170168,38.0055402726073));
#63798=CARTESIAN_POINT('Ctrl Pts',(31.7081404802935,22.032417769243,37.9994477387248));
#63799=CARTESIAN_POINT('Ctrl Pts',(31.742259746902,21.9737348714386,37.9949035570723));
#63800=CARTESIAN_POINT('Ctrl Pts',(31.8377247831637,21.7884010041351,37.9806857591672));
#63801=CARTESIAN_POINT('Ctrl Pts',(31.8887223093803,21.6569104137249,37.9707508615294));
#63802=CARTESIAN_POINT('Ctrl Pts',(31.9401255390151,21.4670006653344,37.9571877036123));
#63803=CARTESIAN_POINT('Ctrl Pts',(31.9524963592611,21.4122327344734,37.9533682340408));
#63804=CARTESIAN_POINT('Ctrl Pts',(31.965399007328,21.3413050821042,37.9485960998558));
#63805=CARTESIAN_POINT('Ctrl Pts',(31.9680676605472,21.3255643400712,37.9475479711228));
#63806=CARTESIAN_POINT('Ctrl Pts',(31.9721310483743,21.2997177073479,37.9458466540851));
#63807=CARTESIAN_POINT('Ctrl Pts',(31.9736377132647,21.2896303982261,37.9451875779669));
#63808=CARTESIAN_POINT('Ctrl Pts',(31.9763562190106,21.2704224420834,37.9439424680055));
#63809=CARTESIAN_POINT('Ctrl Pts',(31.9775824391884,21.2613042403052,37.9433555991971));
#63810=CARTESIAN_POINT('Ctrl Pts',(31.9807697285647,21.2362947503285,37.9417566159598));
#63811=CARTESIAN_POINT('Ctrl Pts',(31.9826026679967,21.2203874452233,37.9407513806375));
#63812=CARTESIAN_POINT('Ctrl Pts',(31.9895929916324,21.1525474699744,37.9365079480485));
#63813=CARTESIAN_POINT('Ctrl Pts',(31.9929032866454,21.1004411941988,37.9333570623933));
#63814=CARTESIAN_POINT('Ctrl Pts',(31.9976126614615,20.9058471974677,37.9217976483913));
#63815=CARTESIAN_POINT('Ctrl Pts',(31.9857942187847,20.7634708645238,37.9137262535013));
#63816=CARTESIAN_POINT('Ctrl Pts',(31.9456057440939,20.5543376691775,37.9011586157495));
#63817=CARTESIAN_POINT('Ctrl Pts',(31.9286441451956,20.485872675882,37.8969312416665));
#63818=CARTESIAN_POINT('Ctrl Pts',(31.9008105876728,20.3945487784849,37.8910505617771));
#63819=CARTESIAN_POINT('Ctrl Pts',(31.8930766839286,20.370784096324,37.8894977499826));
#63820=CARTESIAN_POINT('Ctrl Pts',(31.8791261173115,20.330504888115,37.8868239520947));
#63821=CARTESIAN_POINT('Ctrl Pts',(31.8731329471791,20.3139157490065,37.8857104300889));
#63822=CARTESIAN_POINT('Ctrl Pts',(31.8605004142059,20.2803486706604,37.8834310845565));
#63823=CARTESIAN_POINT('Ctrl Pts',(31.8538467421039,20.2633779480695,37.8822648680552));
#63824=CARTESIAN_POINT('Ctrl Pts',(31.8363490719971,20.2204879966235,37.8792810703293));
#63825=CARTESIAN_POINT('Ctrl Pts',(31.8251886274952,20.1947030248264,37.8774529567593));
#63826=CARTESIAN_POINT('Ctrl Pts',(31.7678171306725,20.069476825239,37.8684007133234));
#63827=CARTESIAN_POINT('Ctrl Pts',(31.7140116982449,19.9737407123065,37.86091967338));
#63828=CARTESIAN_POINT('Ctrl Pts',(31.6060319032221,19.8139937248266,37.8475324685565));
#63829=CARTESIAN_POINT('Ctrl Pts',(31.5551744072725,19.7480487691076,37.8416984592184));
#63830=CARTESIAN_POINT('Ctrl Pts',(31.4715834960407,19.6526415371946,37.8329204961276));
#63831=CARTESIAN_POINT('Ctrl Pts',(31.441747419404,19.6207619422863,37.8299241654506));
#63832=CARTESIAN_POINT('Ctrl Pts',(31.3902499151999,19.569236201777,37.8250059006833));
#63833=CARTESIAN_POINT('Ctrl Pts',(31.3691599303784,19.5490412948252,37.8230574527094));
#63834=CARTESIAN_POINT('Ctrl Pts',(31.3382173537081,19.5206876698258,37.8203008498271));
#63835=CARTESIAN_POINT('Ctrl Pts',(31.3287187815302,19.5121501834922,37.8194679631413));
#63836=CARTESIAN_POINT('Ctrl Pts',(31.312550186523,19.4978959044242,37.8180734829072));
#63837=CARTESIAN_POINT('Ctrl Pts',(31.3059234640638,19.4921310990031,37.8175084567572));
#63838=CARTESIAN_POINT('Ctrl Pts',(31.2905219130485,19.4789104814704,37.8162103216059));
#63839=CARTESIAN_POINT('Ctrl Pts',(31.2817203256556,19.471486619702,37.8154795030613));
#63840=CARTESIAN_POINT('Ctrl Pts',(31.2562075988905,19.450342780771,37.8133909764482));
#63841=CARTESIAN_POINT('Ctrl Pts',(31.2393365079515,19.4368173053894,37.8120461920918));
#63842=CARTESIAN_POINT('Ctrl Pts',(31.1419843348333,19.3613376659719,37.804468890111));
#63843=CARTESIAN_POINT('Ctrl Pts',(31.0570757537695,19.3053207085734,37.7985533536824));
#63844=CARTESIAN_POINT('Ctrl Pts',(30.8830409175739,19.2086967250122,37.7869975478721));
#63845=CARTESIAN_POINT('Ctrl Pts',(30.7944694110043,19.1676938316014,37.781369560801));
#63846=CARTESIAN_POINT('Ctrl Pts',(30.648207810546,19.1125903719245,37.7720758147644));
#63847=CARTESIAN_POINT('Ctrl Pts',(30.5922694474847,19.0942968647123,37.7685231180385));
#63848=CARTESIAN_POINT('Ctrl Pts',(30.5128886839025,19.0721698642366,37.7634348190275));
#63849=CARTESIAN_POINT('Ctrl Pts',(30.4900596550042,19.0662406315522,37.7619663525104));
#63850=CARTESIAN_POINT('Ctrl Pts',(30.4502088604187,19.0566414278505,37.7593913723901));
#63851=CARTESIAN_POINT('Ctrl Pts',(30.4332339450496,19.0527868951685,37.7582909185817));
#63852=CARTESIAN_POINT('Ctrl Pts',(30.3979441854316,19.045257853421,37.7559946722969));
#63853=CARTESIAN_POINT('Ctrl Pts',(30.379623884991,19.0416174783825,37.7547979053101));
#63854=CARTESIAN_POINT('Ctrl Pts',(30.3314293848595,19.032742543633,37.7516361646813));
#63855=CARTESIAN_POINT('Ctrl Pts',(30.301483171276,19.0279312722926,37.7496580376465));
#63856=CARTESIAN_POINT('Ctrl Pts',(30.1169987027008,19.0025914150675,37.7373828549941));
#63857=CARTESIAN_POINT('Ctrl Pts',(29.9606269134045,18.9995593215533,37.7265351049973));
#63858=CARTESIAN_POINT('Ctrl Pts',(29.74128703512,19.0210452139412,37.7111708313249));
#63859=CARTESIAN_POINT('Ctrl Pts',(29.6773830620616,19.0304534499627,37.706685640414));
#63860=CARTESIAN_POINT('Ctrl Pts',(29.588542986694,19.0479737875423,37.7005203398869));
#63861=CARTESIAN_POINT('Ctrl Pts',(29.5631405151695,19.0535013166384,37.6987658340742));
#63862=CARTESIAN_POINT('Ctrl Pts',(29.518357555042,19.0641669194333,37.695695684531));
#63863=CARTESIAN_POINT('Ctrl Pts',(29.498933064531,19.0691035346013,37.6943717547184));
#63864=CARTESIAN_POINT('Ctrl Pts',(29.4689080016486,19.0772178528433,37.6923407920378));
#63865=CARTESIAN_POINT('Ctrl Pts',(29.4582544697299,19.0801922776979,37.6916232146978));
#63866=CARTESIAN_POINT('Ctrl Pts',(29.4381271741554,19.085992630716,37.6902740386753));
#63867=CARTESIAN_POINT('Ctrl Pts',(29.428648939645,19.0888005725898,37.6896415316996));
#63868=CARTESIAN_POINT('Ctrl Pts',(29.4055321029332,19.095836311611,37.688105141187));
#63869=CARTESIAN_POINT('Ctrl Pts',(29.391917000842,19.1001403928171,37.6872055559768));
#63870=CARTESIAN_POINT('Ctrl Pts',(29.3434392927858,19.1160399772163,37.6840175931844));
#63871=CARTESIAN_POINT('Ctrl Pts',(29.3088502934627,19.1284525695894,37.6817709824414));
#63872=CARTESIAN_POINT('Ctrl Pts',(29.166743197239,19.183926797322,37.6725816596675));
#63873=CARTESIAN_POINT('Ctrl Pts',(29.0627287566824,19.2353568115754,37.6659437315219));
#63874=CARTESIAN_POINT('Ctrl Pts',(28.8874295612915,19.3419306086835,37.654017817658));
#63875=CARTESIAN_POINT('Ctrl Pts',(28.8143087223068,19.3934069218964,37.6487837602794));
#63876=CARTESIAN_POINT('Ctrl Pts',(28.7143644434042,19.474316197793,37.6410069708955));
#63877=CARTESIAN_POINT('Ctrl Pts',(28.6845788958735,19.4999210501602,37.6386021999299));
#63878=CARTESIAN_POINT('Ctrl Pts',(28.6404663197341,19.5401665418745,37.6348912988511));
#63879=CARTESIAN_POINT('Ctrl Pts',(28.6255759991514,19.5541769921639,37.6336113748825));
#63880=CARTESIAN_POINT('Ctrl Pts',(28.5986136220483,19.580339104199,37.6312411722315));
#63881=CARTESIAN_POINT('Ctrl Pts',(28.5864775765877,19.592422233784,37.6301539377632));
#63882=CARTESIAN_POINT('Ctrl Pts',(28.5600325858841,19.6194388449124,37.6277383000814));
#63883=CARTESIAN_POINT('Ctrl Pts',(28.5457974412304,19.6344414617993,37.6264068469774));
#63884=CARTESIAN_POINT('Ctrl Pts',(28.5052203826974,19.6785602722322,37.6225183392841));
#63885=CARTESIAN_POINT('Ctrl Pts',(28.4795028524336,19.708234880024,37.6199357443588));
#63886=CARTESIAN_POINT('Ctrl Pts',(28.3430094690274,19.8754570141499,37.6055517139773));
#63887=CARTESIAN_POINT('Ctrl Pts',(28.2500137321363,20.0264789741271,37.5930720741977));
#63888=CARTESIAN_POINT('Ctrl Pts',(28.1535242688254,20.2428973867132,37.5767024843919));
#63889=CARTESIAN_POINT('Ctrl Pts',(28.1314413967557,20.2991668585337,37.5725806125634));
#63890=CARTESIAN_POINT('Ctrl Pts',(28.1066877680849,20.3717788313914,37.5674989615502));
#63891=CARTESIAN_POINT('Ctrl Pts',(28.1016192791251,20.3872653722515,37.5664285907207));
#63892=CARTESIAN_POINT('Ctrl Pts',(28.0936671755941,20.4126090415539,37.5647006959001));
#63893=CARTESIAN_POINT('Ctrl Pts',(28.0906690032086,20.4224291095546,37.5640369438432));
#63894=CARTESIAN_POINT('Ctrl Pts',(28.085144516901,20.4410370008445,37.5627906628838));
#63895=CARTESIAN_POINT('Ctrl Pts',(28.0826025680451,20.4498198008244,37.5622072057508));
#63896=CARTESIAN_POINT('Ctrl Pts',(28.075859475613,20.4737326177067,37.560630812762));
#63897=CARTESIAN_POINT('Ctrl Pts',(28.0717763477665,20.488895608791,37.5596444211528));
#63898=CARTESIAN_POINT('Ctrl Pts',(28.0557786940539,20.5512264552559,37.5556375483807));
#63899=CARTESIAN_POINT('Ctrl Pts',(28.0454116318397,20.5987777744408,37.5526924761184));
#63900=CARTESIAN_POINT('Ctrl Pts',(28.015908250974,20.7627047278765,37.542773362769));
#63901=CARTESIAN_POINT('Ctrl Pts',(28.0053517652046,20.8803735445233,37.53603925341));
#63902=CARTESIAN_POINT('Ctrl Pts',(28.0051704120784,21.0920338424653,37.5236848978873));
#63903=CARTESIAN_POINT('Ctrl Pts',(28.0116981263056,21.1856559230649,37.5181369904141));
#63904=CARTESIAN_POINT('Ctrl Pts',(28.0286140522835,21.3056441447409,37.5107016416399));
#63905=CARTESIAN_POINT('Ctrl Pts',(28.0330060091454,21.3327392735753,37.509001492195));
#63906=CARTESIAN_POINT('Ctrl Pts',(28.0412195766724,21.3775373118615,37.5061509399333));
#63907=CARTESIAN_POINT('Ctrl Pts',(28.0447257906238,21.395294700256,37.5050106163347));
#63908=CARTESIAN_POINT('Ctrl Pts',(28.0521438325434,21.4303466553135,37.5027378938312));
#63909=CARTESIAN_POINT('Ctrl Pts',(28.0560455760191,21.4476416611827,37.5016059131602));
#63910=CARTESIAN_POINT('Ctrl Pts',(28.0661199464601,21.4896792036977,37.4988275782407));
#63911=CARTESIAN_POINT('Ctrl Pts',(28.0725373569274,21.5143592553,37.4971734902399));
#63912=CARTESIAN_POINT('Ctrl Pts',(28.0998188235944,21.6115855383253,37.4905629932941));
#63913=CARTESIAN_POINT('Ctrl Pts',(28.1243182002619,21.6830379331354,37.4854919333402));
#63914=CARTESIAN_POINT('Ctrl Pts',(28.2194466528817,21.9164226484134,37.4682375698175));
#63915=CARTESIAN_POINT('Ctrl Pts',(28.3074946182132,22.0703372899519,37.4556272724443));
#63916=CARTESIAN_POINT('Ctrl Pts',(28.4284591182776,22.2287412040328,37.4422800204101));
#63917=CARTESIAN_POINT('Ctrl Pts',(28.4425833904532,22.2465950818086,37.440771077684));
#63918=CARTESIAN_POINT('Ctrl Pts',(28.4643684060945,22.2731841754553,37.4385217344837));
#63919=CARTESIAN_POINT('Ctrl Pts',(28.4718044159157,22.2821000778645,37.4377671109173));
#63920=CARTESIAN_POINT('Ctrl Pts',(28.4855675982577,22.2983124870437,37.4363950492201));
#63921=CARTESIAN_POINT('Ctrl Pts',(28.4918702711509,22.3056284079557,37.4357760355773));
#63922=CARTESIAN_POINT('Ctrl Pts',(28.5069121987213,22.322834283231,37.4343201382086));
#63923=CARTESIAN_POINT('Ctrl Pts',(28.5156968254845,22.3326836953688,37.4334865666578));
#63924=CARTESIAN_POINT('Ctrl Pts',(28.5460175038624,22.3660077819022,37.4306628171376));
#63925=CARTESIAN_POINT('Ctrl Pts',(28.5680188889317,22.3890546108835,37.4287039139942));
#63926=CARTESIAN_POINT('Ctrl Pts',(28.6256625093559,22.4466112426413,37.4237651933596));
#63927=CARTESIAN_POINT('Ctrl Pts',(28.6620578499049,22.4803374672231,37.4208258430704));
#63928=CARTESIAN_POINT('Ctrl Pts',(28.8013481942874,22.6000743104362,37.4100541646177));
#63929=CARTESIAN_POINT('Ctrl Pts',(28.9115212273816,22.6769563946035,37.4024218142213));
#63930=CARTESIAN_POINT('Ctrl Pts',(29.0285070711969,22.7421908769666,37.3944594262182));
#63931=CARTESIAN_POINT('',(28.0052505873043,21.0015307025596,37.3704548813502));
#63932=CARTESIAN_POINT('Ctrl Pts',(29.0285070491141,22.7421908646526,37.2352940441794));
#63933=CARTESIAN_POINT('Ctrl Pts',(28.9676750007528,22.7082692620487,37.2397348558595));
#63934=CARTESIAN_POINT('Ctrl Pts',(28.9085669082878,22.6711271905714,37.2441756675396));
#63935=CARTESIAN_POINT('Ctrl Pts',(28.8515391222872,22.6309706235439,37.2486164792197));
#63936=CARTESIAN_POINT('Ctrl Pts',(28.7945363606911,22.5908316776489,37.2530553422239));
#63937=CARTESIAN_POINT('Ctrl Pts',(28.7396124938189,22.5476811426052,37.2574942052282));
#63938=CARTESIAN_POINT('Ctrl Pts',(28.6870952912065,22.5017685534489,37.2619330682325));
#63939=CARTESIAN_POINT('Ctrl Pts',(28.6345832990225,22.4558605194525,37.2663714908405));
#63940=CARTESIAN_POINT('Ctrl Pts',(28.5844778645941,22.4071912985624,37.2708099134485));
#63941=CARTESIAN_POINT('Ctrl Pts',(28.5370726524019,22.3560498287856,37.2752483360566));
#63942=CARTESIAN_POINT('Ctrl Pts',(28.4896219666951,22.304859301484,37.2796910162275));
#63943=CARTESIAN_POINT('Ctrl Pts',(28.4448770119837,22.2511921468912,37.2841336963985));
#63944=CARTESIAN_POINT('Ctrl Pts',(28.4030929756531,22.1953725436413,37.2885763765695));
#63945=CARTESIAN_POINT('Ctrl Pts',(28.3612901010681,22.139527774228,37.2930210597145));
#63946=CARTESIAN_POINT('Ctrl Pts',(28.3224510779613,22.0815290297261,37.2974657428595));
#63947=CARTESIAN_POINT('Ctrl Pts',(28.2867876795183,22.0217294688173,37.3019104260045));
#63948=CARTESIAN_POINT('Ctrl Pts',(28.251057438419,21.9618178276898,37.3063634396632));
#63949=CARTESIAN_POINT('Ctrl Pts',(28.2185149452665,21.9000990595722,37.3108164533218));
#63950=CARTESIAN_POINT('Ctrl Pts',(28.189325692928,21.8369504861156,37.3152694669805));
#63951=CARTESIAN_POINT('Ctrl Pts',(28.1613490372183,21.7764252668444,37.3195374909968));
#63952=CARTESIAN_POINT('Ctrl Pts',(28.1364526001043,21.7145870758048,37.3238055150131));
#63953=CARTESIAN_POINT('Ctrl Pts',(28.1147390994969,21.6517813280038,37.3280735390294));
#63954=CARTESIAN_POINT('Ctrl Pts',(28.0881391268734,21.5748415842784,37.3333020521118));
#63955=CARTESIAN_POINT('Ctrl Pts',(28.0662290812613,21.4962022913531,37.3385305651942));
#63956=CARTESIAN_POINT('Ctrl Pts',(28.0491946728556,21.4163966115195,37.3437590782766));
#63957=CARTESIAN_POINT('Ctrl Pts',(28.0323305966141,21.3373889326406,37.3489353098868));
#63958=CARTESIAN_POINT('Ctrl Pts',(28.0202452166158,21.2572382007314,37.354111541497));
#63959=CARTESIAN_POINT('Ctrl Pts',(28.0130723499623,21.1764825090925,37.3592877731071));
#63960=CARTESIAN_POINT('Ctrl Pts',(28.0079141457985,21.1184088873482,37.3630101425215));
#63961=CARTESIAN_POINT('Ctrl Pts',(28.0052954721807,21.0600228505839,37.3667325119358));
#63962=CARTESIAN_POINT('Ctrl Pts',(28.0052505873043,21.0015307025596,37.3704548813502));
#63963=CARTESIAN_POINT('Ctrl Pts',(28.0052505873038,21.0015307018519,37.3704548813952));
#63964=CARTESIAN_POINT('Ctrl Pts',(28.0051970875676,20.9318119861274,37.3748916959726));
#63965=CARTESIAN_POINT('Ctrl Pts',(28.0088030231443,20.8620506010969,37.37932851055));
#63966=CARTESIAN_POINT('Ctrl Pts',(28.0160551888972,20.7926583761076,37.3837653251274));
#63967=CARTESIAN_POINT('Ctrl Pts',(28.0233061729072,20.7232774586061,37.3882014167242));
#63968=CARTESIAN_POINT('Ctrl Pts',(28.0342021560973,20.6542660682087,37.3926375083211));
#63969=CARTESIAN_POINT('Ctrl Pts',(28.0486780446787,20.5860311736604,37.397073599918));
#63970=CARTESIAN_POINT('Ctrl Pts',(28.0631564854405,20.5177842489169,37.4015104736227));
#63971=CARTESIAN_POINT('Ctrl Pts',(28.0812159804205,20.4503145698138,37.4059473473275));
#63972=CARTESIAN_POINT('Ctrl Pts',(28.1027406541306,20.3840174215034,37.4103842210322));
#63973=CARTESIAN_POINT('Ctrl Pts',(28.1242909534436,20.3176413449629,37.4148263769338));
#63974=CARTESIAN_POINT('Ctrl Pts',(28.149314510197,20.2524410501686,37.4192685328354));
#63975=CARTESIAN_POINT('Ctrl Pts',(28.1776463422157,20.1887942872118,37.423710688737));
#63976=CARTESIAN_POINT('Ctrl Pts',(28.2059978569738,20.1251033074656,37.4281559307008));
#63977=CARTESIAN_POINT('Ctrl Pts',(28.2376619969177,20.062968442017,37.4326011726647));
#63978=CARTESIAN_POINT('Ctrl Pts',(28.2724279088081,20.0027426449331,37.4370464146285));
#63979=CARTESIAN_POINT('Ctrl Pts',(28.3072551088155,19.9424106770199,37.4414994930187));
#63980=CARTESIAN_POINT('Ctrl Pts',(28.3451947235225,19.88399490096,37.445952571409));
#63981=CARTESIAN_POINT('Ctrl Pts',(28.3859932468674,19.8278183744222,37.4504056497992));
#63982=CARTESIAN_POINT('Ctrl Pts',(28.4000373498548,19.8084806911069,37.4519385359528));
#63983=CARTESIAN_POINT('Ctrl Pts',(28.4144198789395,19.7894080447954,37.4534714221064));
#63984=CARTESIAN_POINT('Ctrl Pts',(28.4291294646721,19.7706126225886,37.4550043082601));
#63985=CARTESIAN_POINT('Ctrl Pts',(28.4718807834891,19.7159864011795,37.4594594238463));
#63986=CARTESIAN_POINT('Ctrl Pts',(28.5175690562093,19.6634852813327,37.4639145394325));
#63987=CARTESIAN_POINT('Ctrl Pts',(28.565955127025,19.6134420802599,37.4683696550187));
#63988=CARTESIAN_POINT('Ctrl Pts',(28.6142687478787,19.5634738104215,37.4728180998224));
#63989=CARTESIAN_POINT('Ctrl Pts',(28.6652718119006,19.5159565035892,37.4772665446261));
#63990=CARTESIAN_POINT('Ctrl Pts',(28.7186843478964,19.4711907371506,37.4817149894298));
#63991=CARTESIAN_POINT('Ctrl Pts',(28.7720342547224,19.4264774610633,37.4861582181845));
#63992=CARTESIAN_POINT('Ctrl Pts',(28.8277876489463,19.3845096301406,37.4906014469392));
#63993=CARTESIAN_POINT('Ctrl Pts',(28.8856283642533,19.3455504178298,37.4950446756939));
#63994=CARTESIAN_POINT('Ctrl Pts',(28.943432830965,19.3066156211354,37.4994851198911));
#63995=CARTESIAN_POINT('Ctrl Pts',(29.0033216188074,19.2706859752787,37.5039255640882));
#63996=CARTESIAN_POINT('Ctrl Pts',(29.0649474143262,19.2379829102631,37.5083660082854));
#63997=CARTESIAN_POINT('Ctrl Pts',(29.1265555001082,19.2052892433036,37.5128051764082));
#63998=CARTESIAN_POINT('Ctrl Pts',(29.1898991706166,19.1758205456311,37.5172443445309));
#63999=CARTESIAN_POINT('Ctrl Pts',(29.2546057525191,19.1497527250872,37.5216835126537));
#64000=CARTESIAN_POINT('Ctrl Pts',(29.319315694997,19.1236835506953,37.5261229113274));
#64001=CARTESIAN_POINT('Ctrl Pts',(29.3853882346695,19.1010157846872,37.5305623100011));
#64002=CARTESIAN_POINT('Ctrl Pts',(29.4524315863539,19.081876856175,37.5350017086747));
#64003=CARTESIAN_POINT('Ctrl Pts',(29.5195458045972,19.0627176973197,37.5394457999077));
#64004=CARTESIAN_POINT('Ctrl Pts',(29.587632411586,19.0470949553679,37.5438898911408));
#64005=CARTESIAN_POINT('Ctrl Pts',(29.6562862907838,19.0350856383555,37.5483339823738));
#64006=CARTESIAN_POINT('Ctrl Pts',(29.7249803935313,19.0230692852169,37.5527806773508));
#64007=CARTESIAN_POINT('Ctrl Pts',(29.7942419441702,19.0146706297299,37.5572273723278));
#64008=CARTESIAN_POINT('Ctrl Pts',(29.8636602826768,19.0099148148935,37.5616740673048));
#64009=CARTESIAN_POINT('Ctrl Pts',(29.9331988788893,19.0051507612633,37.5661284655681));
#64010=CARTESIAN_POINT('Ctrl Pts',(30.0028943160324,19.0040421529423,37.5705828638314));
#64011=CARTESIAN_POINT('Ctrl Pts',(30.0723363214446,19.0065620102196,37.5750372620947));
#64012=CARTESIAN_POINT('Ctrl Pts',(30.1081809036425,19.0078627104336,37.5773365338934));
#64013=CARTESIAN_POINT('Ctrl Pts',(30.1439580479989,19.010129337037,37.5796358056922));
#64014=CARTESIAN_POINT('Ctrl Pts',(30.1796122418824,19.0133528232054,37.5819350774909));
#64015=CARTESIAN_POINT('Ctrl Pts',(30.2486942549679,19.0195985096005,37.5863900463791));
#64016=CARTESIAN_POINT('Ctrl Pts',(30.3175862033279,19.02946409394,37.5908450152674));
#64017=CARTESIAN_POINT('Ctrl Pts',(30.3858787744911,19.0429294509657,37.5952999841557));
#64018=CARTESIAN_POINT('Ctrl Pts',(30.4540690398109,19.0563746361824,37.5997482792675));
#64019=CARTESIAN_POINT('Ctrl Pts',(30.5216612338784,19.073408796921,37.6041965743794));
#64020=CARTESIAN_POINT('Ctrl Pts',(30.5882509561794,19.0939600279495,37.6086448694913));
#64021=CARTESIAN_POINT('Ctrl Pts',(30.6547625402009,19.1144871435775,37.6130879448468));
#64022=CARTESIAN_POINT('Ctrl Pts',(30.7202735235098,19.1385229889579,37.6175310202023));
#64023=CARTESIAN_POINT('Ctrl Pts',(30.7843912635446,19.1659449549768,37.6219740955578));
#64024=CARTESIAN_POINT('Ctrl Pts',(30.8484687879124,19.1933497215023,37.6264143841457));
#64025=CARTESIAN_POINT('Ctrl Pts',(30.9111543537307,19.2241362034049,37.6308546727336));
#64026=CARTESIAN_POINT('Ctrl Pts',(30.9720734615318,19.2581329706646,37.6352949613216));
#64027=CARTESIAN_POINT('Ctrl Pts',(31.0329750349667,19.292119952624,37.6397339718598));
#64028=CARTESIAN_POINT('Ctrl Pts',(31.0921107326892,19.3293151472234,37.6441729823981));
#64029=CARTESIAN_POINT('Ctrl Pts',(31.1491305142306,19.3695011120015,37.6486119929363));
#64030=CARTESIAN_POINT('Ctrl Pts',(31.2061532348479,19.4096891481592,37.6530512322827));
#64031=CARTESIAN_POINT('Ctrl Pts',(31.2610594241858,19.4528679767003,37.6574904716291));
#64032=CARTESIAN_POINT('Ctrl Pts',(31.3135293763748,19.4987777846367,37.6619297109755));
#64033=CARTESIAN_POINT('Ctrl Pts',(31.3660547742256,19.5447361060475,37.6663736413222));
#64034=CARTESIAN_POINT('Ctrl Pts',(31.4161384277138,19.5934308438923,37.670817571669));
#64035=CARTESIAN_POINT('Ctrl Pts',(31.4634957355631,19.6445636147393,37.6752615020157));
#64036=CARTESIAN_POINT('Ctrl Pts',(31.5108807785624,19.6957263318635,37.6797080349824));
#64037=CARTESIAN_POINT('Ctrl Pts',(31.5555359845813,19.7493295479291,37.6841545679491));
#64038=CARTESIAN_POINT('Ctrl Pts',(31.597217298084,19.8050420655098,37.6886011009158));
#64039=CARTESIAN_POINT('Ctrl Pts',(31.6389708210197,19.8608511004255,37.6930553371335));
#64040=CARTESIAN_POINT('Ctrl Pts',(31.6777398953439,19.9187763244634,37.6975095733513));
#64041=CARTESIAN_POINT('Ctrl Pts',(31.7133244478229,19.9784585671681,37.7019638095691));
#64042=CARTESIAN_POINT('Ctrl Pts',(31.7317043968018,20.0092853304526,37.70426448862));
#64043=CARTESIAN_POINT('Ctrl Pts',(31.7492355156924,20.0405804562712,37.7065651676708));
#64044=CARTESIAN_POINT('Ctrl Pts',(31.7658952391199,20.0722923052202,37.7088658467217));
#64045=CARTESIAN_POINT('Ctrl Pts',(31.7981553081255,20.1336994732228,37.7133209065709));
#64046=CARTESIAN_POINT('Ctrl Pts',(31.8272720354534,20.1969122905168,37.71777596642));
#64047=CARTESIAN_POINT('Ctrl Pts',(31.8530401133341,20.2615760696764,37.7222310262692));
#64048=CARTESIAN_POINT('Ctrl Pts',(31.8787695978004,20.326143000478,37.7266794136777));
#64049=CARTESIAN_POINT('Ctrl Pts',(31.9011602075757,20.3921561290545,37.7311278010862));
#64050=CARTESIAN_POINT('Ctrl Pts',(31.9200527874283,20.4592367838055,37.7355761884947));
#64051=CARTESIAN_POINT('Ctrl Pts',(31.9389232051245,20.5262387488294,37.7400193576716));
#64052=CARTESIAN_POINT('Ctrl Pts',(31.9543036108986,20.5943052840939,37.7444625268485));
#64053=CARTESIAN_POINT('Ctrl Pts',(31.9660838146113,20.6630400670353,37.7489056960254));
#64054=CARTESIAN_POINT('Ctrl Pts',(31.9778566321101,20.7317317531155,37.7533460793254));
#64055=CARTESIAN_POINT('Ctrl Pts',(31.9860336432338,20.8010903745115,37.7577864626254));
#64056=CARTESIAN_POINT('Ctrl Pts',(31.9905555078152,20.8707083420851,37.7622268459254));
#64057=CARTESIAN_POINT('Ctrl Pts',(31.9950760716551,20.9403062836303,37.7666659519224));
#64058=CARTESIAN_POINT('Ctrl Pts',(31.9959435445788,21.0101629352344,37.7711050579193));
#64059=CARTESIAN_POINT('Ctrl Pts',(31.9931505064754,21.0798662697074,37.7755441639163));
#64060=CARTESIAN_POINT('Ctrl Pts',(31.9903573240286,21.1495732064262,37.7799834993248));
#64061=CARTESIAN_POINT('Ctrl Pts',(31.9839032769814,21.2191263214869,37.7844228347333));
#64062=CARTESIAN_POINT('Ctrl Pts',(31.9738329964775,21.2881160608448,37.7888621701419));
#64063=CARTESIAN_POINT('Ctrl Pts',(31.9637520742299,21.3571787049365,37.7933061968069));
#64064=CARTESIAN_POINT('Ctrl Pts',(31.9500473621252,21.4256762999692,37.797750223472));
#64065=CARTESIAN_POINT('Ctrl Pts',(31.9328149407851,21.4932078336542,37.802194250137));
#64066=CARTESIAN_POINT('Ctrl Pts',(31.9155724262556,21.5607789211862,37.8066408797098));
#64067=CARTESIAN_POINT('Ctrl Pts',(31.8947982356396,21.6273823539259,37.8110875092826));
#64068=CARTESIAN_POINT('Ctrl Pts',(31.8706380187518,21.6926333556077,37.8155341388554));
#64069=CARTESIAN_POINT('Ctrl Pts',(31.8464359503377,21.7579973883117,37.8199884711005));
#64070=CARTESIAN_POINT('Ctrl Pts',(31.818836341289,21.8220038643766,37.8244428033456));
#64071=CARTESIAN_POINT('Ctrl Pts',(31.7880322108752,21.8842897575867,37.8288971355908));
#64072=CARTESIAN_POINT('Ctrl Pts',(31.7721276576484,21.916448734014,37.831196962378));
#64073=CARTESIAN_POINT('Ctrl Pts',(31.755369586707,21.9481494680602,37.8334967891652));
#64074=CARTESIAN_POINT('Ctrl Pts',(31.737789077975,21.9793450275418,37.8357966159524));
#64075=CARTESIAN_POINT('Ctrl Pts',(31.7037334727485,22.0397746587157,37.8402516629791));
#64076=CARTESIAN_POINT('Ctrl Pts',(31.6664549874929,22.0985448139774,37.8447067100058));
#64077=CARTESIAN_POINT('Ctrl Pts',(31.6261400249968,22.1552905182695,37.8491617570326));
#64078=CARTESIAN_POINT('Ctrl Pts',(31.5858854431001,22.2119512332815,37.8536101316381));
#64079=CARTESIAN_POINT('Ctrl Pts',(31.5426036914941,22.2665931196839,37.8580585062436));
#64080=CARTESIAN_POINT('Ctrl Pts',(31.4965263710486,22.3188769401488,37.8625068808491));
#64081=CARTESIAN_POINT('Ctrl Pts',(31.4505031013113,22.37109942941,37.8669500373171));
#64082=CARTESIAN_POINT('Ctrl Pts',(31.4016910979545,22.4209689813424,37.871393193785));
#64083=CARTESIAN_POINT('Ctrl Pts',(31.3503633682412,22.4681778966502,37.8758363502529));
#64084=CARTESIAN_POINT('Ctrl Pts',(31.2990678204587,22.5153572124793,37.8802767209098));
#64085=CARTESIAN_POINT('Ctrl Pts',(31.2452600347722,22.5598788706026,37.8847170915668));
#64086=CARTESIAN_POINT('Ctrl Pts',(31.1892500865086,22.6014717588017,37.8891574622237));
#64087=CARTESIAN_POINT('Ctrl Pts',(31.1332562488101,22.6430526833237,37.8935965556632));
#64088=CARTESIAN_POINT('Ctrl Pts',(31.0750618986584,22.6817062187649,37.8980356491027));
#64089=CARTESIAN_POINT('Ctrl Pts',(31.0150090257792,22.7172024458656,37.9024747425423));
#64090=CARTESIAN_POINT('Ctrl Pts',(30.954953047952,22.752700508248,37.9069140654988));
#64091=CARTESIAN_POINT('Ctrl Pts',(30.8930387790592,22.7850406913028,37.9113533884553));
#64092=CARTESIAN_POINT('Ctrl Pts',(30.8296343904043,22.8140381310101,37.9157927114118));
#64093=CARTESIAN_POINT('Ctrl Pts',(30.7661629955968,22.8430662153921,37.9202367258724));
#64094=CARTESIAN_POINT('Ctrl Pts',(30.7011987837915,22.8687443017592,37.9246807403331));
#64095=CARTESIAN_POINT('Ctrl Pts',(30.6351306847448,22.8909353706025,37.9291247547937));
#64096=CARTESIAN_POINT('Ctrl Pts',(30.5690238870659,22.9131394376102,37.9335713722849));
#64097=CARTESIAN_POINT('Ctrl Pts',(30.5018123866641,22.931852290481,37.9380179897762));
#64098=CARTESIAN_POINT('Ctrl Pts',(30.4338983892305,22.9469873523788,37.9424646072674));
#64099=CARTESIAN_POINT('Ctrl Pts',(30.3658667425723,22.9621486331471,37.9469189277524));
#64100=CARTESIAN_POINT('Ctrl Pts',(30.2971306521092,22.9737196700521,37.9513732482374));
#64101=CARTESIAN_POINT('Ctrl Pts',(30.2280997745616,22.9816654751357,37.9558275687223));
#64102=CARTESIAN_POINT('Ctrl Pts',(30.1924564490298,22.9857682031796,37.9581275075426));
#64103=CARTESIAN_POINT('Ctrl Pts',(30.1567345731691,22.9889052759571,37.9604274463629));
#64104=CARTESIAN_POINT('Ctrl Pts',(30.1209904421614,22.9910773152757,37.9627273851832));
#64105=CARTESIAN_POINT('Ctrl Pts',(30.0517594247995,22.9952842294611,37.9671820215084));
#64106=CARTESIAN_POINT('Ctrl Pts',(29.9821723908552,22.99588431811,37.9716366578335));
#64107=CARTESIAN_POINT('Ctrl Pts',(29.9126369316935,22.9928359834156,37.9760912941587));
#64108=CARTESIAN_POINT('Ctrl Pts',(29.8432006204944,22.9897919952256,37.9805395787876));
#64109=CARTESIAN_POINT('Ctrl Pts',(29.7738162228982,22.9831099262811,37.9849878634165));
#64110=CARTESIAN_POINT('Ctrl Pts',(29.7048943424097,22.9728000946265,37.9894361480454));
#64111=CARTESIAN_POINT('Ctrl Pts',(29.6360532006688,22.9625023404556,37.9938792217177));
#64112=CARTESIAN_POINT('Ctrl Pts',(29.5676739814763,22.9485853362069,37.99832229539));
#64113=CARTESIAN_POINT('Ctrl Pts',(29.5001632856801,22.9311112918519,38.0027653690623));
#64114=CARTESIAN_POINT('Ctrl Pts',(29.4326984427486,22.9136491157643,38.0072054250252));
#64115=CARTESIAN_POINT('Ctrl Pts',(29.3661014246855,22.8926348178249,38.0116454809882));
#64116=CARTESIAN_POINT('Ctrl Pts',(29.30076817101,22.868181578923,38.0160855369512));
#64117=CARTESIAN_POINT('Ctrl Pts',(29.2354480376213,22.8437332507441,38.0205247012578));
#64118=CARTESIAN_POINT('Ctrl Pts',(29.1713916246071,22.8158475190688,38.0249638655645));
#64119=CARTESIAN_POINT('Ctrl Pts',(29.1089777080109,22.7846867617816,38.0294030298711));
#64120=CARTESIAN_POINT('Ctrl Pts',(29.08183381087,22.7711349060936,38.0313336284604));
#64121=CARTESIAN_POINT('Ctrl Pts',(29.0550003164454,22.7569642301779,38.0332642270497));
#64122=CARTESIAN_POINT('Ctrl Pts',(29.0285070491141,22.7421908646526,38.0351948256389));
#64123=CARTESIAN_POINT('Origin',(30.,21.,34.5704548813952));
#64124=CARTESIAN_POINT('',(29.0285070786203,22.742190881106,38.9934724864331));
#64125=CARTESIAN_POINT('',(29.0285070491141,22.7421908646526,38.8351573073316));
#64126=CARTESIAN_POINT('',(29.0285070491141,22.7421908646526,34.5704548813952));
#64127=CARTESIAN_POINT('',(28.0052500005311,20.9999539693013,38.3266423355102));
#64128=CARTESIAN_POINT('Ctrl Pts',(29.0285070786203,22.742190881106,38.9934724864331));
#64129=CARTESIAN_POINT('Ctrl Pts',(29.1261719400268,22.7966514586196,38.9856837164118));
#64130=CARTESIAN_POINT('Ctrl Pts',(29.2282644481304,22.8428150981434,38.9778312441651));
#64131=CARTESIAN_POINT('Ctrl Pts',(29.3602290880631,22.8895798912096,38.9683904123005));
#64132=CARTESIAN_POINT('Ctrl Pts',(29.3869429891265,22.8984152003077,38.9665147657409));
#64133=CARTESIAN_POINT('Ctrl Pts',(29.4257458574274,22.9103442054419,38.963849789298));
#64134=CARTESIAN_POINT('Ctrl Pts',(29.4376897690429,22.9138939435479,38.9630375166519));
#64135=CARTESIAN_POINT('Ctrl Pts',(29.4589957458048,22.9200094177528,38.9616037720753));
#64136=CARTESIAN_POINT('Ctrl Pts',(29.4683443248162,22.9226190528019,38.9609799194553));
#64137=CARTESIAN_POINT('Ctrl Pts',(29.4893403217739,22.9283151765138,38.9595905535825));
#64138=CARTESIAN_POINT('Ctrl Pts',(29.5009971120419,22.9313645078824,38.9588271207487));
#64139=CARTESIAN_POINT('Ctrl Pts',(29.5369928297828,22.9404330688693,38.9564920138923));
#64140=CARTESIAN_POINT('Ctrl Pts',(29.5614191016366,22.9460994483439,38.9549387609837));
#64141=CARTESIAN_POINT('Ctrl Pts',(29.6203867865655,22.9586119770588,38.9512497979312));
#64142=CARTESIAN_POINT('Ctrl Pts',(29.6550159104204,22.9650072034573,38.9491330140999));
#64143=CARTESIAN_POINT('Ctrl Pts',(29.8039952556494,22.9884601893047,38.9401692216269));
#64144=CARTESIAN_POINT('Ctrl Pts',(29.9195438375984,22.9964771930964,38.9335633735301));
#64145=CARTESIAN_POINT('Ctrl Pts',(30.1283304682209,22.9927984988894,38.9213727239291));
#64146=CARTESIAN_POINT('Ctrl Pts',(30.221280588503,22.9846275855641,38.9158552584771));
#64147=CARTESIAN_POINT('Ctrl Pts',(30.3403974775534,22.9656828965603,38.9084540736092));
#64148=CARTESIAN_POINT('Ctrl Pts',(30.3673892531734,22.9608173590714,38.9067552395224));
#64149=CARTESIAN_POINT('Ctrl Pts',(30.4120098705479,22.9518204024578,38.9039062719728));
#64150=CARTESIAN_POINT('Ctrl Pts',(30.4296985932853,22.9480025926766,38.902766193145));
#64151=CARTESIAN_POINT('Ctrl Pts',(30.4646137380158,22.939968065006,38.9004934764392));
#64152=CARTESIAN_POINT('Ctrl Pts',(30.4818407297721,22.935761218852,38.899361250248));
#64153=CARTESIAN_POINT('Ctrl Pts',(30.5237157697067,22.9249416967329,38.8965814295517));
#64154=CARTESIAN_POINT('Ctrl Pts',(30.5482968634414,22.9180847719852,38.8949260820902));
#64155=CARTESIAN_POINT('Ctrl Pts',(30.645229076629,22.8890299042917,38.8883015259722));
#64156=CARTESIAN_POINT('Ctrl Pts',(30.7164157546297,22.8631963526262,38.8832170273903));
#64157=CARTESIAN_POINT('Ctrl Pts',(30.9430063740048,22.7660588994322,38.8663369730759));
#64158=CARTESIAN_POINT('Ctrl Pts',(31.0907425043475,22.6788393435921,38.854152321631));
#64159=CARTESIAN_POINT('Ctrl Pts',(31.2462669994359,22.5577340755355,38.8408904933856));
#64160=CARTESIAN_POINT('Ctrl Pts',(31.2666629325392,22.5411950083032,38.8391433092643));
#64161=CARTESIAN_POINT('Ctrl Pts',(31.2960986777053,22.5163463262876,38.8366169998726));
#64162=CARTESIAN_POINT('Ctrl Pts',(31.3053970191235,22.508348966498,38.8358182611524));
#64163=CARTESIAN_POINT('Ctrl Pts',(31.3219161645369,22.4938739209478,38.8343988858292));
#64164=CARTESIAN_POINT('Ctrl Pts',(31.3291641727891,22.4874287374167,38.8337760659393));
#64165=CARTESIAN_POINT('Ctrl Pts',(31.3455957223273,22.4726011988472,38.8323638651608));
#64166=CARTESIAN_POINT('Ctrl Pts',(31.3547482732204,22.4641855326901,38.8315769593707));
#64167=CARTESIAN_POINT('Ctrl Pts',(31.3836785814484,22.4370809070461,38.829086368869));
#64168=CARTESIAN_POINT('Ctrl Pts',(31.4031537338011,22.4180718302162,38.827404820595));
#64169=CARTESIAN_POINT('Ctrl Pts',(31.4499145161824,22.3705231906095,38.8233364773896));
#64170=CARTESIAN_POINT('Ctrl Pts',(31.4767541071958,22.3415601268839,38.8209742265413));
#64171=CARTESIAN_POINT('Ctrl Pts',(31.6050803646051,22.1945594420947,38.8094310299026));
#64172=CARTESIAN_POINT('Ctrl Pts',(31.6933668120287,22.0657237407482,38.8006371880744));
#64173=CARTESIAN_POINT('Ctrl Pts',(31.7911444298746,21.8796604628152,38.7881094478695));
#64174=CARTESIAN_POINT('Ctrl Pts',(31.8145185199592,21.8303750261141,38.784810838852));
#64175=CARTESIAN_POINT('Ctrl Pts',(31.8441510696838,21.7606481263319,38.7801328320607));
#64176=CARTESIAN_POINT('Ctrl Pts',(31.8521458990659,21.7409684572614,38.7788114243597));
#64177=CARTESIAN_POINT('Ctrl Pts',(31.8661548937171,21.704840444289,38.7763814842166));
#64178=CARTESIAN_POINT('Ctrl Pts',(31.8722696853947,21.6884332449827,38.7752764385417));
#64179=CARTESIAN_POINT('Ctrl Pts',(31.8842717352779,21.6548862181166,38.7730128999078));
#64180=CARTESIAN_POINT('Ctrl Pts',(31.8901429752788,21.6377424466212,38.7718539970609));
#64181=CARTESIAN_POINT('Ctrl Pts',(31.9043509182818,21.5943352017041,38.7689132355796));
#64182=CARTESIAN_POINT('Ctrl Pts',(31.9123782926977,21.5679752561361,38.767121449598));
#64183=CARTESIAN_POINT('Ctrl Pts',(31.9482511970124,21.4407802223936,38.7584430581908));
#64184=CARTESIAN_POINT('Ctrl Pts',(31.9686781336224,21.3380392717237,38.7513237551309));
#64185=CARTESIAN_POINT('Ctrl Pts',(31.9980312035058,21.0897428861422,38.7339927097622));
#64186=CARTESIAN_POINT('Ctrl Pts',(31.9992584473795,20.9438644916594,38.7236945439104));
#64187=CARTESIAN_POINT('Ctrl Pts',(31.98250342374,20.7783103372444,38.7125770837495));
#64188=CARTESIAN_POINT('Ctrl Pts',(31.9800666540482,20.7575082274679,38.7111913246484));
#64189=CARTESIAN_POINT('Ctrl Pts',(31.9758020570041,20.7254766387862,38.7090786282242));
#64190=CARTESIAN_POINT('Ctrl Pts',(31.9742051154172,20.7142185770148,38.708340130257));
#64191=CARTESIAN_POINT('Ctrl Pts',(31.9710534470934,20.6932887154148,38.7069754998225));
#64192=CARTESIAN_POINT('Ctrl Pts',(31.9695236892128,20.683614246275,38.7063481313656));
#64193=CARTESIAN_POINT('Ctrl Pts',(31.9656907574216,20.6604799650858,38.7048555578994));
#64194=CARTESIAN_POINT('Ctrl Pts',(31.9633205472482,20.647031925721,38.7039940500255));
#64195=CARTESIAN_POINT('Ctrl Pts',(31.9543948070726,20.5992641201194,38.7009523909232));
#64196=CARTESIAN_POINT('Ctrl Pts',(31.9470755800144,20.5650915952059,38.6988103836295));
#64197=CARTESIAN_POINT('Ctrl Pts',(31.925449041231,20.4756625738358,38.6932527917642));
#64198=CARTESIAN_POINT('Ctrl Pts',(31.9096615288459,20.4207958986623,38.6898916058998));
#64199=CARTESIAN_POINT('Ctrl Pts',(31.8450906662349,20.227941958694,38.6780186853723));
#64200=CARTESIAN_POINT('Ctrl Pts',(31.7835203951718,20.0947450518531,38.6696736552688));
#64201=CARTESIAN_POINT('Ctrl Pts',(31.6859945508057,19.9331100106157,38.658293652308));
#64202=CARTESIAN_POINT('Ctrl Pts',(31.662895341532,19.8974526900899,38.6556992826264));
#64203=CARTESIAN_POINT('Ctrl Pts',(31.6266835933433,19.8452834013188,38.6517580681359));
#64204=CARTESIAN_POINT('Ctrl Pts',(31.6144182797286,19.8281964751232,38.6504428912696));
#64205=CARTESIAN_POINT('Ctrl Pts',(31.5916747503448,19.7975472375871,38.6480373200431));
#64206=CARTESIAN_POINT('Ctrl Pts',(31.5812874656464,19.7839197897455,38.646950535793));
#64207=CARTESIAN_POINT('Ctrl Pts',(31.5583179049367,19.7545771439819,38.6445717443706));
#64208=CARTESIAN_POINT('Ctrl Pts',(31.5456708000475,19.7389153431565,38.6432772203316));
#64209=CARTESIAN_POINT('Ctrl Pts',(31.5087166554658,19.6945435369297,38.6395361472075));
#64210=CARTESIAN_POINT('Ctrl Pts',(31.4838327720682,19.6663274343909,38.6370663980428));
#64211=CARTESIAN_POINT('Ctrl Pts',(31.3841324134644,19.5595221473438,38.6273518474158));
#64212=CARTESIAN_POINT('Ctrl Pts',(31.3037597022464,19.4863937264061,38.6198826459773));
#64213=CARTESIAN_POINT('Ctrl Pts',(31.1196987106189,19.344505669233,38.6036959190505));
#64214=CARTESIAN_POINT('Ctrl Pts',(31.0147014430383,19.2781487132412,38.5949847780099));
#64215=CARTESIAN_POINT('Ctrl Pts',(30.8860615123536,19.2127290350888,38.5853512654273));
#64216=CARTESIAN_POINT('Ctrl Pts',(30.8677631763936,19.2037734965193,38.5840043557759));
#64217=CARTESIAN_POINT('Ctrl Pts',(30.8391528571472,19.1903103704863,38.5819380436388));
#64218=CARTESIAN_POINT('Ctrl Pts',(30.8289350472629,19.1856073261418,38.5812078177547));
#64219=CARTESIAN_POINT('Ctrl Pts',(30.8097174925182,19.1769581208796,38.5798495960728));
#64220=CARTESIAN_POINT('Ctrl Pts',(30.8007279774588,19.1729918389495,38.5792205009467));
#64221=CARTESIAN_POINT('Ctrl Pts',(30.7789652853323,19.1635813618888,38.5777119564451));
#64222=CARTESIAN_POINT('Ctrl Pts',(30.7661639816944,19.1582038361249,38.5768364330705));
#64223=CARTESIAN_POINT('Ctrl Pts',(30.7194291868712,19.1391432530707,38.5736792579904));
#64224=CARTESIAN_POINT('Ctrl Pts',(30.6851751105106,19.1262599897052,38.5714396845317));
#64225=CARTESIAN_POINT('Ctrl Pts',(30.5926001924708,19.0943203652585,38.5655353622074));
#64226=CARTESIAN_POINT('Ctrl Pts',(30.5337210479095,19.0769990560148,38.5619337703739));
#64227=CARTESIAN_POINT('Ctrl Pts',(30.3162492490716,19.0237828458139,38.5488891576929));
#64228=CARTESIAN_POINT('Ctrl Pts',(30.1542500927719,19.004592607178,38.539605629667));
#64229=CARTESIAN_POINT('Ctrl Pts',(29.9623522782642,19.0053890748723,38.5278626789189));
#64230=CARTESIAN_POINT('Ctrl Pts',(29.9329911836527,19.0061595414374,38.5260474684379));
#64231=CARTESIAN_POINT('Ctrl Pts',(29.8851966015945,19.0084705885994,38.5230570271447));
#64232=CARTESIAN_POINT('Ctrl Pts',(29.8667481005039,19.0096198576252,38.5218940835576));
#64233=CARTESIAN_POINT('Ctrl Pts',(29.8308768702242,19.0123554349897,38.5196147760501));
#64234=CARTESIAN_POINT('Ctrl Pts',(29.8134537489871,19.013914902641,38.5184993582715));
#64235=CARTESIAN_POINT('Ctrl Pts',(29.7720490545758,19.0181704801742,38.5158278346409));
#64236=CARTESIAN_POINT('Ctrl Pts',(29.7480919427068,19.0210729864507,38.5142653752762));
#64237=CARTESIAN_POINT('Ctrl Pts',(29.6617427421401,19.0331279166417,38.5085708438117));
#64238=CARTESIAN_POINT('Ctrl Pts',(29.5997459870369,19.04480203505,38.5043615625894));
#64239=CARTESIAN_POINT('Ctrl Pts',(29.4375777013574,19.0833750114181,38.4930361402285));
#64240=CARTESIAN_POINT('Ctrl Pts',(29.3387740896111,19.1151797928065,38.4858030141114));
#64241=CARTESIAN_POINT('Ctrl Pts',(29.1601980044313,19.1884397718601,38.4723440741033));
#64242=CARTESIAN_POINT('Ctrl Pts',(29.0798650600122,19.2278904505962,38.4661343892974));
#64243=CARTESIAN_POINT('Ctrl Pts',(28.9834993954173,19.2835406586168,38.4586889918098));
#64244=CARTESIAN_POINT('Ctrl Pts',(28.9647351365839,19.2947924157477,38.4572396834865));
#64245=CARTESIAN_POINT('Ctrl Pts',(28.9363375327525,19.3124622896474,38.4550513795919));
#64246=CARTESIAN_POINT('Ctrl Pts',(28.9265692127435,19.3186589492467,38.4542995755035));
#64247=CARTESIAN_POINT('Ctrl Pts',(28.9087403618766,19.3301876313821,38.4529299332469));
#64248=CARTESIAN_POINT('Ctrl Pts',(28.9006642053438,19.3354935386767,38.4523105647302));
#64249=CARTESIAN_POINT('Ctrl Pts',(28.8815962470865,19.3482202112982,38.4508503212496));
#64250=CARTESIAN_POINT('Ctrl Pts',(28.8706394246571,19.3556922007663,38.4500128220699));
#64251=CARTESIAN_POINT('Ctrl Pts',(28.8332761447241,19.3817217099671,38.4471593712306));
#64252=CARTESIAN_POINT('Ctrl Pts',(28.8072446373423,19.4008114283597,38.445175588265));
#64253=CARTESIAN_POINT('Ctrl Pts',(28.7416412343071,19.451414039404,38.4401550235173));
#64254=CARTESIAN_POINT('Ctrl Pts',(28.7027828720629,19.4838161068116,38.4371604259035));
#64255=CARTESIAN_POINT('Ctrl Pts',(28.5413125590712,19.6292156101698,38.4244265430131));
#64256=CARTESIAN_POINT('Ctrl Pts',(28.4319085545446,19.7558508007852,38.4149780941566));
#64257=CARTESIAN_POINT('Ctrl Pts',(28.3197215603009,19.924374741007,38.4026931886661));
#64258=CARTESIAN_POINT('Ctrl Pts',(28.3007175542428,19.9546559116108,38.400498821796));
#64259=CARTESIAN_POINT('Ctrl Pts',(28.2723805329349,20.0026247553496,38.397032382148));
#64260=CARTESIAN_POINT('Ctrl Pts',(28.2624820060267,20.0199706247866,38.3957808402538));
#64261=CARTESIAN_POINT('Ctrl Pts',(28.2445732468259,20.0524777602532,38.3934373655492));
#64262=CARTESIAN_POINT('Ctrl Pts',(28.2364947828984,20.0675994424353,38.3923480111075));
#64263=CARTESIAN_POINT('Ctrl Pts',(28.2188511441517,20.101675441006,38.3898940026575));
#64264=CARTESIAN_POINT('Ctrl Pts',(28.2093917662706,20.1206818804129,38.3885257764755));
#64265=CARTESIAN_POINT('Ctrl Pts',(28.181442113687,20.1791622093136,38.3843158605028));
#64266=CARTESIAN_POINT('Ctrl Pts',(28.163941773927,20.2190920865512,38.3814409680758));
#64267=CARTESIAN_POINT('Ctrl Pts',(28.1252843302413,20.3157950757867,38.3744747904176));
#64268=CARTESIAN_POINT('Ctrl Pts',(28.1053787260614,20.3730196231009,38.3703488499643));
#64269=CARTESIAN_POINT('Ctrl Pts',(28.0506865276456,20.5568087832779,38.3571254767949));
#64270=CARTESIAN_POINT('Ctrl Pts',(28.0257640951714,20.6859410108696,38.3478535727279));
#64271=CARTESIAN_POINT('Ctrl Pts',(28.0100420914412,20.8562012952192,38.336166849105));
#64272=CARTESIAN_POINT('Ctrl Pts',(28.0075695812252,20.8959229884023,38.333480220987));
#64273=CARTESIAN_POINT('Ctrl Pts',(28.0058509138303,20.9492083396158,38.3299513932691));
#64274=CARTESIAN_POINT('Ctrl Pts',(28.0055524375389,20.9627264884663,38.3290626395997));
#64275=CARTESIAN_POINT('Ctrl Pts',(28.0052973275745,20.9841488621085,38.3276655801364));
#64276=CARTESIAN_POINT('Ctrl Pts',(28.0052501828923,20.9920513079393,38.3271526709971));
#64277=CARTESIAN_POINT('Ctrl Pts',(28.0052500005311,20.9999539693013,38.3266423355102));
#64278=CARTESIAN_POINT('Ctrl Pts',(28.0052500005237,20.9999542895831,38.3266423148271));
#64279=CARTESIAN_POINT('Ctrl Pts',(28.0052499353216,21.0027996336104,38.3264585691541));
#64280=CARTESIAN_POINT('Ctrl Pts',(28.0052559580871,21.0056449990733,38.3262751575534));
#64281=CARTESIAN_POINT('Ctrl Pts',(28.0052915554529,21.014008266251,38.3257370685318));
#64282=CARTESIAN_POINT('Ctrl Pts',(28.0053379360369,21.0195259182242,38.3253833666345));
#64283=CARTESIAN_POINT('Ctrl Pts',(28.0055430235024,21.0358601424736,38.3243399943713));
#64284=CARTESIAN_POINT('Ctrl Pts',(28.0057668233762,21.0466758070004,38.3236539289844));
#64285=CARTESIAN_POINT('Ctrl Pts',(28.0067037247021,21.0791706198002,38.3216056947997));
#64286=CARTESIAN_POINT('Ctrl Pts',(28.0076824637508,21.1008412192493,38.3202571251304));
#64287=CARTESIAN_POINT('Ctrl Pts',(28.0146518748454,21.2141215530399,38.3132786163443));
#64288=CARTESIAN_POINT('Ctrl Pts',(28.0266085742015,21.3052622726676,38.307904085915));
#64289=CARTESIAN_POINT('Ctrl Pts',(28.0625866105701,21.4832301201308,38.2973486523115));
#64290=CARTESIAN_POINT('Ctrl Pts',(28.0862862554856,21.5698957836393,38.2921768223953));
#64291=CARTESIAN_POINT('Ctrl Pts',(28.1394109870688,21.7227988264733,38.2826331726122));
#64292=CARTESIAN_POINT('Ctrl Pts',(28.1667576821797,21.789588915637,38.2783118530124));
#64293=CARTESIAN_POINT('Ctrl Pts',(28.2084407559848,21.877482875285,38.2723216468109));
#64294=CARTESIAN_POINT('Ctrl Pts',(28.2196517372263,21.9000114974699,38.2707584839981));
#64295=CARTESIAN_POINT('Ctrl Pts',(28.2394550801156,21.9379879177497,38.2680724063024));
#64296=CARTESIAN_POINT('Ctrl Pts',(28.2478322496926,21.953544907737,38.2669571320671));
#64297=CARTESIAN_POINT('Ctrl Pts',(28.2652475144405,21.9848817181851,38.2646790454114));
#64298=CARTESIAN_POINT('Ctrl Pts',(28.2742969192428,22.0006532995147,38.2635159040854));
#64299=CARTESIAN_POINT('Ctrl Pts',(28.2977586079486,22.0402780447871,38.2605501691011));
#64300=CARTESIAN_POINT('Ctrl Pts',(28.3124571079463,22.0639563075914,38.2587372983413));
#64301=CARTESIAN_POINT('Ctrl Pts',(28.3862524131256,22.1774574780032,38.2498430952989));
#64302=CARTESIAN_POINT('Ctrl Pts',(28.452041508447,22.2626977740906,38.242515249841));
#64303=CARTESIAN_POINT('Ctrl Pts',(28.5940153617141,22.4187842910637,38.2278755020148));
#64304=CARTESIAN_POINT('Ctrl Pts',(28.6695177488835,22.4898184268421,38.2205970864918));
#64305=CARTESIAN_POINT('Ctrl Pts',(28.7762789410399,22.5756442072145,38.2111915221725));
#64306=CARTESIAN_POINT('Ctrl Pts',(28.8028910913515,22.5959568895346,38.2089135559009));
#64307=CARTESIAN_POINT('Ctrl Pts',(28.8495779822753,22.6297671227649,38.205045765066));
#64308=CARTESIAN_POINT('Ctrl Pts',(28.8694098895584,22.643586875849,38.2034410056227));
#64309=CARTESIAN_POINT('Ctrl Pts',(28.8993576194421,22.6636571284915,38.2010796882376));
#64310=CARTESIAN_POINT('Ctrl Pts',(28.909285345264,22.6701826996185,38.2003068273198));
#64311=CARTESIAN_POINT('Ctrl Pts',(28.9274388052809,22.6818842041793,38.1989123887478));
#64312=CARTESIAN_POINT('Ctrl Pts',(28.9356446367017,22.6870891085592,38.1982890263585));
#64313=CARTESIAN_POINT('Ctrl Pts',(28.9546287244898,22.6989369420292,38.1968625524669));
#64314=CARTESIAN_POINT('Ctrl Pts',(28.9654326137859,22.7055375047443,38.1960621349731));
#64315=CARTESIAN_POINT('Ctrl Pts',(28.9935484837526,22.7223492207744,38.1940064685457));
#64316=CARTESIAN_POINT('Ctrl Pts',(29.010953171196,22.7324023454945,38.1927604000512));
#64317=CARTESIAN_POINT('Ctrl Pts',(29.0285070492154,22.7421908647091,38.1915268296408));
#64318=CARTESIAN_POINT('',(28.0052504446904,20.9986680494153,38.1704548814437));
#64319=CARTESIAN_POINT('Ctrl Pts',(29.0285070491141,22.7421908646526,38.0351948256389));
#64320=CARTESIAN_POINT('Ctrl Pts',(28.9662244865535,22.7074604159295,38.0397334363702));
#64321=CARTESIAN_POINT('Ctrl Pts',(28.9058244632904,22.6693959224897,38.0442720471014));
#64322=CARTESIAN_POINT('Ctrl Pts',(28.8476729941294,22.62824139305,38.0488106578327));
#64323=CARTESIAN_POINT('Ctrl Pts',(28.7907206949419,22.5879355313514,38.0532556756455));
#64324=CARTESIAN_POINT('Ctrl Pts',(28.7359254420456,22.544666231565,38.0577006934583));
#64325=CARTESIAN_POINT('Ctrl Pts',(28.6835980319698,22.4987039137422,38.0621457112711));
#64326=CARTESIAN_POINT('Ctrl Pts',(28.6296179372828,22.451289943425,38.0667311184616));
#64327=CARTESIAN_POINT('Ctrl Pts',(28.5782646094843,22.4010103669668,38.0713165256521));
#64328=CARTESIAN_POINT('Ctrl Pts',(28.5298368250253,22.3482016916799,38.0759019328425));
#64329=CARTESIAN_POINT('Ctrl Pts',(28.4814090405664,22.295393016393,38.080487340033));
#64330=CARTESIAN_POINT('Ctrl Pts',(28.4359071028786,22.2400557227533,38.0850727472235));
#64331=CARTESIAN_POINT('Ctrl Pts',(28.3935816618508,22.1825598020219,38.0896581544139));
#64332=CARTESIAN_POINT('Ctrl Pts',(28.3522336481963,22.1263916426889,38.0941376701501));
#64333=CARTESIAN_POINT('Ctrl Pts',(28.3137534845701,22.0679416529915,38.0986171858863));
#64334=CARTESIAN_POINT('Ctrl Pts',(28.2784002030468,22.0075324816753,38.1030967016224));
#64335=CARTESIAN_POINT('Ctrl Pts',(28.2431007530867,21.947215293903,38.1075693965113));
#64336=CARTESIAN_POINT('Ctrl Pts',(28.2109189775721,21.8849452570051,38.1120420914001));
#64337=CARTESIAN_POINT('Ctrl Pts',(28.182072043412,21.8210758230248,38.116514786289));
#64338=CARTESIAN_POINT('Ctrl Pts',(28.1530811998829,21.7568877621189,38.1210097942145));
#64339=CARTESIAN_POINT('Ctrl Pts',(28.1274588572479,21.6910846990376,38.12550480214));
#64340=CARTESIAN_POINT('Ctrl Pts',(28.105379654119,21.6240523275126,38.1299998100656));
#64341=CARTESIAN_POINT('Ctrl Pts',(28.0834561672684,21.5574927099795,38.1344631163984));
#64342=CARTESIAN_POINT('Ctrl Pts',(28.065026159838,21.4897215305499,38.1389264227312));
#64343=CARTESIAN_POINT('Ctrl Pts',(28.0502123832888,21.4211363344806,38.143389729064));
#64344=CARTESIAN_POINT('Ctrl Pts',(28.0352407796909,21.3518204267628,38.1479005877858));
#64345=CARTESIAN_POINT('Ctrl Pts',(28.0239630968909,21.2816735241105,38.1524114465077));
#64346=CARTESIAN_POINT('Ctrl Pts',(28.0164536567916,21.2111195558078,38.1569223052296));
#64347=CARTESIAN_POINT('Ctrl Pts',(28.0089442166923,21.140565587505,38.1614331639515));
#64348=CARTESIAN_POINT('Ctrl Pts',(28.0052030780735,21.0696050596119,38.1659440226733));
#64349=CARTESIAN_POINT('Ctrl Pts',(28.0052504446899,20.9986680501775,38.1704548813952));
#64350=CARTESIAN_POINT('Ctrl Pts',(28.0052504446904,20.9986680494153,38.1704548814437));
#64351=CARTESIAN_POINT('Ctrl Pts',(28.0053033577008,20.9194247162574,38.1754939362809));
#64352=CARTESIAN_POINT('Ctrl Pts',(28.0100823501052,20.8403644159677,38.1805329911182));
#64353=CARTESIAN_POINT('Ctrl Pts',(28.0194980695967,20.7620091048615,38.1855720459555));
#64354=CARTESIAN_POINT('Ctrl Pts',(28.0291574941401,20.681625740012,38.1907415255704));
#64355=CARTESIAN_POINT('Ctrl Pts',(28.0436968045175,20.6019846203246,38.1959110051852));
#64356=CARTESIAN_POINT('Ctrl Pts',(28.0629665565717,20.5236293443753,38.2010804848001));
#64357=CARTESIAN_POINT('Ctrl Pts',(28.0822363086259,20.445274068426,38.206249964415));
#64358=CARTESIAN_POINT('Ctrl Pts',(28.1062363183479,20.3682048301099,38.2114194440298));
#64359=CARTESIAN_POINT('Ctrl Pts',(28.134766354791,20.2929420028879,38.2165889236447));
#64360=CARTESIAN_POINT('Ctrl Pts',(28.159353446891,20.2280807445326,38.2210439642702));
#64361=CARTESIAN_POINT('Ctrl Pts',(28.1873762006749,20.1643757540817,38.2254990048957));
#64362=CARTESIAN_POINT('Ctrl Pts',(28.2187051826263,20.1022158744456,38.2299540455211));
#64363=CARTESIAN_POINT('Ctrl Pts',(28.2499872411846,20.0401490955835,38.2344024135512));
#64364=CARTESIAN_POINT('Ctrl Pts',(28.2845654808836,19.979623267721,38.2388507815812));
#64365=CARTESIAN_POINT('Ctrl Pts',(28.3222619153755,19.9210085811738,38.2432991496112));
#64366=CARTESIAN_POINT('Ctrl Pts',(28.3599141283183,19.8624626553006,38.247742299277));
#64367=CARTESIAN_POINT('Ctrl Pts',(28.4006770073976,19.8058238274401,38.2521854489428));
#64368=CARTESIAN_POINT('Ctrl Pts',(28.4443268903497,19.7514373310038,38.2566285986086));
#64369=CARTESIAN_POINT('Ctrl Pts',(28.4879494039135,19.6970849360366,38.2610689623267));
#64370=CARTESIAN_POINT('Ctrl Pts',(28.5344550246538,19.6449824515438,38.2655093260449));
#64371=CARTESIAN_POINT('Ctrl Pts',(28.5835779446301,19.5954445103302,38.2699496897631));
#64372=CARTESIAN_POINT('Ctrl Pts',(28.6326867335903,19.5459208195203,38.2743887761376));
#64373=CARTESIAN_POINT('Ctrl Pts',(28.6844109827346,19.498960554679,38.2788278625121));
#64374=CARTESIAN_POINT('Ctrl Pts',(28.7384471413776,19.4548424198802,38.2832669488865));
#64375=CARTESIAN_POINT('Ctrl Pts',(28.7924860924751,19.4107220051658,38.287706264662));
#64376=CARTESIAN_POINT('Ctrl Pts',(28.8488368097305,19.3694443196648,38.2921455804375));
#64377=CARTESIAN_POINT('Ctrl Pts',(28.907163086983,19.3312474587143,38.2965848962129));
#64378=CARTESIAN_POINT('Ctrl Pts',(28.9655510022316,19.2930102321159,38.3010289033649));
#64379=CARTESIAN_POINT('Ctrl Pts',(29.0259182342395,19.2578605967989,38.3054729105169));
#64380=CARTESIAN_POINT('Ctrl Pts',(29.0879008637305,19.225992466725,38.3099169176689));
#64381=CARTESIAN_POINT('Ctrl Pts',(29.149919797734,19.194105670826,38.3143635277681));
#64382=CARTESIAN_POINT('Ctrl Pts',(29.2135555660711,19.1655044064381,38.3188101378674));
#64383=CARTESIAN_POINT('Ctrl Pts',(29.2784235434252,19.1403347129613,38.3232567479666));
#64384=CARTESIAN_POINT('Ctrl Pts',(29.3434038927321,19.115121417576,38.3277110610077));
#64385=CARTESIAN_POINT('Ctrl Pts',(29.4096202471859,19.0933517118923,38.3321653740488));
#64386=CARTESIAN_POINT('Ctrl Pts',(29.4766728619332,19.0751217521457,38.3366196870899));
#64387=CARTESIAN_POINT('Ctrl Pts',(29.511295741333,19.0657086412603,38.3389196890184));
#64388=CARTESIAN_POINT('Ctrl Pts',(29.5461414162752,19.0572384654601,38.341219690947));
#64389=CARTESIAN_POINT('Ctrl Pts',(29.581154132761,19.0497190710062,38.3435196928755));
#64390=CARTESIAN_POINT('Ctrl Pts',(29.6489727799341,19.0351542154165,38.3479747319283));
#64391=CARTESIAN_POINT('Ctrl Pts',(29.717685610293,19.0241023559207,38.3524297709811));
#64392=CARTESIAN_POINT('Ctrl Pts',(29.7868958052815,19.0166658968562,38.3568848100339));
#64393=CARTESIAN_POINT('Ctrl Pts',(29.8560023391715,19.0092405759125,38.3613331764535));
#64394=CARTESIAN_POINT('Ctrl Pts',(29.9256042765727,19.0054199595103,38.3657815428732));
#64395=CARTESIAN_POINT('Ctrl Pts',(29.9952941040524,19.0052555509431,38.3702299092928));
#64396=CARTESIAN_POINT('Ctrl Pts',(30.0649021778678,19.0050913352449,38.3746730573001));
#64397=CARTESIAN_POINT('Ctrl Pts',(30.1345974500217,19.0085748096506,38.3791162053074));
#64398=CARTESIAN_POINT('Ctrl Pts',(30.2039685684346,19.0157055698333,38.3835593533148));
#64399=CARTESIAN_POINT('Ctrl Pts',(30.2732961892405,19.0228318588324,38.3879997153456));
#64400=CARTESIAN_POINT('Ctrl Pts',(30.3422995739079,19.0336008467942,38.3924400773764));
#64401=CARTESIAN_POINT('Ctrl Pts',(30.4105701878447,19.0479601224992,38.3968804394072));
#64402=CARTESIAN_POINT('Ctrl Pts',(30.4788211622039,19.0623152674357,38.401319524068));
#64403=CARTESIAN_POINT('Ctrl Pts',(30.5463393057376,19.0802585490548,38.4057586087288));
#64404=CARTESIAN_POINT('Ctrl Pts',(30.6127257662419,19.1016863541861,38.4101976933896));
#64405=CARTESIAN_POINT('Ctrl Pts',(30.6791156570786,19.1231152665386,38.4146370074275));
#64406=CARTESIAN_POINT('Ctrl Pts',(30.7443732838954,19.1480289072775,38.4190763214655));
#64407=CARTESIAN_POINT('Ctrl Pts',(30.8081161690147,19.1762741927919,38.4235156355034));
#64408=CARTESIAN_POINT('Ctrl Pts',(30.8719264159649,19.2045493271928,38.4279596408935));
#64409=CARTESIAN_POINT('Ctrl Pts',(30.934218278086,19.2361629349013,38.4324036462836));
#64410=CARTESIAN_POINT('Ctrl Pts',(30.9946313357288,19.2709146728729,38.4368476516737));
#64411=CARTESIAN_POINT('Ctrl Pts',(31.0550797783436,19.3056867655379,38.4412942599945));
#64412=CARTESIAN_POINT('Ctrl Pts',(31.1136468153052,19.3436003809612,38.4457408683154));
#64413=CARTESIAN_POINT('Ctrl Pts',(31.1700009906591,19.3844117961694,38.4501874766363));
#64414=CARTESIAN_POINT('Ctrl Pts',(31.2264527893072,19.4252939096845,38.4546417878921));
#64415=CARTESIAN_POINT('Ctrl Pts',(31.2806836939092,19.4690835359395,38.459096099148));
#64416=CARTESIAN_POINT('Ctrl Pts',(31.3323959319347,19.5154971731034,38.4635504104039));
#64417=CARTESIAN_POINT('Ctrl Pts',(31.3590979363168,19.5394632049415,38.465850427638));
#64418=CARTESIAN_POINT('Ctrl Pts',(31.3851290117348,19.5641282675209,38.4681504448722));
#64419=CARTESIAN_POINT('Ctrl Pts',(31.4104522994071,19.5894497975623,38.4704504621063));
#64420=CARTESIAN_POINT('Ctrl Pts',(31.4595024849717,19.6384965786668,38.4749055026048));
#64421=CARTESIAN_POINT('Ctrl Pts',(31.5060879097224,19.6902014941159,38.4793605431033));
#64422=CARTESIAN_POINT('Ctrl Pts',(31.5499071425516,19.7442868910585,38.4838155836019));
#64423=CARTESIAN_POINT('Ctrl Pts',(31.593660744409,19.7982912807142,38.4882639514907));
#64424=CARTESIAN_POINT('Ctrl Pts',(31.6346560720253,19.8546686981639,38.4927123193795));
#64425=CARTESIAN_POINT('Ctrl Pts',(31.6726286347102,19.9131048749545,38.4971606872683));
#64426=CARTESIAN_POINT('Ctrl Pts',(31.7105566517444,19.9714725002086,38.5016038367724));
#64427=CARTESIAN_POINT('Ctrl Pts',(31.745468681447,20.031893679646,38.5060469862765));
#64428=CARTESIAN_POINT('Ctrl Pts',(31.7771417410935,20.0940227405927,38.5104901357806));
#64429=CARTESIAN_POINT('Ctrl Pts',(31.8087949409794,20.1561128451425,38.5149304993244));
#64430=CARTESIAN_POINT('Ctrl Pts',(31.8372129780541,20.2199082718438,38.5193708628682));
#64431=CARTESIAN_POINT('Ctrl Pts',(31.8622180745264,20.2850374797186,38.523811226412));
#64432=CARTESIAN_POINT('Ctrl Pts',(31.8872159778013,20.3501479519226,38.5282503125997));
#64433=CARTESIAN_POINT('Ctrl Pts',(31.9088027142856,20.4165909870344,38.5326893987874));
#64434=CARTESIAN_POINT('Ctrl Pts',(31.9268487620699,20.4839753779035,38.5371284849752));
#64435=CARTESIAN_POINT('Ctrl Pts',(31.9448957423796,20.5513632508458,38.5415678005517));
#64436=CARTESIAN_POINT('Ctrl Pts',(31.9594015464992,20.6196921028616,38.5460071161282));
#64437=CARTESIAN_POINT('Ctrl Pts',(31.9702870874265,20.6885576207058,38.5504464317047));
#64438=CARTESIAN_POINT('Ctrl Pts',(31.9811841319252,20.7574959139321,38.5548904386405));
#64439=CARTESIAN_POINT('Ctrl Pts',(31.9884532007772,20.826971520689,38.5593344455763));
#64440=CARTESIAN_POINT('Ctrl Pts',(31.9920668706479,20.8965729949813,38.5637784525121));
#64441=CARTESIAN_POINT('Ctrl Pts',(31.9956826571119,20.966215236145,38.568225062385));
#64442=CARTESIAN_POINT('Ctrl Pts',(31.9956387833975,21.0359830021607,38.5726716722579));
#64443=CARTESIAN_POINT('Ctrl Pts',(31.9919599809071,21.1054656198218,38.5771182821308));
#64444=CARTESIAN_POINT('Ctrl Pts',(31.9882748055725,21.175068603255,38.5815725949321));
#64445=CARTESIAN_POINT('Ctrl Pts',(31.9809421837478,21.2443849658485,38.5860269077334));
#64446=CARTESIAN_POINT('Ctrl Pts',(31.9700385397303,21.3130107258186,38.5904812205348));
#64447=CARTESIAN_POINT('Ctrl Pts',(31.9644083961772,21.3484459325667,38.5927812241355));
#64448=CARTESIAN_POINT('Ctrl Pts',(31.9578269728795,21.3836971987488,38.5950812277363));
#64449=CARTESIAN_POINT('Ctrl Pts',(31.9503100035496,21.41871046387,38.597381231337));
#64450=CARTESIAN_POINT('Ctrl Pts',(31.9357498524979,21.4865301404717,38.6018362714438));
#64451=CARTESIAN_POINT('Ctrl Pts',(31.9176192905568,21.5537230114834,38.6062913115506));
#64452=CARTESIAN_POINT('Ctrl Pts',(31.8959878436836,21.6198851983264,38.6107463516575));
#64453=CARTESIAN_POINT('Ctrl Pts',(31.8743887956824,21.6859482896147,38.6151947191512));
#64454=CARTESIAN_POINT('Ctrl Pts',(31.849299420854,21.7509832993906,38.619643086645));
#64455=CARTESIAN_POINT('Ctrl Pts',(31.8208400497719,21.8145974930276,38.6240914541388));
#64456=CARTESIAN_POINT('Ctrl Pts',(31.7924140644281,21.878137060742,38.6285346032448));
#64457=CARTESIAN_POINT('Ctrl Pts',(31.7606261336652,21.9402586782658,38.6329777523509));
#64458=CARTESIAN_POINT('Ctrl Pts',(31.725645495878,22.0005874199968,38.6374209014569));
#64459=CARTESIAN_POINT('Ctrl Pts',(31.6906867917963,22.0608783341486,38.641861264601));
#64460=CARTESIAN_POINT('Ctrl Pts',(31.6525395969839,22.1193781803559,38.6463016277452));
#64461=CARTESIAN_POINT('Ctrl Pts',(31.6114194156794,22.1757359521897,38.6507419908893));
#64462=CARTESIAN_POINT('Ctrl Pts',(31.5703110633973,22.2320775116109,38.6551810766764));
#64463=CARTESIAN_POINT('Ctrl Pts',(31.5262317107216,22.2862778249092,38.6596201624635));
#64464=CARTESIAN_POINT('Ctrl Pts',(31.4794395755487,22.3380157341378,38.6640592482505));
#64465=CARTESIAN_POINT('Ctrl Pts',(31.4326450224067,22.3897563169068,38.668498563426));
#64466=CARTESIAN_POINT('Ctrl Pts',(31.383137738449,22.439033881712,38.6729378786014));
#64467=CARTESIAN_POINT('Ctrl Pts',(31.3312143290751,22.4855625104872,38.6773771937769));
#64468=CARTESIAN_POINT('Ctrl Pts',(31.2792360482914,22.532140309598,38.6818212003138));
#64469=CARTESIAN_POINT('Ctrl Pts',(31.2248369110719,22.5759630474057,38.6862652068507));
#64470=CARTESIAN_POINT('Ctrl Pts',(31.168347561005,22.6167843205554,38.6907092133877));
#64471=CARTESIAN_POINT('Ctrl Pts',(31.1118251240692,22.6576295034882,38.6951558228623));
#64472=CARTESIAN_POINT('Ctrl Pts',(31.0532104486739,22.6954694571733,38.699602432337));
#64473=CARTESIAN_POINT('Ctrl Pts',(30.992861844136,22.7301019972704,38.7040490418117));
#64474=CARTESIAN_POINT('Ctrl Pts',(30.9324086967318,22.7647945318783,38.7085033542201));
#64475=CARTESIAN_POINT('Ctrl Pts',(30.8702160609267,22.7962683411249,38.7129576666284));
#64476=CARTESIAN_POINT('Ctrl Pts',(30.8066646905723,22.8243682850466,38.7174119790368));
#64477=CARTESIAN_POINT('Ctrl Pts',(30.7738496128403,22.8388778359644,38.7197119862138));
#64478=CARTESIAN_POINT('Ctrl Pts',(30.7406725588488,22.8524886398037,38.7220119933908));
#64479=CARTESIAN_POINT('Ctrl Pts',(30.7071874705828,22.8651845602917,38.7243120005678));
#64480=CARTESIAN_POINT('Ctrl Pts',(30.6399473745884,22.8906787416293,38.7289305550163));
#64481=CARTESIAN_POINT('Ctrl Pts',(30.5711895972421,22.9125843100179,38.7335491094648));
#64482=CARTESIAN_POINT('Ctrl Pts',(30.5013345674729,22.9307229770106,38.7381676639133));
#64483=CARTESIAN_POINT('Ctrl Pts',(30.434069343021,22.9481891710779,38.7426149900778));
#64484=CARTESIAN_POINT('Ctrl Pts',(30.3657873143873,22.9621626908888,38.7470623162424));
#64485=CARTESIAN_POINT('Ctrl Pts',(30.2968839503906,22.9725332652456,38.751509642407));
#64486=CARTESIAN_POINT('Ctrl Pts',(30.2280487577815,22.9828935791971,38.7559525684904));
#64487=CARTESIAN_POINT('Ctrl Pts',(30.1585939306255,22.9896579468043,38.7603954945738));
#64488=CARTESIAN_POINT('Ctrl Pts',(30.0889264887833,22.9927668308391,38.7648384206572));
#64489=CARTESIAN_POINT('Ctrl Pts',(30.0193043302163,22.9958736941244,38.7692784588745));
#64490=CARTESIAN_POINT('Ctrl Pts',(29.9494703188918,22.9953297680141,38.7737184970918));
#64491=CARTESIAN_POINT('Ctrl Pts',(29.8798362094755,22.9911273756209,38.7781585353091));
#64492=CARTESIAN_POINT('Ctrl Pts',(29.8102237308516,22.9869262886378,38.7825971942951));
#64493=CARTESIAN_POINT('Ctrl Pts',(29.7408115187254,22.9790690231803,38.787035853281));
#64494=CARTESIAN_POINT('Ctrl Pts',(29.6720091552,22.9675999512674,38.791474512267));
#64495=CARTESIAN_POINT('Ctrl Pts',(29.6031755485967,22.9561256712615,38.7959151868432));
#64496=CARTESIAN_POINT('Ctrl Pts',(29.5349528272508,22.9410363868837,38.8003558614193));
#64497=CARTESIAN_POINT('Ctrl Pts',(29.4677420410995,22.9224278992168,38.8047965359955));
#64498=CARTESIAN_POINT('Ctrl Pts',(29.4005125436344,22.9038142309938,38.8092384468443));
#64499=CARTESIAN_POINT('Ctrl Pts',(29.334296008895,22.8816795567646,38.8136803576931));
#64500=CARTESIAN_POINT('Ctrl Pts',(29.2694776142112,22.8561693366612,38.8181222685418));
#64501=CARTESIAN_POINT('Ctrl Pts',(29.2045867169759,22.8306305821263,38.8225691478856));
#64502=CARTESIAN_POINT('Ctrl Pts',(29.1410975277273,22.8017089455978,38.8270160272294));
#64503=CARTESIAN_POINT('Ctrl Pts',(29.0793734864984,22.7695972381132,38.8314629065732));
#64504=CARTESIAN_POINT('Ctrl Pts',(29.0622803501589,22.7607045962317,38.8326943734927));
#64505=CARTESIAN_POINT('Ctrl Pts',(29.0453224246989,22.7515675748504,38.8339258404121));
#64506=CARTESIAN_POINT('Ctrl Pts',(29.0285070491141,22.7421908646526,38.8351573073316));
#64507=CARTESIAN_POINT('Origin',(30.,21.,34.5704548813952));
#64508=CARTESIAN_POINT('',(29.0285070493988,22.7421908648114,39.7951262847314));
#64509=CARTESIAN_POINT('',(29.0285070491141,22.7421908646526,39.6352957892028));
#64510=CARTESIAN_POINT('',(29.0285070491141,22.7421908646526,34.5704548813952));
#64511=CARTESIAN_POINT('Ctrl Pts',(29.0285070493988,22.7421908648114,39.7951262847314));
#64512=CARTESIAN_POINT('Ctrl Pts',(29.036539361456,22.7466699002019,39.7945520334221));
#64513=CARTESIAN_POINT('Ctrl Pts',(29.0446025931056,22.7510933553019,39.7939758446525));
#64514=CARTESIAN_POINT('Ctrl Pts',(29.0679332045984,22.7636833123941,39.7923092073879));
#64515=CARTESIAN_POINT('Ctrl Pts',(29.0832762380762,22.7717067621654,39.7912138221446));
#64516=CARTESIAN_POINT('Ctrl Pts',(29.1156263497491,22.7880911309112,39.788904618725));
#64517=CARTESIAN_POINT('Ctrl Pts',(29.132651951512,22.796411413743,39.7876895104054));
#64518=CARTESIAN_POINT('Ctrl Pts',(29.1784375838042,22.8179838881956,39.7844211433771));
#64519=CARTESIAN_POINT('Ctrl Pts',(29.2073979806479,22.8307954746988,39.7823530619238));
#64520=CARTESIAN_POINT('Ctrl Pts',(29.3707593117285,22.8984611764182,39.7706772357746));
#64521=CARTESIAN_POINT('Ctrl Pts',(29.510511170617,22.9391972368264,39.7606050976751));
#64522=CARTESIAN_POINT('Ctrl Pts',(29.7225137441991,22.9766011141778,39.7455891852928));
#64523=CARTESIAN_POINT('Ctrl Pts',(29.7922092847968,22.9851384194155,39.7407023088821));
#64524=CARTESIAN_POINT('Ctrl Pts',(29.9018599149984,22.9927306714876,39.7332063243256));
#64525=CARTESIAN_POINT('Ctrl Pts',(29.9415834412332,22.9942905959305,39.7305304517894));
#64526=CARTESIAN_POINT('Ctrl Pts',(29.9956257829792,22.9947964360434,39.7269663075634));
#64527=CARTESIAN_POINT('Ctrl Pts',(30.0099232799932,22.9947765569524,39.7260306439618));
#64528=CARTESIAN_POINT('Ctrl Pts',(30.0341069483306,22.9944829024896,39.7244616798304));
#64529=CARTESIAN_POINT('Ctrl Pts',(30.0439933645323,22.9942893304325,39.7238241691572));
#64530=CARTESIAN_POINT('Ctrl Pts',(30.0649267946733,22.9937237090246,39.7224829691445));
#64531=CARTESIAN_POINT('Ctrl Pts',(30.0759727385705,22.9933333573353,39.7217802620254));
#64532=CARTESIAN_POINT('Ctrl Pts',(30.1069969335266,22.9919787274037,39.7198192366003));
#64533=CARTESIAN_POINT('Ctrl Pts',(30.126965330382,22.9908057339666,39.7185717700403));
#64534=CARTESIAN_POINT('Ctrl Pts',(30.2763099853637,22.9797765281081,39.7093297276297));
#64535=CARTESIAN_POINT('Ctrl Pts',(30.4044824469687,22.9576171520778,39.7018778467403));
#64536=CARTESIAN_POINT('Ctrl Pts',(30.6463707309361,22.8910050748657,39.6873159889492));
#64537=CARTESIAN_POINT('Ctrl Pts',(30.759950135686,22.8482874585378,39.680242682745));
#64538=CARTESIAN_POINT('Ctrl Pts',(30.8942645725224,22.7832861358474,39.6710957038127));
#64539=CARTESIAN_POINT('Ctrl Pts',(30.9193176298218,22.7705009295334,39.6693549498248));
#64540=CARTESIAN_POINT('Ctrl Pts',(30.9601536807495,22.7485608240514,39.6664551459016));
#64541=CARTESIAN_POINT('Ctrl Pts',(30.9760967366155,22.7397112321717,39.6653069367518));
#64542=CARTESIAN_POINT('Ctrl Pts',(31.007041123299,22.721975512469,39.6630454764577));
#64543=CARTESIAN_POINT('Ctrl Pts',(31.0220517174939,22.7131087952896,39.6619330018443));
#64544=CARTESIAN_POINT('Ctrl Pts',(31.0548174625421,22.6931702362864,39.6594694504006));
#64545=CARTESIAN_POINT('Ctrl Pts',(31.0725183190534,22.6820135933654,39.6581153463001));
#64546=CARTESIAN_POINT('Ctrl Pts',(31.133431399875,22.6422683254831,39.6533723970482));
#64547=CARTESIAN_POINT('Ctrl Pts',(31.1756998199195,22.612278241014,39.6499323550293));
#64548=CARTESIAN_POINT('Ctrl Pts',(31.3379604917383,22.4873757941637,39.6361224559463));
#64549=CARTESIAN_POINT('Ctrl Pts',(31.4480280930436,22.380445386564,39.6253320913515));
#64550=CARTESIAN_POINT('Ctrl Pts',(31.5721117980322,22.2285594000522,39.6117634676041));
#64551=CARTESIAN_POINT('Ctrl Pts',(31.5983499650048,22.1942242306438,39.608799037308));
#64552=CARTESIAN_POINT('Ctrl Pts',(31.6402957240669,22.135472427847,39.6039264574108));
#64553=CARTESIAN_POINT('Ctrl Pts',(31.6566225584666,22.111516800433,39.601992361586));
#64554=CARTESIAN_POINT('Ctrl Pts',(31.6793639839113,22.0765344294473,39.5992520729199));
#64555=CARTESIAN_POINT('Ctrl Pts',(31.6862033755062,22.0657898317303,39.59842153022));
#64556=CARTESIAN_POINT('Ctrl Pts',(31.6975828484574,22.0475290513263,39.5970296428039));
#64557=CARTESIAN_POINT('Ctrl Pts',(31.7021768848335,22.0400473565419,39.5964648985972));
#64558=CARTESIAN_POINT('Ctrl Pts',(31.7126941853753,22.0226628587045,39.5951655284143));
#64559=CARTESIAN_POINT('Ctrl Pts',(31.7185811263426,22.0127386745704,39.5944332187545));
#64560=CARTESIAN_POINT('Ctrl Pts',(31.7353092515664,21.9839725004442,39.5923360055154));
#64561=CARTESIAN_POINT('Ctrl Pts',(31.7459293389183,21.9650030637591,39.5909841909232));
#64562=CARTESIAN_POINT('Ctrl Pts',(31.8022849931748,21.8603643031657,39.5836750507146));
#64563=CARTESIAN_POINT('Ctrl Pts',(31.8420325602963,21.7716074610855,39.578005650729));
#64564=CARTESIAN_POINT('Ctrl Pts',(31.9214090425261,21.5528163594701,39.5644868324749));
#64565=CARTESIAN_POINT('Ctrl Pts',(31.9545350176356,21.4209607285378,39.556679494198));
#64566=CARTESIAN_POINT('Ctrl Pts',(31.9792139773808,21.2510782517781,39.5462613715487));
#64567=CARTESIAN_POINT('Ctrl Pts',(31.983429621771,21.2152555373467,39.5440468889905));
#64568=CARTESIAN_POINT('Ctrl Pts',(31.9884545489312,21.1595909366878,39.5405681285468));
#64569=CARTESIAN_POINT('Ctrl Pts',(31.98994268374,21.1398171328206,39.5393250675867));
#64570=CARTESIAN_POINT('Ctrl Pts',(31.9921680020967,21.102900559982,39.5369891882851));
#64571=CARTESIAN_POINT('Ctrl Pts',(31.9929792726879,21.0857639918764,39.535898806203));
#64572=CARTESIAN_POINT('Ctrl Pts',(31.9943061497982,21.0472148792541,39.5334313789949));
#64573=CARTESIAN_POINT('Ctrl Pts',(31.9946981073203,21.0258004883987,39.5320505841083));
#64574=CARTESIAN_POINT('Ctrl Pts',(31.9948207884896,20.9699876220486,39.5284239734044));
#64575=CARTESIAN_POINT('Ctrl Pts',(31.9940066814086,20.9355963121984,39.5261616705115));
#64576=CARTESIAN_POINT('Ctrl Pts',(31.9848113712231,20.7500883739725,39.5138053010006));
#64577=CARTESIAN_POINT('Ctrl Pts',(31.960141334953,20.6002945780966,39.5032235081476));
#64578=CARTESIAN_POINT('Ctrl Pts',(31.9028457745142,20.3986628464908,39.4886284538996));
#64579=CARTESIAN_POINT('Ctrl Pts',(31.8844523582095,20.3432896644977,39.4845887054885));
#64580=CARTESIAN_POINT('Ctrl Pts',(31.8549341227635,20.2659389187308,39.4789635159574));
#64581=CARTESIAN_POINT('Ctrl Pts',(31.8457899192858,20.2432398314864,39.4773151633225));
#64582=CARTESIAN_POINT('Ctrl Pts',(31.8287498502307,20.2030883645434,39.4744105693014));
#64583=CARTESIAN_POINT('Ctrl Pts',(31.8210160062335,20.1855707893965,39.4731471829315));
#64584=CARTESIAN_POINT('Ctrl Pts',(31.8084962199335,20.1582831661363,39.4711882686405));
#64585=CARTESIAN_POINT('Ctrl Pts',(31.8038807772557,20.1484367546845,39.4704833029243));
#64586=CARTESIAN_POINT('Ctrl Pts',(31.7949325171252,20.1297461305102,39.4691494220737));
#64587=CARTESIAN_POINT('Ctrl Pts',(31.7906143990114,20.120895560238,39.4685197199439));
#64588=CARTESIAN_POINT('Ctrl Pts',(31.7797141684215,20.0989676093408,39.4669636269963));
#64589=CARTESIAN_POINT('Ctrl Pts',(31.77305314167,20.0859297197853,39.4660419790785));
#64590=CARTESIAN_POINT('Ctrl Pts',(31.7479574947235,20.0381157723963,39.4626708981153));
#64591=CARTESIAN_POINT('Ctrl Pts',(31.7286372558179,20.0038120885293,39.4602698051089));
#64592=CARTESIAN_POINT('Ctrl Pts',(31.6280555694553,19.8369754385789,39.448567706297));
#64593=CARTESIAN_POINT('Ctrl Pts',(31.5325081399703,19.7136807639498,39.4398026153954));
#64594=CARTESIAN_POINT('Ctrl Pts',(31.3726604466452,19.5508207917746,39.4263527703968));
#64595=CARTESIAN_POINT('Ctrl Pts',(31.3189196381397,19.5017455263475,39.421996765647));
#64596=CARTESIAN_POINT('Ctrl Pts',(31.2430947229039,19.4397502216716,39.4159661665922));
#64597=CARTESIAN_POINT('Ctrl Pts',(31.2232658464881,19.4241559594372,39.4143992642414));
#64598=CARTESIAN_POINT('Ctrl Pts',(31.1890453615028,19.3982786539014,39.4117087437697));
#64599=CARTESIAN_POINT('Ctrl Pts',(31.1748026870798,19.3878031273614,39.4105928303341));
#64600=CARTESIAN_POINT('Ctrl Pts',(31.1456462635157,19.366950016697,39.4083151626601));
#64601=CARTESIAN_POINT('Ctrl Pts',(31.1307262466197,19.3565841280522,39.4071531023408));
#64602=CARTESIAN_POINT('Ctrl Pts',(31.0926321783687,19.3308820779916,39.4041937274019));
#64603=CARTESIAN_POINT('Ctrl Pts',(31.0692760186317,19.3158241239205,39.4023862250952));
#64604=CARTESIAN_POINT('Ctrl Pts',(30.9556059664718,19.2458575875083,39.39361815547));
#64605=CARTESIAN_POINT('Ctrl Pts',(30.8613506353367,19.1977049332483,39.38642006757));
#64606=CARTESIAN_POINT('Ctrl Pts',(30.6666764102505,19.1170211348587,39.3718063969198));
#64607=CARTESIAN_POINT('Ctrl Pts',(30.5665886628764,19.0845250397915,39.3644161747849));
#64608=CARTESIAN_POINT('Ctrl Pts',(30.4316247101106,19.0522156343634,39.3548851780221));
#64609=CARTESIAN_POINT('Ctrl Pts',(30.3986470411496,19.0451996008548,39.3525905483028));
#64610=CARTESIAN_POINT('Ctrl Pts',(30.3416237862887,19.0345710608401,39.3486978429287));
#64611=CARTESIAN_POINT('Ctrl Pts',(30.3176611870913,19.0305561137239,39.3470845943403));
#64612=CARTESIAN_POINT('Ctrl Pts',(30.2818564198595,19.0252275552892,39.3447133944285));
#64613=CARTESIAN_POINT('Ctrl Pts',(30.2700670315828,19.0235807465391,39.3439389501191));
#64614=CARTESIAN_POINT('Ctrl Pts',(30.248629463671,19.0207816329349,39.3425430375795));
#64615=CARTESIAN_POINT('Ctrl Pts',(30.2389869108534,19.0195941783973,39.3419197599276));
#64616=CARTESIAN_POINT('Ctrl Pts',(30.2167882993152,19.017024978859,39.3404951749532));
#64617=CARTESIAN_POINT('Ctrl Pts',(30.2042272897888,19.0156919757201,39.3396965330382));
#64618=CARTESIAN_POINT('Ctrl Pts',(30.1626258394908,19.0116763622526,39.3370735980436));
#64619=CARTESIAN_POINT('Ctrl Pts',(30.1335379129146,19.0095111458063,39.3352752317517));
#64620=CARTESIAN_POINT('Ctrl Pts',(29.9366289899129,18.9991901838455,39.3232788075919));
#64621=CARTESIAN_POINT('Ctrl Pts',(29.7683928234852,19.0116272344936,39.3138485730711));
#64622=CARTESIAN_POINT('Ctrl Pts',(29.5306879467169,19.0598137747538,39.2995672354121));
#64623=CARTESIAN_POINT('Ctrl Pts',(29.4585754864453,19.0786894598511,39.2951101529228));
#64624=CARTESIAN_POINT('Ctrl Pts',(29.3635160308809,19.1093490534305,39.2889619759911));
#64625=CARTESIAN_POINT('Ctrl Pts',(29.3394920508996,19.1176073729015,39.2873844247795));
#64626=CARTESIAN_POINT('Ctrl Pts',(29.298996294201,19.1323985764078,39.2846812348498));
#64627=CARTESIAN_POINT('Ctrl Pts',(29.2824415720761,19.1386963861972,39.2835634839099));
#64628=CARTESIAN_POINT('Ctrl Pts',(29.2491216366345,19.1518826603319,39.2812869086713));
#64629=CARTESIAN_POINT('Ctrl Pts',(29.2323620929147,19.1587808317543,39.2801278423885));
#64630=CARTESIAN_POINT('Ctrl Pts',(29.1903538877437,19.1767445065439,39.2771861159289));
#64631=CARTESIAN_POINT('Ctrl Pts',(29.1652369650154,19.1881065233334,39.2753935149562));
#64632=CARTESIAN_POINT('Ctrl Pts',(29.0527584166285,19.2418230435803,39.2672081296334));
#64633=CARTESIAN_POINT('Ctrl Pts',(28.9683357554302,19.28999502394,39.2606182858524));
#64634=CARTESIAN_POINT('Ctrl Pts',(28.7945763681421,19.4067067635837,39.2461416331602));
#64635=CARTESIAN_POINT('Ctrl Pts',(28.706840534923,19.4770529692606,39.2382359896392));
#64636=CARTESIAN_POINT('Ctrl Pts',(28.5884725136578,19.5896005445797,39.2270077220312));
#64637=CARTESIAN_POINT('Ctrl Pts',(28.5528188533942,19.6262081330973,39.2235419411672));
#64638=CARTESIAN_POINT('Ctrl Pts',(28.5082100646531,19.6756770067108,39.2191366704599));
#64639=CARTESIAN_POINT('Ctrl Pts',(28.4979474901013,19.6873283368284,39.218118149193));
#64640=CARTESIAN_POINT('Ctrl Pts',(28.481228013859,19.7067631940213,39.2164520575789));
#64641=CARTESIAN_POINT('Ctrl Pts',(28.4746925250606,19.7144779638994,39.2157990472697));
#64642=CARTESIAN_POINT('Ctrl Pts',(28.4614188950304,19.7303904799072,39.2144697261078));
#64643=CARTESIAN_POINT('Ctrl Pts',(28.4546870172411,19.7385928699133,39.2137938349335));
#64644=CARTESIAN_POINT('Ctrl Pts',(28.4367724369021,19.7607793847186,39.2119893304385));
#64645=CARTESIAN_POINT('Ctrl Pts',(28.4257117558051,19.7748613449683,39.2108689452228));
#64646=CARTESIAN_POINT('Ctrl Pts',(28.3550264195727,19.8673930174197,39.203653438866));
#64647=CARTESIAN_POINT('Ctrl Pts',(28.3010875597762,19.9500295849003,39.1978806799631));
#64648=CARTESIAN_POINT('Ctrl Pts',(28.2139735807999,20.1079113217731,39.1873965940486));
#64649=CARTESIAN_POINT('Ctrl Pts',(28.1789129008328,20.1818593835315,39.1826820133975));
#64650=CARTESIAN_POINT('Ctrl Pts',(28.1190415846686,20.3312054717283,39.1732303802816));
#64651=CARTESIAN_POINT('Ctrl Pts',(28.0939937861229,20.406342665544,39.1685072648476));
#64652=CARTESIAN_POINT('Ctrl Pts',(28.0667756506715,20.5077206859994,39.1620505163735));
#64653=CARTESIAN_POINT('Ctrl Pts',(28.0605610103498,20.5328045191102,39.1604466639663));
#64654=CARTESIAN_POINT('Ctrl Pts',(28.0508931693392,20.5753510986682,39.1577120750776));
#64655=CARTESIAN_POINT('Ctrl Pts',(28.0471831570209,20.5927525673691,39.1565896833262));
#64656=CARTESIAN_POINT('Ctrl Pts',(28.0401846661912,20.6278760496174,39.1543152043465));
#64657=CARTESIAN_POINT('Ctrl Pts',(28.0369026261939,20.6455976258528,39.1531630280942));
#64658=CARTESIAN_POINT('Ctrl Pts',(28.0292960540955,20.6900237501206,39.150262142754));
#64659=CARTESIAN_POINT('Ctrl Pts',(28.0252738967388,20.716775679519,39.1485040575199));
#64660=CARTESIAN_POINT('Ctrl Pts',(28.0107008279263,20.8292113074831,39.1410644376238));
#64661=CARTESIAN_POINT('Ctrl Pts',(28.0051750809864,20.9154415709448,39.1352306109172));
#64662=CARTESIAN_POINT('Ctrl Pts',(28.0053176225983,21.0779873850309,39.124035666902));
#64663=CARTESIAN_POINT('Ctrl Pts',(28.0097550986224,21.1541564993808,39.1187090408974));
#64664=CARTESIAN_POINT('Ctrl Pts',(28.0285782558279,21.3164024973286,39.1073225283172));
#64665=CARTESIAN_POINT('Ctrl Pts',(28.0442732178099,21.4021810359098,39.1012776071046));
#64666=CARTESIAN_POINT('Ctrl Pts',(28.0708295633449,21.5077413895338,39.0939963969326));
#64667=CARTESIAN_POINT('Ctrl Pts',(28.0764762180912,21.5287307860752,39.0925568501137));
#64668=CARTESIAN_POINT('Ctrl Pts',(28.0856440218507,21.560715492244,39.0903801380092));
#64669=CARTESIAN_POINT('Ctrl Pts',(28.0889192463241,21.5717788410034,39.0896303592631));
#64670=CARTESIAN_POINT('Ctrl Pts',(28.0948555962653,21.5912101555911,39.0883197671906));
#64671=CARTESIAN_POINT('Ctrl Pts',(28.0974761396397,21.5995895364476,39.0877567408961));
#64672=CARTESIAN_POINT('Ctrl Pts',(28.104034099362,21.620083143173,39.0863847132165));
#64673=CARTESIAN_POINT('Ctrl Pts',(28.1080323446956,21.6321773584763,39.0855792172441));
#64674=CARTESIAN_POINT('Ctrl Pts',(28.1215099090744,21.6716718843333,39.0829600643823));
#64675=CARTESIAN_POINT('Ctrl Pts',(28.1314711933364,21.6989051710781,39.0811718777035));
#64676=CARTESIAN_POINT('Ctrl Pts',(28.1577497566417,21.7661652275158,39.0767775167423));
#64677=CARTESIAN_POINT('Ctrl Pts',(28.174781118424,21.8058979952606,39.0742013516575));
#64678=CARTESIAN_POINT('Ctrl Pts',(28.2574821614429,21.9827320241816,39.0626946049925));
#64679=CARTESIAN_POINT('Ctrl Pts',(28.3373975873175,22.1126030987577,39.0540887564798));
#64680=CARTESIAN_POINT('Ctrl Pts',(28.4636887270526,22.2733917758775,39.0418842982781));
#64681=CARTESIAN_POINT('Ctrl Pts',(28.4977010645186,22.3133454116577,39.0387072556169));
#64682=CARTESIAN_POINT('Ctrl Pts',(28.5474923447362,22.3673664180795,39.0341689392116));
#64683=CARTESIAN_POINT('Ctrl Pts',(28.5619814072631,22.3825960670351,39.0328607715581));
#64684=CARTESIAN_POINT('Ctrl Pts',(28.5889386140916,22.4100489545731,39.0304472782084));
#64685=CARTESIAN_POINT('Ctrl Pts',(28.6013318543462,22.4223430233554,39.0293452646484));
#64686=CARTESIAN_POINT('Ctrl Pts',(28.6269713288994,22.4471181730405,39.0270795917211));
#64687=CARTESIAN_POINT('Ctrl Pts',(28.6402301824945,22.459583757621,39.0259154128056));
#64688=CARTESIAN_POINT('Ctrl Pts',(28.6742766464513,22.4907266809058,39.0229435798523));
#64689=CARTESIAN_POINT('Ctrl Pts',(28.6952890445337,22.5091512974628,39.0211255627704));
#64690=CARTESIAN_POINT('Ctrl Pts',(28.8043883830207,22.6008327514987,39.0117622549586));
#64691=CARTESIAN_POINT('Ctrl Pts',(28.8982689392763,22.6668334911248,39.0039334509847));
#64692=CARTESIAN_POINT('Ctrl Pts',(29.0076366686528,22.730429466154,38.9951403796879));
#64693=CARTESIAN_POINT('Ctrl Pts',(29.0180464715703,22.736357762696,38.9943067195587));
#64694=CARTESIAN_POINT('Ctrl Pts',(29.0285070786203,22.742190881106,38.9934724864331));
#64695=CARTESIAN_POINT('',(28.0052501307333,20.9992778085393,38.970454881338));
#64696=CARTESIAN_POINT('Ctrl Pts',(29.0285070491141,22.7421908646526,38.8351573073316));
#64697=CARTESIAN_POINT('Ctrl Pts',(28.9676751363981,22.7082693376882,38.8396123067325));
#64698=CARTESIAN_POINT('Ctrl Pts',(28.9087114018273,22.6712078571221,38.8440673061334));
#64699=CARTESIAN_POINT('Ctrl Pts',(28.8519426650187,22.6312547066892,38.8485223055344));
#64700=CARTESIAN_POINT('Ctrl Pts',(28.8403873084475,22.6231221864791,38.8494291269558));
#64701=CARTESIAN_POINT('Ctrl Pts',(28.8289227839801,22.614869985163,38.8503359483772));
#64702=CARTESIAN_POINT('Ctrl Pts',(28.8175516689289,22.6065003911756,38.8512427697985));
#64703=CARTESIAN_POINT('Ctrl Pts',(28.7621838466573,22.5657474667445,38.8556582318764));
#64704=CARTESIAN_POINT('Ctrl Pts',(28.7088067554031,22.5220413849772,38.8600736939542));
#64705=CARTESIAN_POINT('Ctrl Pts',(28.6577568306917,22.4756052442795,38.864489156032));
#64706=CARTESIAN_POINT('Ctrl Pts',(28.6067094902745,22.429171454313,38.8689043945864));
#64707=CARTESIAN_POINT('Ctrl Pts',(28.5579895074002,22.3800081452107,38.8733196331408));
#64708=CARTESIAN_POINT('Ctrl Pts',(28.5119039421239,22.3283816036943,38.8777348716952));
#64709=CARTESIAN_POINT('Ctrl Pts',(28.4659385855046,22.2768897238054,38.8821385936306));
#64710=CARTESIAN_POINT('Ctrl Pts',(28.422594285554,22.2229477866579,38.8865423155661));
#64711=CARTESIAN_POINT('Ctrl Pts',(28.3821406240037,22.1668584327162,38.8909460375015));
#64712=CARTESIAN_POINT('Ctrl Pts',(28.3417112466882,22.1108027490774,38.8953471158933));
#64713=CARTESIAN_POINT('Ctrl Pts',(28.3041693581068,22.0526026086582,38.8997481942851));
#64714=CARTESIAN_POINT('Ctrl Pts',(28.2697438215374,21.9925931288257,38.9041492726769));
#64715=CARTESIAN_POINT('Ctrl Pts',(28.2353267479062,21.9325984013129,38.9085492691378));
#64716=CARTESIAN_POINT('Ctrl Pts',(28.2040247535269,21.8707956500677,38.9129492655986));
#64717=CARTESIAN_POINT('Ctrl Pts',(28.1760219557701,21.8075466900851,38.9173492620595));
#64718=CARTESIAN_POINT('Ctrl Pts',(28.1478570483352,21.7439315785259,38.9217747303327));
#64719=CARTESIAN_POINT('Ctrl Pts',(28.1230298891774,21.6788539153757,38.9262001986059));
#64720=CARTESIAN_POINT('Ctrl Pts',(28.1016788534891,21.6127025275038,38.9306256668791));
#64721=CARTESIAN_POINT('Ctrl Pts',(28.0804264062742,21.5468565938703,38.9350307005389));
#64722=CARTESIAN_POINT('Ctrl Pts',(28.0626181345658,21.4799473286767,38.9394357341986));
#64723=CARTESIAN_POINT('Ctrl Pts',(28.0483398485905,21.412371453789,38.9438407678584));
#64724=CARTESIAN_POINT('Ctrl Pts',(28.033962208804,21.3443253599466,38.9482764534383));
#64725=CARTESIAN_POINT('Ctrl Pts',(28.0231639545741,21.2756038496504,38.9527121390182));
#64726=CARTESIAN_POINT('Ctrl Pts',(28.0159796898694,21.2066179360303,38.9571478245982));
#64727=CARTESIAN_POINT('Ctrl Pts',(28.0087954251648,21.1376320224102,38.9615835101781));
#64728=CARTESIAN_POINT('Ctrl Pts',(28.0052251117498,21.0683822176057,38.966019195758));
#64729=CARTESIAN_POINT('Ctrl Pts',(28.0052501307333,20.9992778085393,38.970454881338));
#64730=CARTESIAN_POINT('Ctrl Pts',(28.0052501307336,20.9992778076475,38.9704548813952));
#64731=CARTESIAN_POINT('Ctrl Pts',(28.0052646428238,20.9591943177361,38.9730277672733));
#64732=CARTESIAN_POINT('Ctrl Pts',(28.0064872516091,20.9191342037145,38.9756006531513));
#64733=CARTESIAN_POINT('Ctrl Pts',(28.0089142811437,20.8791479306482,38.9781735390294));
#64734=CARTESIAN_POINT('Ctrl Pts',(28.013116765964,20.8099103283949,38.982628579107));
#64735=CARTESIAN_POINT('Ctrl Pts',(28.0209433109417,20.7407558325127,38.9870836191846));
#64736=CARTESIAN_POINT('Ctrl Pts',(28.0323858767816,20.6720941833217,38.9915386592623));
#64737=CARTESIAN_POINT('Ctrl Pts',(28.0438113043172,20.603535373324,38.9959870267253));
#64738=CARTESIAN_POINT('Ctrl Pts',(28.0588419233784,20.5354684236485,39.0004353941882));
#64739=CARTESIAN_POINT('Ctrl Pts',(28.0774177922863,20.4682996924181,39.0048837616512));
#64740=CARTESIAN_POINT('Ctrl Pts',(28.0959718697999,20.4012097569798,39.0093269107241));
#64741=CARTESIAN_POINT('Ctrl Pts',(28.118062807048,20.3350164165094,39.0137700597971));
#64742=CARTESIAN_POINT('Ctrl Pts',(28.1435796335573,20.2701157724975,39.01821320887));
#64743=CARTESIAN_POINT('Ctrl Pts',(28.1690804603916,20.205255822779,39.0226535719796));
#64744=CARTESIAN_POINT('Ctrl Pts',(28.1980027363842,20.1416874158493,39.0270939350893));
#64745=CARTESIAN_POINT('Ctrl Pts',(28.2301861559739,20.0797899587629,39.0315342981989));
#64746=CARTESIAN_POINT('Ctrl Pts',(28.2623603173653,20.0179103077064,39.0359733839502));
#64747=CARTESIAN_POINT('Ctrl Pts',(28.2977935343363,19.9577010861296,39.0404124697014));
#64748=CARTESIAN_POINT('Ctrl Pts',(28.3362787869917,19.8995186108406,39.0448515554526));
#64749=CARTESIAN_POINT('Ctrl Pts',(28.3747660283493,19.8413331290073,39.0492908705909));
#64750=CARTESIAN_POINT('Ctrl Pts',(28.4163053465543,19.7851750081495,39.0537301857292));
#64751=CARTESIAN_POINT('Ctrl Pts',(28.4606464741506,19.7313714945047,39.0581695008675));
#64752=CARTESIAN_POINT('Ctrl Pts',(28.505034460367,19.6775111226217,39.0626135073655));
#64753=CARTESIAN_POINT('Ctrl Pts',(28.5522298537989,19.6260107026534,39.0670575138636));
#64754=CARTESIAN_POINT('Ctrl Pts',(28.6019427969031,19.5771635303491,39.0715015203616));
#64755=CARTESIAN_POINT('Ctrl Pts',(28.6516848577964,19.5282877473535,39.0759481297963));
#64756=CARTESIAN_POINT('Ctrl Pts',(28.7039470367298,19.4820686294349,39.0803947392311));
#64757=CARTESIAN_POINT('Ctrl Pts',(28.7584054791707,19.4387599132912,39.0848413486658));
#64758=CARTESIAN_POINT('Ctrl Pts',(28.8129582608405,19.3953761727673,39.0892956610331));
#64759=CARTESIAN_POINT('Ctrl Pts',(28.86971450213,19.3549131818436,39.0937499734003));
#64760=CARTESIAN_POINT('Ctrl Pts',(28.9283210888019,19.3175815402245,39.0982042857675));
#64761=CARTESIAN_POINT('Ctrl Pts',(28.9585829064826,19.2983051517407,39.1005042932651));
#64762=CARTESIAN_POINT('Ctrl Pts',(28.9893376579779,19.2798629034819,39.1028043007626));
#64763=CARTESIAN_POINT('Ctrl Pts',(29.0205344389625,19.262278855155,39.1051043082601));
#64764=CARTESIAN_POINT('Ctrl Pts',(29.0809615938137,19.2282191227843,39.109559348326));
#64765=CARTESIAN_POINT('Ctrl Pts',(29.1432864519631,19.1972479889171,39.1140143883918));
#64766=CARTESIAN_POINT('Ctrl Pts',(29.2071605495953,19.1695811494683,39.1184694284577));
#64767=CARTESIAN_POINT('Ctrl Pts',(29.2709389786676,19.1419557485177,39.1229177959085));
#64768=CARTESIAN_POINT('Ctrl Pts',(29.3362615963458,19.1176250120267,39.1273661633593));
#64769=CARTESIAN_POINT('Ctrl Pts',(29.4027546014648,19.0967592121782,39.13181453081));
#64770=CARTESIAN_POINT('Ctrl Pts',(29.4691696034795,19.0759178900498,39.1362576798703));
#64771=CARTESIAN_POINT('Ctrl Pts',(29.5367518013512,19.0585335771767,39.1407008289305));
#64772=CARTESIAN_POINT('Ctrl Pts',(29.6051083039763,19.0447281235308,39.1451439779907));
#64773=CARTESIAN_POINT('Ctrl Pts',(29.6734219453948,19.0309313262434,39.1495843410873));
#64774=CARTESIAN_POINT('Ctrl Pts',(29.7425084498925,19.0207090330657,39.1540247041839));
#64775=CARTESIAN_POINT('Ctrl Pts',(29.8119621623945,19.0141325990569,39.1584650672805));
#64776=CARTESIAN_POINT('Ctrl Pts',(29.881395895155,19.0075580568901,39.1629041530183));
#64777=CARTESIAN_POINT('Ctrl Pts',(29.9511961393392,19.0046273378733,39.1673432387562));
#64778=CARTESIAN_POINT('Ctrl Pts',(30.0209512698956,19.0053600307851,39.171782324494));
#64779=CARTESIAN_POINT('Ctrl Pts',(30.0907100050019,19.0060927615582,39.1762216396187));
#64780=CARTESIAN_POINT('Ctrl Pts',(30.1604231326141,19.0104892725408,39.1806609547433));
#64781=CARTESIAN_POINT('Ctrl Pts',(30.2296799620765,19.0185170509135,39.185100269868));
#64782=CARTESIAN_POINT('Ctrl Pts',(30.2990099804584,19.0265533128455,39.1895442763521));
#64783=CARTESIAN_POINT('Ctrl Pts',(30.3678822512674,19.0382284448406,39.1939882828361));
#64784=CARTESIAN_POINT('Ctrl Pts',(30.4358931020272,19.0534582547232,39.1984322893201));
#64785=CARTESIAN_POINT('Ctrl Pts',(30.5039437879954,19.0686969849862,39.2028788987407));
#64786=CARTESIAN_POINT('Ctrl Pts',(30.5711315783388,19.0874944053553,39.2073255081612));
#64787=CARTESIAN_POINT('Ctrl Pts',(30.6370675653063,19.1097162964955,39.2117721175817));
#64788=CARTESIAN_POINT('Ctrl Pts',(30.7031177742337,19.1319766829715,39.2162264299346));
#64789=CARTESIAN_POINT('Ctrl Pts',(30.7679113964543,19.1576732013188,39.2206807422874));
#64790=CARTESIAN_POINT('Ctrl Pts',(30.8310798655559,19.1866236409483,39.2251350546402));
#64791=CARTESIAN_POINT('Ctrl Pts',(30.8636972368969,19.2015723527552,39.2274350622571));
#64792=CARTESIAN_POINT('Ctrl Pts',(30.8958817114017,19.2173878829902,39.229735069874));
#64793=CARTESIAN_POINT('Ctrl Pts',(30.9275854478883,19.2340405442463,39.2320350774909));
#64794=CARTESIAN_POINT('Ctrl Pts',(30.9889945562375,19.2662962084899,39.2364901175777));
#64795=CARTESIAN_POINT('Ctrl Pts',(31.0488401240088,19.3018223558264,39.2409451576645));
#64796=CARTESIAN_POINT('Ctrl Pts',(31.1067518297036,19.3404434478006,39.2454001977513));
#64797=CARTESIAN_POINT('Ctrl Pts',(31.1645767971218,19.3790066943546,39.2498485652234));
#64798=CARTESIAN_POINT('Ctrl Pts',(31.2204732475762,19.4206554157403,39.2542969326955));
#64799=CARTESIAN_POINT('Ctrl Pts',(31.2740952507473,19.4651681347707,39.2587453001676));
#64800=CARTESIAN_POINT('Ctrl Pts',(31.3276543498231,19.509628635828,39.2631884492496));
#64801=CARTESIAN_POINT('Ctrl Pts',(31.3789439263179,19.5569461504788,39.2676315983316));
#64802=CARTESIAN_POINT('Ctrl Pts',(31.427648350918,19.606856881501,39.2720747474136));
#64803=CARTESIAN_POINT('Ctrl Pts',(31.4763222366504,19.6567363172717,39.2765151105322));
#64804=CARTESIAN_POINT('Ctrl Pts',(31.5224138452266,19.7092053943128,39.2809554736508));
#64805=CARTESIAN_POINT('Ctrl Pts',(31.5656430233468,19.7639621826394,39.2853958367694));
#64806=CARTESIAN_POINT('Ctrl Pts',(31.6088597657366,19.81870321909,39.2898349225296));
#64807=CARTESIAN_POINT('Ctrl Pts',(31.6492154093433,19.8757302764879,39.2942740082897));
#64808=CARTESIAN_POINT('Ctrl Pts',(31.6864700330219,19.9347083074485,39.2987130940498));
#64809=CARTESIAN_POINT('Ctrl Pts',(31.7237265818099,19.9936893860621,39.3031524091969));
#64810=CARTESIAN_POINT('Ctrl Pts',(31.7578815332684,20.0546212234293,39.307591724344));
#64811=CARTESIAN_POINT('Ctrl Pts',(31.7887392283771,20.1171412710037,39.3120310394912));
#64812=CARTESIAN_POINT('Ctrl Pts',(31.8196295331424,20.1797273882334,39.3164750459978));
#64813=CARTESIAN_POINT('Ctrl Pts',(31.8472154099551,20.2439046259247,39.3209190525045));
#64814=CARTESIAN_POINT('Ctrl Pts',(31.8713484101972,20.309288272756,39.3253630590111));
#64815=CARTESIAN_POINT('Ctrl Pts',(31.8954955455828,20.3747102159956,39.3298096684544));
#64816=CARTESIAN_POINT('Ctrl Pts',(31.9161856338551,20.4413395074155,39.3342562778977));
#64817=CARTESIAN_POINT('Ctrl Pts',(31.9333202548722,20.5087766754307,39.3387028873409));
#64818=CARTESIAN_POINT('Ctrl Pts',(31.9504845584657,20.5763306659243,39.3431571997164));
#64819=CARTESIAN_POINT('Ctrl Pts',(31.964081004968,20.6446948467698,39.3476115120919));
#64820=CARTESIAN_POINT('Ctrl Pts',(31.9740625204969,20.7134607746408,39.3520658244674));
#64821=CARTESIAN_POINT('Ctrl Pts',(31.9792165280798,20.7489684200146,39.3543658318855));
#64822=CARTESIAN_POINT('Ctrl Pts',(31.9834075640945,20.7845831134649,39.3566658393035));
#64823=CARTESIAN_POINT('Ctrl Pts',(31.986634587087,20.820248560813,39.3589658467216));
#64824=CARTESIAN_POINT('Ctrl Pts',(31.9928852263902,20.8893313803301,39.3634208868));
#64825=CARTESIAN_POINT('Ctrl Pts',(31.9955404755269,20.9588766803797,39.3678759268784));
#64826=CARTESIAN_POINT('Ctrl Pts',(31.9945467045323,21.028478166011,39.3723309669568));
#64827=CARTESIAN_POINT('Ctrl Pts',(31.9935544219757,21.0979754047903,39.3767793344204));
#64828=CARTESIAN_POINT('Ctrl Pts',(31.9889239738688,21.1675281768276,39.381227701884));
#64829=CARTESIAN_POINT('Ctrl Pts',(31.9806535514527,21.2367257307899,39.3856760693476));
#64830=CARTESIAN_POINT('Ctrl Pts',(31.9723928310883,21.3058421089405,39.390119218421));
#64831=CARTESIAN_POINT('Ctrl Pts',(31.9605006752226,21.3746036131444,39.3945623674944));
#64832=CARTESIAN_POINT('Ctrl Pts',(31.9450272657607,21.4426019633345,39.3990055165678));
#64833=CARTESIAN_POINT('Ctrl Pts',(31.9295635585059,21.5105576768917,39.4034458796777));
#64834=CARTESIAN_POINT('Ctrl Pts',(31.91052316071,21.5777507097199,39.4078862427877));
#64835=CARTESIAN_POINT('Ctrl Pts',(31.88800753798,21.6437818722445,39.4123266058976));
#64836=CARTESIAN_POINT('Ctrl Pts',(31.8654983923157,21.7097940395949,39.416765691649));
#64837=CARTESIAN_POINT('Ctrl Pts',(31.8395161642236,21.7746445372969,39.4212047774004));
#64838=CARTESIAN_POINT('Ctrl Pts',(31.8102119732197,21.8379499832998,39.4256438631518));
#64839=CARTESIAN_POINT('Ctrl Pts',(31.7809062679401,21.9012587005718,39.4300831782902));
#64840=CARTESIAN_POINT('Ctrl Pts',(31.7482784666747,21.9630217646245,39.4345224934285));
#64841=CARTESIAN_POINT('Ctrl Pts',(31.7125268142031,22.0228780343401,39.4389618085669));
#64842=CARTESIAN_POINT('Ctrl Pts',(31.6767373802605,22.082797558696,39.4434058150648));
#64843=CARTESIAN_POINT('Ctrl Pts',(31.6378177576339,22.1408058459857,39.4478498215627));
#64844=CARTESIAN_POINT('Ctrl Pts',(31.5960104338124,22.1965693701837,39.4522938280606));
#64845=CARTESIAN_POINT('Ctrl Pts',(31.5541786226701,22.2523655561066,39.4567404374951));
#64846=CARTESIAN_POINT('Ctrl Pts',(31.509456057548,22.3059139863257,39.4611870469296));
#64847=CARTESIAN_POINT('Ctrl Pts',(31.4621247819541,22.3569151353329,39.4656336563641));
#64848=CARTESIAN_POINT('Ctrl Pts',(31.414711513638,22.4080046344426,39.470087968731));
#64849=CARTESIAN_POINT('Ctrl Pts',(31.3646808653404,22.4565377035091,39.4745422810978));
#64850=CARTESIAN_POINT('Ctrl Pts',(31.3123502908188,22.5022530667927,39.4789965934646));
#64851=CARTESIAN_POINT('Ctrl Pts',(31.2853291248666,22.5258584338107,39.4812966009605));
#64852=CARTESIAN_POINT('Ctrl Pts',(31.2576952644839,22.5487132149282,39.4835966084565));
#64853=CARTESIAN_POINT('Ctrl Pts',(31.2294954200378,22.5707859735196,39.4858966159524));
#64854=CARTESIAN_POINT('Ctrl Pts',(31.1748732340598,22.6135401925059,39.4903516560302));
#64855=CARTESIAN_POINT('Ctrl Pts',(31.1179107266147,22.6535260881525,39.4948066961079));
#64856=CARTESIAN_POINT('Ctrl Pts',(31.0589199879724,22.6904780452797,39.4992617361857));
#64857=CARTESIAN_POINT('Ctrl Pts',(31.0000176037491,22.7273746569614,39.5037101036486));
#64858=CARTESIAN_POINT('Ctrl Pts',(30.9390934290822,22.7612460916392,39.5081584711115));
#64859=CARTESIAN_POINT('Ctrl Pts',(30.8764914303458,22.7918678341413,39.5126068385744));
#64860=CARTESIAN_POINT('Ctrl Pts',(30.8139628701606,22.8224536542057,39.5170499876471));
#64861=CARTESIAN_POINT('Ctrl Pts',(30.7497608326115,22.8497971397991,39.5214931367197));
#64862=CARTESIAN_POINT('Ctrl Pts',(30.6842554343482,22.8737187790768,39.5259362857923));
#64863=CARTESIAN_POINT('Ctrl Pts',(30.6187911095762,22.8976254188999,39.5303766489015));
#64864=CARTESIAN_POINT('Ctrl Pts',(30.5520255039005,22.9181143013995,39.5348170120107));
#64865=CARTESIAN_POINT('Ctrl Pts',(30.4843489416209,22.9350539179182,39.5392573751199));
#64866=CARTESIAN_POINT('Ctrl Pts',(30.4166918478479,22.95198866142,39.5436964608705));
#64867=CARTESIAN_POINT('Ctrl Pts',(30.3481247921238,22.9653760471501,39.5481355466211));
#64868=CARTESIAN_POINT('Ctrl Pts',(30.2790517806338,22.9751348476054,39.5525746323717));
#64869=CARTESIAN_POINT('Ctrl Pts',(30.2099751998398,22.9848941523405,39.5570139475092));
#64870=CARTESIAN_POINT('Ctrl Pts',(30.14039309619,22.9910244334813,39.5614532626468));
#64871=CARTESIAN_POINT('Ctrl Pts',(30.0707163821908,22.9934961138136,39.5658925777843));
#64872=CARTESIAN_POINT('Ctrl Pts',(30.0009660355468,22.9959704061571,39.5703365842813));
#64873=CARTESIAN_POINT('Ctrl Pts',(29.931121368945,22.9947783635379,39.5747805907784));
#64874=CARTESIAN_POINT('Ctrl Pts',(29.8615941230685,22.9899425558872,39.5792245972754));
#64875=CARTESIAN_POINT('Ctrl Pts',(29.7920261538018,22.9851039158148,39.583671206709));
#64876=CARTESIAN_POINT('Ctrl Pts',(29.7227764611,22.9766173223029,39.5881178161426));
#64877=CARTESIAN_POINT('Ctrl Pts',(29.6542497069565,22.9645570231888,39.5925644255762));
#64878=CARTESIAN_POINT('Ctrl Pts',(29.5856042428263,22.9524758318266,39.5970187379421));
#64879=CARTESIAN_POINT('Ctrl Pts',(29.5176846937674,22.9368086873366,39.601473050308));
#64880=CARTESIAN_POINT('Ctrl Pts',(29.4508828238384,22.9176803407618,39.6059273626739));
#64881=CARTESIAN_POINT('Ctrl Pts',(29.4163893286731,22.907803318894,39.608227370177));
#64882=CARTESIAN_POINT('Ctrl Pts',(29.3821935436789,22.8970042653971,39.6105273776801));
#64883=CARTESIAN_POINT('Ctrl Pts',(29.3483472282633,22.8853053406777,39.6128273851832));
#64884=CARTESIAN_POINT('Ctrl Pts',(29.2828030888582,22.8626501138596,39.6172814006518));
#64885=CARTESIAN_POINT('Ctrl Pts',(29.2183127414046,22.8365281678362,39.6217354161204));
#64886=CARTESIAN_POINT('Ctrl Pts',(29.1552684130968,22.8070573063929,39.626189431589));
#64887=CARTESIAN_POINT('Ctrl Pts',(29.112303123076,22.7869726430606,39.6292248841269));
#64888=CARTESIAN_POINT('Ctrl Pts',(29.0700092676253,22.7653336290579,39.6322603366649));
#64889=CARTESIAN_POINT('Ctrl Pts',(29.0285070491141,22.7421908646526,39.6352957892028));
#64890=CARTESIAN_POINT('Origin',(30.,21.,34.5704548813952));
#64891=CARTESIAN_POINT('',(29.0285071367644,22.7421909135288,40.592474930186));
#64892=CARTESIAN_POINT('',(29.0285070491141,22.7421908646526,40.4352302045579));
#64893=CARTESIAN_POINT('',(29.0285070491141,22.7421908646526,34.5704548813952));
#64894=CARTESIAN_POINT('',(28.0052502116719,20.9990810521211,39.9301166301426));
#64895=CARTESIAN_POINT('Ctrl Pts',(29.0285071367644,22.7421909135288,40.592474930186));
#64896=CARTESIAN_POINT('Ctrl Pts',(29.0960687329284,22.7798650903325,40.5879600119655));
#64897=CARTESIAN_POINT('Ctrl Pts',(29.1657938625114,22.8135936960508,40.5835015453423));
#64898=CARTESIAN_POINT('Ctrl Pts',(29.3247841510807,22.879379618777,40.5734612728819));
#64899=CARTESIAN_POINT('Ctrl Pts',(29.4146880486724,22.9092907596867,40.5678627366657));
#64900=CARTESIAN_POINT('Ctrl Pts',(29.5329960975536,22.9395077127843,40.5603706304539));
#64901=CARTESIAN_POINT('Ctrl Pts',(29.5597597683602,22.9457572400108,40.5586683913905));
#64902=CARTESIAN_POINT('Ctrl Pts',(29.6043568641948,22.9552038078342,40.5558153011756));
#64903=CARTESIAN_POINT('Ctrl Pts',(29.6221204769607,22.958714489749,40.5546745677748));
#64904=CARTESIAN_POINT('Ctrl Pts',(29.6573621342639,22.9651821816829,40.5524017752951));
#64905=CARTESIAN_POINT('Ctrl Pts',(29.6748366922898,22.9681490045451,40.5512701446101));
#64906=CARTESIAN_POINT('Ctrl Pts',(29.7175143111167,22.974810920883,40.5484940314886));
#64907=CARTESIAN_POINT('Ctrl Pts',(29.7427525223607,22.9782568016268,40.5468418447261));
#64908=CARTESIAN_POINT('Ctrl Pts',(29.8427293246642,22.9899615858731,40.5402527064019));
#64909=CARTESIAN_POINT('Ctrl Pts',(29.9178357607172,22.9944743417707,40.5352020751141));
#64910=CARTESIAN_POINT('Ctrl Pts',(30.1669081109147,22.9953470928876,40.5181527011763));
#64911=CARTESIAN_POINT('Ctrl Pts',(30.3401244480812,22.9732154522397,40.5057420662623));
#64912=CARTESIAN_POINT('Ctrl Pts',(30.5321243766572,22.9226231325099,40.4924105970826));
#64913=CARTESIAN_POINT('Ctrl Pts',(30.5558605981998,22.9158954009407,40.4907718030728));
#64914=CARTESIAN_POINT('Ctrl Pts',(30.590924269536,22.9052504912435,40.4883709020529));
#64915=CARTESIAN_POINT('Ctrl Pts',(30.6023502095324,22.9016690483001,40.4875917246693));
#64916=CARTESIAN_POINT('Ctrl Pts',(30.6220567253492,22.8952966333065,40.4862542248366));
#64917=CARTESIAN_POINT('Ctrl Pts',(30.6303519883818,22.8925539028408,40.4856932388778));
#64918=CARTESIAN_POINT('Ctrl Pts',(30.6501852574323,22.8858513939182,40.4843567110806));
#64919=CARTESIAN_POINT('Ctrl Pts',(30.6617053213933,22.8818401724716,40.4835841585812));
#64920=CARTESIAN_POINT('Ctrl Pts',(30.6975577794693,22.868986600885,40.4811894916869));
#64921=CARTESIAN_POINT('Ctrl Pts',(30.7217562832923,22.8597757344726,40.4795871810929));
#64922=CARTESIAN_POINT('Ctrl Pts',(30.7799113448541,22.8363335475747,40.4757547316584));
#64923=CARTESIAN_POINT('Ctrl Pts',(30.8136672007711,22.8216280035967,40.4735455508008));
#64924=CARTESIAN_POINT('Ctrl Pts',(30.9633523573462,22.7514267949069,40.4637372845584));
#64925=CARTESIAN_POINT('Ctrl Pts',(31.0741638298145,22.6857397442724,40.4564246481082));
#64926=CARTESIAN_POINT('Ctrl Pts',(31.2417254070379,22.5631385717563,40.4442369430036));
#64927=CARTESIAN_POINT('Ctrl Pts',(31.3027207039125,22.5126800779375,40.4395215207509));
#64928=CARTESIAN_POINT('Ctrl Pts',(31.3800497389339,22.4405557518614,40.4330253376262));
#64929=CARTESIAN_POINT('Ctrl Pts',(31.3991764833804,22.421985660879,40.4313725361311));
#64930=CARTESIAN_POINT('Ctrl Pts',(31.4292871360043,22.3915555359962,40.4286914046391));
#64931=CARTESIAN_POINT('Ctrl Pts',(31.440509390113,22.3799352155775,40.4276736852452));
#64932=CARTESIAN_POINT('Ctrl Pts',(31.463639712474,22.3553947909158,40.4255361669615));
#64933=CARTESIAN_POINT('Ctrl Pts',(31.4755206409163,22.3424511361077,40.4244153336846));
#64934=CARTESIAN_POINT('Ctrl Pts',(31.5036181893569,22.311016674992,40.421707932134));
#64935=CARTESIAN_POINT('Ctrl Pts',(31.5196665051278,22.2923799769558,40.4201145510715));
#64936=CARTESIAN_POINT('Ctrl Pts',(31.5780877378331,22.2219431253007,40.4141328358146));
#64937=CARTESIAN_POINT('Ctrl Pts',(31.6181863326005,22.1683224023332,40.4096564473149));
#64938=CARTESIAN_POINT('Ctrl Pts',(31.725666617251,22.0084230824251,40.3965331214788));
#64939=CARTESIAN_POINT('Ctrl Pts',(31.7857908214355,21.8976574936066,40.3876913783191));
#64940=CARTESIAN_POINT('Ctrl Pts',(31.8629083714837,21.7166854304469,40.3740427701163));
#64941=CARTESIAN_POINT('Ctrl Pts',(31.8872314312267,21.6499423692024,40.3691707287951));
#64942=CARTESIAN_POINT('Ctrl Pts',(31.9129709497089,21.5655672104859,40.3633167114285));
#64943=CARTESIAN_POINT('Ctrl Pts',(31.9177824672936,21.5490305822521,40.362183684447));
#64944=CARTESIAN_POINT('Ctrl Pts',(31.925172600491,21.5223480921013,40.3603806678989));
#64945=CARTESIAN_POINT('Ctrl Pts',(31.9278864647504,21.5122410195493,40.359703461862));
#64946=CARTESIAN_POINT('Ctrl Pts',(31.933093199993,21.4922221896989,40.3583741372569));
#64947=CARTESIAN_POINT('Ctrl Pts',(31.9355896658313,21.4823117847147,40.3577218557724));
#64948=CARTESIAN_POINT('Ctrl Pts',(31.9418143625754,21.4567741626826,40.3560549040052));
#64949=CARTESIAN_POINT('Ctrl Pts',(31.9454302644967,21.4411199148273,40.3550463887352));
#64950=CARTESIAN_POINT('Ctrl Pts',(31.961094679351,21.3693614687676,40.3504769146551));
#64951=CARTESIAN_POINT('Ctrl Pts',(31.9709090000554,21.3127925244291,40.3470233104871));
#64952=CARTESIAN_POINT('Ctrl Pts',(31.9974623778437,21.1074972505957,40.3347712016247));
#64953=CARTESIAN_POINT('Ctrl Pts',(31.9999006372939,20.9574316356273,40.3263066742011));
#64954=CARTESIAN_POINT('Ctrl Pts',(31.9798064399963,20.7490886013524,40.3138780160435));
#64955=CARTESIAN_POINT('Ctrl Pts',(31.9714132188086,20.6899693042299,40.3102790028381));
#64956=CARTESIAN_POINT('Ctrl Pts',(31.9558918794299,20.6074379231036,40.3051002091521));
#64957=CARTESIAN_POINT('Ctrl Pts',(31.9509648783114,20.5836419913619,40.3035888610824));
#64958=CARTESIAN_POINT('Ctrl Pts',(31.9417395168266,20.542854328133,40.3009639463476));
#64959=CARTESIAN_POINT('Ctrl Pts',(31.9376495846089,20.525817996923,40.2998571460824));
#64960=CARTESIAN_POINT('Ctrl Pts',(31.9287980722794,20.4909762286221,40.2975711058046));
#64961=CARTESIAN_POINT('Ctrl Pts',(31.9240130756965,20.4731785404145,40.2963912014753));
#64962=CARTESIAN_POINT('Ctrl Pts',(31.9110386121741,20.4274567988189,40.2933274612075));
#64963=CARTESIAN_POINT('Ctrl Pts',(31.9024837135227,20.3996418851171,40.2914319399806));
#64964=CARTESIAN_POINT('Ctrl Pts',(31.8549392864333,20.2562969623157,40.2814929830942));
#64965=CARTESIAN_POINT('Ctrl Pts',(31.8060310704993,20.1443499242521,40.2731275645003));
#64966=CARTESIAN_POINT('Ctrl Pts',(31.6862794250549,19.9269465798762,40.2558454622255));
#64967=CARTESIAN_POINT('Ctrl Pts',(31.6149634027058,19.8223415627265,40.2469606497743));
#64968=CARTESIAN_POINT('Ctrl Pts',(31.5213539423238,19.7096839120542,40.2371868425998));
#64969=CARTESIAN_POINT('Ctrl Pts',(31.5082442616112,19.6943841506517,40.2358551510203));
#64970=CARTESIAN_POINT('Ctrl Pts',(31.4874894521765,19.6708919847042,40.2338070412667));
#64971=CARTESIAN_POINT('Ctrl Pts',(31.4800036834338,19.662561366562,40.2330800831842));
#64972=CARTESIAN_POINT('Ctrl Pts',(31.4658097940107,19.6470306613671,40.2317242908243));
#64973=CARTESIAN_POINT('Ctrl Pts',(31.4591182800737,19.6398168388623,40.2310944118102));
#64974=CARTESIAN_POINT('Ctrl Pts',(31.4427899530334,19.6224731689399,40.2295790970551));
#64975=CARTESIAN_POINT('Ctrl Pts',(31.4330995722738,19.61239463057,40.2286976836892));
#64976=CARTESIAN_POINT('Ctrl Pts',(31.3971688175285,19.5758025783677,40.2254906065939));
#64977=CARTESIAN_POINT('Ctrl Pts',(31.3702906264709,19.5499231089544,40.2232087841669));
#64978=CARTESIAN_POINT('Ctrl Pts',(31.2959178956472,19.4822298783655,40.2171502537228));
#64979=CARTESIAN_POINT('Ctrl Pts',(31.2471330798358,19.4418955730976,40.2134408174098));
#64980=CARTESIAN_POINT('Ctrl Pts',(31.0696822991831,19.3088663539484,40.2005288783621));
#64981=CARTESIAN_POINT('Ctrl Pts',(30.9319860950049,19.2292513045153,40.1914610929956));
#64982=CARTESIAN_POINT('Ctrl Pts',(30.7587912730339,19.1549631985256,40.1799381376238));
#64983=CARTESIAN_POINT('Ctrl Pts',(30.7309985141636,19.1437764086102,40.1780877469968));
#64984=CARTESIAN_POINT('Ctrl Pts',(30.6855559610989,19.1266642968388,40.1750543717657));
#64985=CARTESIAN_POINT('Ctrl Pts',(30.6680560836306,19.1203525160011,40.1738843807477));
#64986=CARTESIAN_POINT('Ctrl Pts',(30.6339863597613,19.1086002712322,40.1716017591842));
#64987=CARTESIAN_POINT('Ctrl Pts',(30.6174283629187,19.103130520251,40.1704902239753));
#64988=CARTESIAN_POINT('Ctrl Pts',(30.5781183392696,19.0907141146697,40.1678452584596));
#64989=CARTESIAN_POINT('Ctrl Pts',(30.5553099898122,19.0839561226298,40.1663058125653));
#64990=CARTESIAN_POINT('Ctrl Pts',(30.4742205382256,19.0614992202077,40.1608134534591));
#64991=CARTESIAN_POINT('Ctrl Pts',(30.4153584522196,19.0480403421593,40.1567904937402));
#64992=CARTESIAN_POINT('Ctrl Pts',(30.2554872697765,19.0190443869337,40.1457719792754));
#64993=CARTESIAN_POINT('Ctrl Pts',(30.1537492991613,19.0085641626037,40.1386556363141));
#64994=CARTESIAN_POINT('Ctrl Pts',(29.9570826895674,19.0034685850981,40.1249336148917));
#64995=CARTESIAN_POINT('Ctrl Pts',(29.8624366157282,19.0077502916956,40.1183482940853));
#64996=CARTESIAN_POINT('Ctrl Pts',(29.7468143079319,19.0212633166416,40.1105608703395));
#64997=CARTESIAN_POINT('Ctrl Pts',(29.7252250232875,19.0241455871365,40.1091182523118));
#64998=CARTESIAN_POINT('Ctrl Pts',(29.6922675017215,19.0290962473652,40.1069378922821));
#64999=CARTESIAN_POINT('Ctrl Pts',(29.6808635097747,19.0309106650382,40.1061874755816));
#65000=CARTESIAN_POINT('Ctrl Pts',(29.660818549599,19.0342786143093,40.1048763293535));
#65001=CARTESIAN_POINT('Ctrl Pts',(29.6521714935312,19.0357902462071,40.1043133769416));
#65002=CARTESIAN_POINT('Ctrl Pts',(29.6310150410694,19.0396327993481,40.1029422502506));
#65003=CARTESIAN_POINT('Ctrl Pts',(29.6185175567197,19.0420263977322,40.1021375686636));
#65004=CARTESIAN_POINT('Ctrl Pts',(29.5777000507225,19.0502496904801,40.0995241565624));
#65005=CARTESIAN_POINT('Ctrl Pts',(29.5494824784796,19.0565757860059,40.0977407422773));
#65006=CARTESIAN_POINT('Ctrl Pts',(29.4796241136988,19.0738407955747,40.0933611912371));
#65007=CARTESIAN_POINT('Ctrl Pts',(29.4381801580459,19.0855185468424,40.0907948025244));
#65008=CARTESIAN_POINT('Ctrl Pts',(29.2422551456768,19.1476359782371,40.0786779397923));
#65009=CARTESIAN_POINT('Ctrl Pts',(29.0939500578891,19.2154818238749,40.0694995621531));
#65010=CARTESIAN_POINT('Ctrl Pts',(28.9158107052753,19.3249677977458,40.0569433889924));
#65011=CARTESIAN_POINT('Ctrl Pts',(28.87697787,19.3507516555636,40.0541058904729));
#65012=CARTESIAN_POINT('Ctrl Pts',(28.8214012657796,19.390526329014,40.049870962468));
#65013=CARTESIAN_POINT('Ctrl Pts',(28.8039257224924,19.4034704080505,40.0485129378575));
#65014=CARTESIAN_POINT('Ctrl Pts',(28.773028841815,19.4271476489753,40.0460620374657));
#65015=CARTESIAN_POINT('Ctrl Pts',(28.7595278143415,19.4377735543045,40.0449734517593));
#65016=CARTESIAN_POINT('Ctrl Pts',(28.7309210098843,19.460893021243,40.0426278421931));
#65017=CARTESIAN_POINT('Ctrl Pts',(28.7158588605419,19.4734374353878,40.0413688306624));
#65018=CARTESIAN_POINT('Ctrl Pts',(28.6744922139242,19.5089348375416,40.0378422189949));
#65019=CARTESIAN_POINT('Ctrl Pts',(28.6486027938534,19.5323585085854,40.0355554233331));
#65020=CARTESIAN_POINT('Ctrl Pts',(28.5912097710309,19.5870919327397,40.0302981622785));
#65021=CARTESIAN_POINT('Ctrl Pts',(28.5601111979405,19.6187980287938,40.0273122730739));
#65022=CARTESIAN_POINT('Ctrl Pts',(28.4492410694052,19.7396507084203,40.0161521445457));
#65023=CARTESIAN_POINT('Ctrl Pts',(28.3764799802037,19.8348768043067,40.0077611379531));
#65024=CARTESIAN_POINT('Ctrl Pts',(28.2708359236142,20.0024142243903,39.9939901212667));
#65025=CARTESIAN_POINT('Ctrl Pts',(28.2329283045117,20.0712127072359,39.988583916848));
#65026=CARTESIAN_POINT('Ctrl Pts',(28.191628135908,20.1579036356095,39.9822076652887));
#65027=CARTESIAN_POINT('Ctrl Pts',(28.1842946609797,20.1738346060227,39.9810533137794));
#65028=CARTESIAN_POINT('Ctrl Pts',(28.1728944992523,20.1994851808,39.9792247396629));
#65029=CARTESIAN_POINT('Ctrl Pts',(28.1686932279146,20.209143498844,39.9785429521871));
#65030=CARTESIAN_POINT('Ctrl Pts',(28.1605872142881,20.2281894502355,39.9772123215074));
#65031=CARTESIAN_POINT('Ctrl Pts',(28.1566774032896,20.2375744414096,39.9765632234225));
#65032=CARTESIAN_POINT('Ctrl Pts',(28.1468729834634,20.261625005888,39.9749155620193));
#65033=CARTESIAN_POINT('Ctrl Pts',(28.1410804630544,20.2763318691068,39.9739228747092));
#65034=CARTESIAN_POINT('Ctrl Pts',(28.1161968059784,20.3417810518088,39.9695640755936));
#65035=CARTESIAN_POINT('Ctrl Pts',(28.0990025554086,20.3932245710578,39.966293504175));
#65036=CARTESIAN_POINT('Ctrl Pts',(28.0318197074381,20.62529508557,39.9519609221912));
#65037=CARTESIAN_POINT('Ctrl Pts',(28.0053365300759,20.8117106669367,39.9414689951905));
#65038=CARTESIAN_POINT('Ctrl Pts',(28.0052502116719,20.9990810521211,39.9301166301426));
#65039=CARTESIAN_POINT('Ctrl Pts',(28.005250210651,20.9990832709263,39.9301164957099));
#65040=CARTESIAN_POINT('Ctrl Pts',(28.0052354568568,21.0311866794835,39.9281714189102));
#65041=CARTESIAN_POINT('Ctrl Pts',(28.0059957083417,21.0632847101422,39.9262061723218));
#65042=CARTESIAN_POINT('Ctrl Pts',(28.0083647951165,21.1127902920397,39.9231358281105));
#65043=CARTESIAN_POINT('Ctrl Pts',(28.0094283613751,21.1302188951357,39.9220473890065));
#65044=CARTESIAN_POINT('Ctrl Pts',(28.0119188963853,21.1637780693675,39.9199358763793));
#65045=CARTESIAN_POINT('Ctrl Pts',(28.0133137609071,21.1799096799813,39.918913879985));
#65046=CARTESIAN_POINT('Ctrl Pts',(28.0166746677519,21.2139452218374,39.9167419279425));
#65047=CARTESIAN_POINT('Ctrl Pts',(28.0186871221377,21.2318429993355,39.9155905989823));
#65048=CARTESIAN_POINT('Ctrl Pts',(28.0243199698841,21.2764856162233,39.9126947615763));
#65049=CARTESIAN_POINT('Ctrl Pts',(28.0282412168507,21.303188159405,39.9109409461418));
#65050=CARTESIAN_POINT('Ctrl Pts',(28.0474792090956,21.4179444701417,39.9033064013374));
#65051=CARTESIAN_POINT('Ctrl Pts',(28.0681605298537,21.5049827132208,39.8972608557067));
#65052=CARTESIAN_POINT('Ctrl Pts',(28.1180316848069,21.6659503350148,39.8856420114441));
#65053=CARTESIAN_POINT('Ctrl Pts',(28.1459400045123,21.7401049364899,39.880104935248));
#65054=CARTESIAN_POINT('Ctrl Pts',(28.2028256377524,21.8676716318516,39.8703745597673));
#65055=CARTESIAN_POINT('Ctrl Pts',(28.2299757372047,21.9217942520003,39.8661777875862));
#65056=CARTESIAN_POINT('Ctrl Pts',(28.2772701141578,22.0062530950429,39.8595958008263));
#65057=CARTESIAN_POINT('Ctrl Pts',(28.2958556505021,22.0374179274833,39.857159792246));
#65058=CARTESIAN_POINT('Ctrl Pts',(28.322693410728,22.0797507846873,39.8538579929893));
#65059=CARTESIAN_POINT('Ctrl Pts',(28.3302264135108,22.0913639848687,39.8529529880005));
#65060=CARTESIAN_POINT('Ctrl Pts',(28.3433091531497,22.1110802955399,39.8514191214463));
#65061=CARTESIAN_POINT('Ctrl Pts',(28.3487988375268,22.1192223741704,39.850786499799));
#65062=CARTESIAN_POINT('Ctrl Pts',(28.3607177100019,22.1366213702486,39.8494367108435));
#65063=CARTESIAN_POINT('Ctrl Pts',(28.3671655130134,22.1458647906036,39.8487207798172));
#65064=CARTESIAN_POINT('Ctrl Pts',(28.3855456419138,22.1717439072819,39.8467181298957));
#65065=CARTESIAN_POINT('Ctrl Pts',(28.3976565663506,22.1882517641354,39.8454427528857));
#65066=CARTESIAN_POINT('Ctrl Pts',(28.4840721076974,22.3023164252069,39.8366224074094));
#65067=CARTESIAN_POINT('Ctrl Pts',(28.5669893915256,22.3930374980453,39.8295553376561));
#65068=CARTESIAN_POINT('Ctrl Pts',(28.7203560479146,22.532549413148,39.8175268258092));
#65069=CARTESIAN_POINT('Ctrl Pts',(28.7865492704861,22.5854754778512,39.8126056876589));
#65070=CARTESIAN_POINT('Ctrl Pts',(28.9003002051002,22.665120285285,39.8043199837267));
#65071=CARTESIAN_POINT('Ctrl Pts',(28.945944363292,22.6943822378488,39.801037111244));
#65072=CARTESIAN_POINT('Ctrl Pts',(29.0045791278445,22.7286855139769,39.7968375625133));
#65073=CARTESIAN_POINT('Ctrl Pts',(29.0165085923217,22.7355001992225,39.7959840862754));
#65074=CARTESIAN_POINT('Ctrl Pts',(29.0285070493988,22.7421908648114,39.7951262847314));
#65075=CARTESIAN_POINT('',(28.0052508284892,21.0018180365441,39.7704548813608));
#65076=CARTESIAN_POINT('Ctrl Pts',(29.0285070491141,22.7421908646526,39.6352957892028));
#65077=CARTESIAN_POINT('Ctrl Pts',(28.96774165785,22.7083064318567,39.6397401410411));
#65078=CARTESIAN_POINT('Ctrl Pts',(28.9086745168633,22.6711963538654,39.6441844928793));
#65079=CARTESIAN_POINT('Ctrl Pts',(28.8516654162016,22.6310595470897,39.6486288447176));
#65080=CARTESIAN_POINT('Ctrl Pts',(28.7946982147363,22.5909522391122,39.6530699301515));
#65081=CARTESIAN_POINT('Ctrl Pts',(28.7397864521312,22.5478228956387,39.6575110155855));
#65082=CARTESIAN_POINT('Ctrl Pts',(28.6872624264623,22.5019146532085,39.6619521010195));
#65083=CARTESIAN_POINT('Ctrl Pts',(28.6347591791897,22.4560245719843,39.6663914295692));
#65084=CARTESIAN_POINT('Ctrl Pts',(28.584642162309,22.4073580952149,39.6708307581189));
#65085=CARTESIAN_POINT('Ctrl Pts',(28.5372105475533,22.3561985770199,39.6752700866686));
#65086=CARTESIAN_POINT('Ctrl Pts',(28.4897816008461,22.3050419365695,39.6797091655042));
#65087=CARTESIAN_POINT('Ctrl Pts',(28.4450380877795,22.2513928930657,39.6841482443398));
#65088=CARTESIAN_POINT('Ctrl Pts',(28.4032410154082,22.195570285523,39.6885873231754));
#65089=CARTESIAN_POINT('Ctrl Pts',(28.3614026648769,22.1396925484126,39.6930307859785));
#65090=CARTESIAN_POINT('Ctrl Pts',(28.3225168610619,22.0816373523696,39.6974742487816));
#65091=CARTESIAN_POINT('Ctrl Pts',(28.2868025451921,22.0217543948229,39.7019177115847));
#65092=CARTESIAN_POINT('Ctrl Pts',(28.2510707672903,21.9618421583134,39.7063633469589));
#65093=CARTESIAN_POINT('Ctrl Pts',(28.2185137948009,21.9001008135688,39.7108089823331));
#65094=CARTESIAN_POINT('Ctrl Pts',(28.1893042843611,21.8369041688671,39.7152546177073));
#65095=CARTESIAN_POINT('Ctrl Pts',(28.1600412481287,21.7735917176884,39.7197083996116));
#65096=CARTESIAN_POINT('Ctrl Pts',(28.1341381106743,21.7088190942514,39.7241621815159));
#65097=CARTESIAN_POINT('Ctrl Pts',(28.1117188940398,21.6429790256094,39.7286159634202));
#65098=CARTESIAN_POINT('Ctrl Pts',(28.0930232327615,21.5880741802737,39.7323300270848));
#65099=CARTESIAN_POINT('Ctrl Pts',(28.0767494597394,21.5324274606828,39.7360440907494));
#65100=CARTESIAN_POINT('Ctrl Pts',(28.0629422857144,21.4762719538526,39.7397581544139));
#65101=CARTESIAN_POINT('Ctrl Pts',(28.0412145886808,21.3879026874869,39.7456028008217));
#65102=CARTESIAN_POINT('Ctrl Pts',(28.0255254144271,21.2979944490804,39.7514474472295));
#65103=CARTESIAN_POINT('Ctrl Pts',(28.016046414538,21.2072576493942,39.7572920936373));
#65104=CARTESIAN_POINT('Ctrl Pts',(28.0089304971288,21.1391412257108,39.7616796895451));
#65105=CARTESIAN_POINT('Ctrl Pts',(28.0053134790015,21.070558160593,39.7660672854529));
#65106=CARTESIAN_POINT('Ctrl Pts',(28.0052508284892,21.0018180365441,39.7704548813608));
#65107=CARTESIAN_POINT('Ctrl Pts',(28.0052508284887,21.0018180360048,39.7704548813952));
#65108=CARTESIAN_POINT('Ctrl Pts',(28.005188142268,20.9330387123611,39.774844979364));
#65109=CARTESIAN_POINT('Ctrl Pts',(28.0086869930047,20.8641639778316,39.7792350773327));
#65110=CARTESIAN_POINT('Ctrl Pts',(28.0157502989284,20.7955967556587,39.7836251753015));
#65111=CARTESIAN_POINT('Ctrl Pts',(28.0228088252637,20.727075931462,39.7880123025846));
#65112=CARTESIAN_POINT('Ctrl Pts',(28.0334269744883,20.6588627054711,39.7923994298677));
#65113=CARTESIAN_POINT('Ctrl Pts',(28.0475556429306,20.5913576196137,39.7967865571509));
#65114=CARTESIAN_POINT('Ctrl Pts',(28.0616798259449,20.5238739645937,39.8011722916529));
#65115=CARTESIAN_POINT('Ctrl Pts',(28.079312214332,20.4570984951133,39.8055580261549));
#65116=CARTESIAN_POINT('Ctrl Pts',(28.1003524606402,20.3914223231958,39.8099437606568));
#65117=CARTESIAN_POINT('Ctrl Pts',(28.1213935848097,20.3257434110742,39.8143296781446));
#65118=CARTESIAN_POINT('Ctrl Pts',(28.145842692668,20.2611643649232,39.8187155956324));
#65119=CARTESIAN_POINT('Ctrl Pts',(28.173549948333,20.1980599952207,39.8231015131202));
#65120=CARTESIAN_POINT('Ctrl Pts',(28.2012858294595,20.1348904298983,39.8274919618728));
#65121=CARTESIAN_POINT('Ctrl Pts',(28.2322863701428,20.0731990405785,39.8318824106254));
#65122=CARTESIAN_POINT('Ctrl Pts',(28.2663545563422,20.0133384378702,39.836272859378));
#65123=CARTESIAN_POINT('Ctrl Pts',(28.3004436157103,19.953441159289,39.8406659981058));
#65124=CARTESIAN_POINT('Ctrl Pts',(28.3376037860427,19.8953773196889,39.8450591368337));
#65125=CARTESIAN_POINT('Ctrl Pts',(28.37759484984,19.8394703402178,39.8494522755615));
#65126=CARTESIAN_POINT('Ctrl Pts',(28.4176522429257,19.7834706332766,39.8538527007613));
#65127=CARTESIAN_POINT('Ctrl Pts',(28.460549579183,19.7296353109768,39.8582531259612));
#65128=CARTESIAN_POINT('Ctrl Pts',(28.5060073039398,19.678253660259,39.862653551161));
#65129=CARTESIAN_POINT('Ctrl Pts',(28.519902843827,19.662547291741,39.8639986753222));
#65130=CARTESIAN_POINT('Ctrl Pts',(28.5340373797176,19.6470699231913,39.8653437994835));
#65131=CARTESIAN_POINT('Ctrl Pts',(28.5484022985648,19.6318290765815,39.8666889236447));
#65132=CARTESIAN_POINT('Ctrl Pts',(28.5959787907883,19.5813515188641,39.8711439637238));
#65133=CARTESIAN_POINT('Ctrl Pts',(28.6462850630246,19.5332591277618,39.8755990038028));
#65134=CARTESIAN_POINT('Ctrl Pts',(28.6990524875787,19.4878614043598,39.8800540438819));
#65135=CARTESIAN_POINT('Ctrl Pts',(28.7517408787924,19.4425316761982,39.8845024113461));
#65136=CARTESIAN_POINT('Ctrl Pts',(28.8068827379929,19.3998889216797,39.8889507788104));
#65137=CARTESIAN_POINT('Ctrl Pts',(28.8641717466803,19.3602067991784,39.8933991462746));
#65138=CARTESIAN_POINT('Ctrl Pts',(28.9213935494979,19.3205712278676,39.8978422953486));
#65139=CARTESIAN_POINT('Ctrl Pts',(28.9807570987089,19.2838896676793,39.9022854444226));
#65140=CARTESIAN_POINT('Ctrl Pts',(29.0419234591962,19.250395214781,39.9067285934966));
#65141=CARTESIAN_POINT('Ctrl Pts',(29.1030514668754,19.216921763726,39.9111689566072));
#65142=CARTESIAN_POINT('Ctrl Pts',(29.1659796151259,19.1866316899739,39.9156093197177));
#65143=CARTESIAN_POINT('Ctrl Pts',(29.2303417765112,19.1597136686059,39.9200496828283));
#65144=CARTESIAN_POINT('Ctrl Pts',(29.2946854228434,19.132803390741,39.9244887685803));
#65145=CARTESIAN_POINT('Ctrl Pts',(29.3604618121782,19.1092634282051,39.9289278543323));
#65146=CARTESIAN_POINT('Ctrl Pts',(29.4272837340643,19.0892348021715,39.9333669400843));
#65147=CARTESIAN_POINT('Ctrl Pts',(29.4941091089309,19.0692051411713,39.9378062552232));
#65148=CARTESIAN_POINT('Ctrl Pts',(29.5619796542283,19.0526873150749,39.9422455703622));
#65149=CARTESIAN_POINT('Ctrl Pts',(29.6304935693411,19.0397723192951,39.9466848855011));
#65150=CARTESIAN_POINT('Ctrl Pts',(29.6990798882816,19.026843675264,39.9511288919996));
#65151=CARTESIAN_POINT('Ctrl Pts',(29.7683104522737,19.0175255515059,39.955572898498));
#65152=CARTESIAN_POINT('Ctrl Pts',(29.8377748049809,19.0118575130034,39.9600169049965));
#65153=CARTESIAN_POINT('Ctrl Pts',(29.9072798442408,19.0061861546262,39.9644635144316));
#65154=CARTESIAN_POINT('Ctrl Pts',(29.9770184555524,19.0041691509635,39.9689101238666));
#65155=CARTESIAN_POINT('Ctrl Pts',(30.0465794144433,19.0057939121921,39.9733567333016));
#65156=CARTESIAN_POINT('Ctrl Pts',(30.1162608748904,19.0074214880204,39.977811045669));
#65157=CARTESIAN_POINT('Ctrl Pts',(30.1857635808322,19.0127033844924,39.9822653580363));
#65158=CARTESIAN_POINT('Ctrl Pts',(30.2546814693548,19.0215751437906,39.9867196704037));
#65159=CARTESIAN_POINT('Ctrl Pts',(30.2902675815907,19.0261561231108,39.9890196778942));
#65160=CARTESIAN_POINT('Ctrl Pts',(30.3256979326675,19.0316934036972,39.9913196853848));
#65161=CARTESIAN_POINT('Ctrl Pts',(30.3609180206438,19.0381728555057,39.9936196928754));
#65162=CARTESIAN_POINT('Ctrl Pts',(30.4291381913059,19.0507233439789,39.9980747329548));
#65163=CARTESIAN_POINT('Ctrl Pts',(30.4968372954426,19.0668612003423,40.0025297730341));
#65164=CARTESIAN_POINT('Ctrl Pts',(30.563609577007,19.0865288590611,40.0069848131134));
#65165=CARTESIAN_POINT('Ctrl Pts',(30.6302818492097,19.1061670601974,40.011433180578));
#65166=CARTESIAN_POINT('Ctrl Pts',(30.6960295884878,19.1293244333095,40.0158815480425));
#65167=CARTESIAN_POINT('Ctrl Pts',(30.7604566771772,19.1558923012371,40.020329915507));
#65168=CARTESIAN_POINT('Ctrl Pts',(30.8248081862986,19.1824290023368,40.0247730645813));
#65169=CARTESIAN_POINT('Ctrl Pts',(30.8878416717185,19.2123680662701,40.0292162136556));
#65170=CARTESIAN_POINT('Ctrl Pts',(30.9491773723481,19.24555140334,40.0336593627299));
#65171=CARTESIAN_POINT('Ctrl Pts',(31.0104746139893,19.2787139336437,40.0380997258407));
#65172=CARTESIAN_POINT('Ctrl Pts',(31.0700757533565,19.3151164692266,40.0425400889516));
#65173=CARTESIAN_POINT('Ctrl Pts',(31.1276235714594,19.3545539681931,40.0469804520625));
#65174=CARTESIAN_POINT('Ctrl Pts',(31.1851548347903,19.3939801221803,40.0514195378148));
#65175=CARTESIAN_POINT('Ctrl Pts',(31.2406335460804,19.436439229852,40.055858623567));
#65176=CARTESIAN_POINT('Ctrl Pts',(31.2937310600872,19.4816826726057,40.0602977093193));
#65177=CARTESIAN_POINT('Ctrl Pts',(31.3468313178745,19.5269284532858,40.0647370244586));
#65178=CARTESIAN_POINT('Ctrl Pts',(31.397549763227,19.5749585355209,40.0691763395978));
#65179=CARTESIAN_POINT('Ctrl Pts',(31.4455918414855,19.6254848890134,40.0736156547371));
#65180=CARTESIAN_POINT('Ctrl Pts',(31.4936846894358,19.6760646375189,40.0780596612358));
#65181=CARTESIAN_POINT('Ctrl Pts',(31.5390951874425,19.7291455671678,40.0825036677346));
#65182=CARTESIAN_POINT('Ctrl Pts',(31.5815672728679,19.7844044571104,40.0869476742334));
#65183=CARTESIAN_POINT('Ctrl Pts',(31.6240642349772,19.8396957132041,40.0913942836687));
#65184=CARTESIAN_POINT('Ctrl Pts',(31.6636190813938,19.8971670655199,40.0958408931041));
#65185=CARTESIAN_POINT('Ctrl Pts',(31.7000191319871,19.956466333376,40.1002875025394));
#65186=CARTESIAN_POINT('Ctrl Pts',(31.7364822389673,20.0158683262974,40.1047418149071));
#65187=CARTESIAN_POINT('Ctrl Pts',(31.7697794075027,20.0771041257262,40.1091961272747));
#65188=CARTESIAN_POINT('Ctrl Pts',(31.7997443183266,20.1397977266066,40.1136504396423));
#65189=CARTESIAN_POINT('Ctrl Pts',(31.815216856753,20.1721698953213,40.1159504471303));
#65190=CARTESIAN_POINT('Ctrl Pts',(31.8298017323675,20.2049304303304,40.1182504546183));
#65191=CARTESIAN_POINT('Ctrl Pts',(31.8434812225516,20.2380258898101,40.1205504621063));
#65192=CARTESIAN_POINT('Ctrl Pts',(31.8699779523889,20.3021307238994,40.1250055021854));
#65193=CARTESIAN_POINT('Ctrl Pts',(31.8931791300075,20.367745542848,40.1294605422646));
#65194=CARTESIAN_POINT('Ctrl Pts',(31.9129128146097,20.4344983411148,40.1339155823438));
#65195=CARTESIAN_POINT('Ctrl Pts',(31.932616942738,20.5011511592013,40.1383639498082));
#65196=CARTESIAN_POINT('Ctrl Pts',(31.9488637482724,20.5689381082344,40.1428123172725));
#65197=CARTESIAN_POINT('Ctrl Pts',(31.9615294465421,20.6374675285603,40.1472606847369));
#65198=CARTESIAN_POINT('Ctrl Pts',(31.9741802866517,20.7059165568633,40.151703833811));
#65199=CARTESIAN_POINT('Ctrl Pts',(31.9832582748551,20.7751058476765,40.1561469828851));
#65200=CARTESIAN_POINT('Ctrl Pts',(31.988690003011,20.8446306515937,40.1605901319593));
#65201=CARTESIAN_POINT('Ctrl Pts',(31.9941183253401,20.9141118617539,40.16503049507));
#65202=CARTESIAN_POINT('Ctrl Pts',(31.9959048851972,20.9839276809806,40.1694708581806));
#65203=CARTESIAN_POINT('Ctrl Pts',(31.9940279428916,21.0536668004215,40.1739112212913));
#65204=CARTESIAN_POINT('Ctrl Pts',(31.9921515405257,21.1233858580206,40.1783503070435));
#65205=CARTESIAN_POINT('Ctrl Pts',(31.9866137413496,21.1930277707646,40.1827893927956));
#65206=CARTESIAN_POINT('Ctrl Pts',(31.9774449139628,21.2621815682738,40.1872284785477));
#65207=CARTESIAN_POINT('Ctrl Pts',(31.9682756127827,21.3313389392618,40.1916677936868));
#65208=CARTESIAN_POINT('Ctrl Pts',(31.9554749775831,21.40000766021,40.1961071088259));
#65209=CARTESIAN_POINT('Ctrl Pts',(31.9391249825634,21.4677839934184,40.200546423965));
#65210=CARTESIAN_POINT('Ctrl Pts',(31.9227577092693,21.535631950996,40.2049904304636));
#65211=CARTESIAN_POINT('Ctrl Pts',(31.9028337047619,21.6025851620144,40.2094344369622));
#65212=CARTESIAN_POINT('Ctrl Pts',(31.8794853934634,21.6682531094261,40.2138784434608));
#65213=CARTESIAN_POINT('Ctrl Pts',(31.8561234066284,21.7339595197657,40.2183250528959));
#65214=CARTESIAN_POINT('Ctrl Pts',(31.8293333088405,21.798378716223,40.2227716623311));
#65215=CARTESIAN_POINT('Ctrl Pts',(31.7992953972322,21.8611408920722,40.2272182717663));
#65216=CARTESIAN_POINT('Ctrl Pts',(31.7692054504717,21.9240117918375,40.2316725841338));
#65217=CARTESIAN_POINT('Ctrl Pts',(31.7358566933557,21.9852195116337,40.2361268965012));
#65218=CARTESIAN_POINT('Ctrl Pts',(31.6994745999223,22.0444202443074,40.2405812088687));
#65219=CARTESIAN_POINT('Ctrl Pts',(31.6806885156796,22.0749888522756,40.2428812163581));
#65220=CARTESIAN_POINT('Ctrl Pts',(31.6610943714265,22.1050228457397,40.2451812238476));
#65221=CARTESIAN_POINT('Ctrl Pts',(31.6407274259471,22.1344783277988,40.247481231337));
#65222=CARTESIAN_POINT('Ctrl Pts',(31.6012773116242,22.191532643373,40.2519362714162));
#65223=CARTESIAN_POINT('Ctrl Pts',(31.5587699647844,22.2466391273221,40.2563913114954));
#65224=CARTESIAN_POINT('Ctrl Pts',(31.5134244487598,22.2994514228689,40.2608463515746));
#65225=CARTESIAN_POINT('Ctrl Pts',(31.4681468497813,22.3521846178689,40.265294719039));
#65226=CARTESIAN_POINT('Ctrl Pts',(31.4200398349791,22.4026300762978,40.2697430865033));
#65227=CARTESIAN_POINT('Ctrl Pts',(31.3693651170561,22.4504712126375,40.2741914539677));
#65228=CARTESIAN_POINT('Ctrl Pts',(31.3187498457626,22.4982562264287,40.2786346030418));
#65229=CARTESIAN_POINT('Ctrl Pts',(31.2655732081003,22.5434426518239,40.283077752116));
#65230=CARTESIAN_POINT('Ctrl Pts',(31.2101352588555,22.5857491030345,40.2875209011901));
#65231=CARTESIAN_POINT('Ctrl Pts',(31.1547320705643,22.6280290270627,40.2919612643008));
#65232=CARTESIAN_POINT('Ctrl Pts',(31.097070771626,22.667432263163,40.2964016274115));
#65233=CARTESIAN_POINT('Ctrl Pts',(31.037484976151,22.7037172555213,40.3008419905222));
#65234=CARTESIAN_POINT('Ctrl Pts',(30.9779163217127,22.7399918097814,40.3052810762743));
#65235=CARTESIAN_POINT('Ctrl Pts',(30.9164246874985,22.7731496467442,40.3097201620265));
#65236=CARTESIAN_POINT('Ctrl Pts',(30.8533716928697,22.8029931548147,40.3141592477786));
#65237=CARTESIAN_POINT('Ctrl Pts',(30.7903154400174,22.8328382050296,40.3185985629177));
#65238=CARTESIAN_POINT('Ctrl Pts',(30.7256981098559,22.8593683791901,40.3230378780568));
#65239=CARTESIAN_POINT('Ctrl Pts',(30.6599032643427,22.8824333306149,40.3274771931959));
#65240=CARTESIAN_POINT('Ctrl Pts',(30.594038888448,22.9055226565155,40.3319211996945));
#65241=CARTESIAN_POINT('Ctrl Pts',(30.526994976218,22.9251392885967,40.3363652061931));
#65242=CARTESIAN_POINT('Ctrl Pts',(30.4591713762641,22.9411824256673,40.3408092126917));
#65243=CARTESIAN_POINT('Ctrl Pts',(30.3913080507767,22.9572349594992,40.3452558221269));
#65244=CARTESIAN_POINT('Ctrl Pts',(30.322664610131,22.9697097447899,40.3497024315621));
#65245=CARTESIAN_POINT('Ctrl Pts',(30.2536495004518,22.9785574273749,40.3541490409973));
#65246=CARTESIAN_POINT('Ctrl Pts',(30.1845148347999,22.9874204369413,40.3586033533648));
#65247=CARTESIAN_POINT('Ctrl Pts',(30.1150077027371,22.9926437650225,40.3630576657322));
#65248=CARTESIAN_POINT('Ctrl Pts',(30.0455392424493,22.9942301120726,40.3675119780997));
#65249=CARTESIAN_POINT('Ctrl Pts',(30.0096688396229,22.9950492306694,40.3698119855891));
#65250=CARTESIAN_POINT('Ctrl Pts',(29.9738087108839,22.9948995004175,40.3721119930784));
#65251=CARTESIAN_POINT('Ctrl Pts',(29.9380148627151,22.9937867000398,40.3744120005678));
#65252=CARTESIAN_POINT('Ctrl Pts',(29.8686813887232,22.9916311811452,40.3788671658435));
#65253=CARTESIAN_POINT('Ctrl Pts',(29.7993239332432,22.9858505246595,40.3833223311191));
#65254=CARTESIAN_POINT('Ctrl Pts',(29.7303523298611,22.9764406635385,40.3877774963948));
#65255=CARTESIAN_POINT('Ctrl Pts',(29.6614987482632,22.9670469042413,40.3922250381482));
#65256=CARTESIAN_POINT('Ctrl Pts',(29.5930301878976,22.9540363429594,40.3966725799016));
#65257=CARTESIAN_POINT('Ctrl Pts',(29.5253543733448,22.9374568618674,40.401120121655));
#65258=CARTESIAN_POINT('Ctrl Pts',(29.4577458049611,22.9208938550004,40.4055632441022));
#65259=CARTESIAN_POINT('Ctrl Pts',(29.3909288925793,22.9007690785748,40.4100063665495));
#65260=CARTESIAN_POINT('Ctrl Pts',(29.3253028373582,22.877181744324,40.4144494889967));
#65261=CARTESIAN_POINT('Ctrl Pts',(29.2597185852575,22.8536094349617,40.4188897812207));
#65262=CARTESIAN_POINT('Ctrl Pts',(29.1953241446342,22.82657910902,40.4233300734448));
#65263=CARTESIAN_POINT('Ctrl Pts',(29.1325034769165,22.7962397793552,40.4277703656688));
#65264=CARTESIAN_POINT('Ctrl Pts',(29.0973232052565,22.7792494177693,40.4302569786319));
#65265=CARTESIAN_POINT('Ctrl Pts',(29.0626361878621,22.7612221995001,40.4327435915949));
#65266=CARTESIAN_POINT('Ctrl Pts',(29.0285070491141,22.7421908646526,40.4352302045579));
#65267=CARTESIAN_POINT('Origin',(30.,21.,34.5704548813952));
#65268=CARTESIAN_POINT('',(29.0285070491341,22.7421908646638,41.392186712139));
#65269=CARTESIAN_POINT('',(29.0285070491141,22.7421908646526,41.2351467212172));
#65270=CARTESIAN_POINT('',(29.0285070491141,22.7421908646526,34.5704548813952));
#65271=CARTESIAN_POINT('Ctrl Pts',(29.0285070491341,22.7421908646638,41.392186712139));
#65272=CARTESIAN_POINT('Ctrl Pts',(29.0783988147974,22.7700118684534,41.3882464250647));
#65273=CARTESIAN_POINT('Ctrl Pts',(29.1294676353672,22.7956796508801,41.3843557908295));
#65274=CARTESIAN_POINT('Ctrl Pts',(29.1962551987017,22.825727547167,41.3795065614409));
#65275=CARTESIAN_POINT('Ctrl Pts',(29.2110179528093,22.8321556023395,41.3784492427945));
#65276=CARTESIAN_POINT('Ctrl Pts',(29.2352826800822,22.8423733524512,41.3767369552561));
#65277=CARTESIAN_POINT('Ctrl Pts',(29.2447385844778,22.8462698496204,41.3760759583762));
#65278=CARTESIAN_POINT('Ctrl Pts',(29.2639220336912,22.8540027282305,41.3747482377556));
#65279=CARTESIAN_POINT('Ctrl Pts',(29.273650556896,22.8578356728283,41.3740817146443));
#65280=CARTESIAN_POINT('Ctrl Pts',(29.299442411749,22.8677638470503,41.3723314490789));
#65281=CARTESIAN_POINT('Ctrl Pts',(29.3155554921175,22.8737284982767,41.3712550948816));
#65282=CARTESIAN_POINT('Ctrl Pts',(29.3976470125942,22.902916358766,41.3658479894058));
#65283=CARTESIAN_POINT('Ctrl Pts',(29.4647436332688,22.9228682767636,41.3616769625914));
#65284=CARTESIAN_POINT('Ctrl Pts',(29.6558376539838,22.9689104467555,41.350134650315));
#65285=CARTESIAN_POINT('Ctrl Pts',(29.7814617199492,22.9867807798648,41.3429173419661));
#65286=CARTESIAN_POINT('Ctrl Pts',(29.9749843992764,22.9957222222231,41.3314614568032));
#65287=CARTESIAN_POINT('Ctrl Pts',(30.0421430316378,22.9954336933537,41.3274282679224));
#65288=CARTESIAN_POINT('Ctrl Pts',(30.1337345118057,22.9904141798851,41.3217745626348));
#65289=CARTESIAN_POINT('Ctrl Pts',(30.1582860397527,22.9886123235188,41.3202441914261));
#65290=CARTESIAN_POINT('Ctrl Pts',(30.2002965755275,22.9847462479271,41.3175969133747));
#65291=CARTESIAN_POINT('Ctrl Pts',(30.217773512646,22.9829047006894,41.3164870911432));
#65292=CARTESIAN_POINT('Ctrl Pts',(30.2512602343165,22.9789281603819,41.3143432623251));
#65293=CARTESIAN_POINT('Ctrl Pts',(30.267272949745,22.9768291565714,41.3133104767029));
#65294=CARTESIAN_POINT('Ctrl Pts',(30.3096169904497,22.9707546713981,41.3105582895207));
#65295=CARTESIAN_POINT('Ctrl Pts',(30.3358964648287,22.966446059951,41.3088285131224));
#65296=CARTESIAN_POINT('Ctrl Pts',(30.4396008200475,22.9473039770417,41.3019129629953));
#65297=CARTESIAN_POINT('Ctrl Pts',(30.5161952487708,22.9284142448369,41.296602652232));
#65298=CARTESIAN_POINT('Ctrl Pts',(30.7144745279476,22.8668540138849,41.2823521968396));
#65299=CARTESIAN_POINT('Ctrl Pts',(30.8334886344292,22.8168411497006,41.2732627458577));
#65300=CARTESIAN_POINT('Ctrl Pts',(30.9945703783259,22.7299702955147,41.2606589141987));
#65301=CARTESIAN_POINT('Ctrl Pts',(31.0412288178922,22.7022958172686,41.2569727124745));
#65302=CARTESIAN_POINT('Ctrl Pts',(31.0999597343551,22.6641412120747,41.2523381714851));
#65303=CARTESIAN_POINT('Ctrl Pts',(31.1131119502518,22.6553728326301,41.251300720779));
#65304=CARTESIAN_POINT('Ctrl Pts',(31.1345503416056,22.6407091277087,41.2496121302984));
#65305=CARTESIAN_POINT('Ctrl Pts',(31.1428979450318,22.6349052639044,41.2489552648657));
#65306=CARTESIAN_POINT('Ctrl Pts',(31.1598021219504,22.6229594945695,41.24762697227));
#65307=CARTESIAN_POINT('Ctrl Pts',(31.1683550821845,22.6168131918126,41.2469558550686));
#65308=CARTESIAN_POINT('Ctrl Pts',(31.1910177415001,22.6002536667147,41.245178991534));
#65309=CARTESIAN_POINT('Ctrl Pts',(31.2050398254683,22.5897213991733,41.244081041016));
#65310=CARTESIAN_POINT('Ctrl Pts',(31.2810095779918,22.5310761296009,41.2381293927626));
#65311=CARTESIAN_POINT('Ctrl Pts',(31.3402234880531,22.4795213149424,41.233477641371));
#65312=CARTESIAN_POINT('Ctrl Pts',(31.5094624950596,22.3136508167594,41.2196167053532));
#65313=CARTESIAN_POINT('Ctrl Pts',(31.6090365643494,22.189603034915,41.2106063583353));
#65314=CARTESIAN_POINT('Ctrl Pts',(31.7131036889562,22.0226267398648,41.1986942672323));
#65315=CARTESIAN_POINT('Ctrl Pts',(31.732390381713,21.9896024323267,41.1963507917934));
#65316=CARTESIAN_POINT('Ctrl Pts',(31.7604202776747,21.9382739659812,41.1927145730851));
#65317=CARTESIAN_POINT('Ctrl Pts',(31.7698538283404,21.9203558919153,41.1914463757514));
#65318=CARTESIAN_POINT('Ctrl Pts',(31.7867610830616,21.887020755466,41.1890874412639));
#65319=CARTESIAN_POINT('Ctrl Pts',(31.7943121486991,21.8716449229019,41.187999557427));
#65320=CARTESIAN_POINT('Ctrl Pts',(31.8106320704697,21.8373025904847,41.1855691831093));
#65321=CARTESIAN_POINT('Ctrl Pts',(31.8193027170477,21.8182919352196,41.1842234390547));
#65322=CARTESIAN_POINT('Ctrl Pts',(31.8438387173611,21.7621775276537,41.1802484839769));
#65323=CARTESIAN_POINT('Ctrl Pts',(31.8588779554427,21.7247262647507,41.1775919622537));
#65324=CARTESIAN_POINT('Ctrl Pts',(31.9237899582611,21.5477358974643,41.1650155444085));
#65325=CARTESIAN_POINT('Ctrl Pts',(31.9591444679488,21.4033895812671,41.1546481264045));
#65326=CARTESIAN_POINT('Ctrl Pts',(31.9855885476766,21.1994373616712,41.1403314195655));
#65327=CARTESIAN_POINT('Ctrl Pts',(31.9905146236455,21.1420894092123,41.1363478960723));
#65328=CARTESIAN_POINT('Ctrl Pts',(31.9939842612521,21.0603595494968,41.1307914416761));
#65329=CARTESIAN_POINT('Ctrl Pts',(31.9945710681169,21.0360952805971,41.1291570180706));
#65330=CARTESIAN_POINT('Ctrl Pts',(31.9948277521411,20.9927973209204,41.1262742496738));
#65331=CARTESIAN_POINT('Ctrl Pts',(31.9946682875041,20.9737678514942,41.125018904176));
#65332=CARTESIAN_POINT('Ctrl Pts',(31.9939903879076,20.9438965575214,41.1230695779838));
#65333=CARTESIAN_POINT('Ctrl Pts',(31.9936557557704,20.9330522283619,41.1223663028804));
#65334=CARTESIAN_POINT('Ctrl Pts',(31.9928481862978,20.9123594430176,41.1210334230297));
#65335=CARTESIAN_POINT('Ctrl Pts',(31.9923906888463,20.9025109877388,41.120403060864));
#65336=CARTESIAN_POINT('Ctrl Pts',(31.9910689099022,20.8779819210449,41.1188422391293));
#65337=CARTESIAN_POINT('Ctrl Pts',(31.990115246675,20.8633063609461,41.1179165893663));
#65338=CARTESIAN_POINT('Ctrl Pts',(31.9859753857473,20.8089042788245,41.1145111368561));
#65339=CARTESIAN_POINT('Ctrl Pts',(31.9817610088244,20.7692629788546,41.1120809646955));
#65340=CARTESIAN_POINT('Ctrl Pts',(31.9592578261142,20.6046819809806,41.1021078289706));
#65341=CARTESIAN_POINT('Ctrl Pts',(31.9303159879416,20.4814902520085,41.094908319882));
#65342=CARTESIAN_POINT('Ctrl Pts',(31.8589011775357,20.269989544181,41.0818882115268));
#65343=CARTESIAN_POINT('Ctrl Pts',(31.8212292749245,20.1805186462145,41.076155824671));
#65344=CARTESIAN_POINT('Ctrl Pts',(31.7648746092339,20.0699556814467,41.0685378423553));
#65345=CARTESIAN_POINT('Ctrl Pts',(31.7520519963007,20.0460196476569,41.0668553369791));
#65346=CARTESIAN_POINT('Ctrl Pts',(31.7299025405598,20.0066268121713,41.0640261216806));
#65347=CARTESIAN_POINT('Ctrl Pts',(31.7208470716229,19.9910211043967,41.0628891655105));
#65348=CARTESIAN_POINT('Ctrl Pts',(31.702558528249,19.9604661247648,41.0606298275783));
#65349=CARTESIAN_POINT('Ctrl Pts',(31.693337150051,19.9455117432933,41.0595079468783));
#65350=CARTESIAN_POINT('Ctrl Pts',(31.6702032711251,19.9090814429663,41.0567340749481));
#65351=CARTESIAN_POINT('Ctrl Pts',(31.6560730842049,19.8877481833498,41.0550741107011));
#65352=CARTESIAN_POINT('Ctrl Pts',(31.6014702546122,19.8086587598874,41.0487818048469));
#65353=CARTESIAN_POINT('Ctrl Pts',(31.558358490369,19.75279599977,41.044051623411));
#65354=CARTESIAN_POINT('Ctrl Pts',(31.4225767115047,19.5949116704993,41.0298264469451));
#65355=CARTESIAN_POINT('Ctrl Pts',(31.3221965749725,19.5000702089894,41.0200991070525));
#65356=CARTESIAN_POINT('Ctrl Pts',(31.1686596491569,19.3824827594207,41.0067700897673));
#65357=CARTESIAN_POINT('Ctrl Pts',(31.1230553297336,19.3504924263493,41.0029816437539));
#65358=CARTESIAN_POINT('Ctrl Pts',(31.0627572081478,19.3118565278575,40.9982414732662));
#65359=CARTESIAN_POINT('Ctrl Pts',(31.0492430418437,19.3034239351426,40.9971957807613));
#65360=CARTESIAN_POINT('Ctrl Pts',(31.0269186395826,19.2898627151663,40.9954973694422));
#65361=CARTESIAN_POINT('Ctrl Pts',(31.0181677414245,19.2846382624943,40.9948387998748));
#65362=CARTESIAN_POINT('Ctrl Pts',(31.0014359384849,19.2748222162752,40.9935937862481));
#65363=CARTESIAN_POINT('Ctrl Pts',(30.9934626614644,19.2702184320494,40.99300651775));
#65364=CARTESIAN_POINT('Ctrl Pts',(30.9715054965582,19.2577422285986,40.9914049204877));
#65365=CARTESIAN_POINT('Ctrl Pts',(30.9574577081136,19.2499829007143,40.9903975098373));
#65366=CARTESIAN_POINT('Ctrl Pts',(30.8969647553191,19.2175159900352,40.9861260697649));
#65367=CARTESIAN_POINT('Ctrl Pts',(30.8496420807292,19.1944794897122,40.982950817927));
#65368=CARTESIAN_POINT('Ctrl Pts',(30.6713740279114,19.1162631454633,40.9713938503068));
#65369=CARTESIAN_POINT('Ctrl Pts',(30.535560558107,19.0732446873642,40.963343843533));
#65370=CARTESIAN_POINT('Ctrl Pts',(30.3496517391777,19.035556302364,40.9521489172287));
#65371=CARTESIAN_POINT('Ctrl Pts',(30.3026581794283,19.0277695428048,40.9493078450722));
#65372=CARTESIAN_POINT('Ctrl Pts',(30.2189882499579,19.0169664453593,40.9441917969594));
#65373=CARTESIAN_POINT('Ctrl Pts',(30.1824222360765,19.0132690667533,40.941936781028));
#65374=CARTESIAN_POINT('Ctrl Pts',(30.1258677157363,19.0091249728261,40.9384085026455));
#65375=CARTESIAN_POINT('Ctrl Pts',(30.1059386227073,19.0079651062285,40.9371574792123));
#65376=CARTESIAN_POINT('Ctrl Pts',(30.068867323712,19.0063654313446,40.9348144746451));
#65377=CARTESIAN_POINT('Ctrl Pts',(30.0517302495366,19.0058471841884,40.9337250632387));
#65378=CARTESIAN_POINT('Ctrl Pts',(30.0133514864003,19.0051815946914,40.9312702634482));
#65379=CARTESIAN_POINT('Ctrl Pts',(29.9921101078738,19.0051525311417,40.9299012923569));
#65380=CARTESIAN_POINT('Ctrl Pts',(29.937115896891,19.0059556335037,40.9263288598602));
#65381=CARTESIAN_POINT('Ctrl Pts',(29.9033785831263,19.0073054875259,40.9241097203117));
#65382=CARTESIAN_POINT('Ctrl Pts',(29.6900619657174,19.0212701780155,40.9098988032085));
#65383=CARTESIAN_POINT('Ctrl Pts',(29.5128666115394,19.0572923524432,40.8971793153853));
#65384=CARTESIAN_POINT('Ctrl Pts',(29.285618296824,19.1365693946878,40.8805499618143));
#65385=CARTESIAN_POINT('Ctrl Pts',(29.2292216323176,19.1591803683033,40.8764060424333));
#65386=CARTESIAN_POINT('Ctrl Pts',(29.159088626545,19.1910882169286,40.8713019679127));
#65387=CARTESIAN_POINT('Ctrl Pts',(29.1443202204914,19.1980272107316,40.8702300796092));
#65388=CARTESIAN_POINT('Ctrl Pts',(29.1203956233064,19.2096287500604,40.8685003693419));
#65389=CARTESIAN_POINT('Ctrl Pts',(29.111187653951,19.214182064474,40.8678362959442));
#65390=CARTESIAN_POINT('Ctrl Pts',(29.0938540759062,19.2229207517305,40.8665899123099));
#65391=CARTESIAN_POINT('Ctrl Pts',(29.0857213456674,19.2270911922328,40.8660066677032));
#65392=CARTESIAN_POINT('Ctrl Pts',(29.0637125555656,19.2385689591375,40.8644317213948));
#65393=CARTESIAN_POINT('Ctrl Pts',(29.0498932211605,19.2459844255293,40.8634465424598));
#65394=CARTESIAN_POINT('Ctrl Pts',(28.9937573030636,19.2769651572645,40.8594540272724));
#65395=CARTESIAN_POINT('Ctrl Pts',(28.9522151689417,19.3019066116733,40.8565214078539));
#65396=CARTESIAN_POINT('Ctrl Pts',(28.7892147114622,19.4080324652554,40.8449361372304));
#65397=CARTESIAN_POINT('Ctrl Pts',(28.6759297202561,19.5009322748394,40.8366715659025));
#65398=CARTESIAN_POINT('Ctrl Pts',(28.5240501537722,19.6562503766664,40.8238565377191));
#65399=CARTESIAN_POINT('Ctrl Pts',(28.4770626782782,19.7097475450698,40.8195908341328));
#65400=CARTESIAN_POINT('Ctrl Pts',(28.4175283521975,19.7853234542852,40.8136654456841));
#65401=CARTESIAN_POINT('Ctrl Pts',(28.4023932791891,19.8052999102075,40.8121083707291));
#65402=CARTESIAN_POINT('Ctrl Pts',(28.3772468686914,19.8398226914187,40.8094295180314));
#65403=CARTESIAN_POINT('Ctrl Pts',(28.3670447647968,19.8542267763879,40.8083152769599));
#65404=CARTESIAN_POINT('Ctrl Pts',(28.3467087718258,19.883762006806,40.8060364663726));
#65405=CARTESIAN_POINT('Ctrl Pts',(28.3365882792009,19.8989002981793,40.8048715304247));
#65406=CARTESIAN_POINT('Ctrl Pts',(28.3114350366837,19.9376629821515,40.8018952514135));
#65407=CARTESIAN_POINT('Ctrl Pts',(28.2966902808344,19.9614686122781,40.800073482506));
#65408=CARTESIAN_POINT('Ctrl Pts',(28.2270105001256,20.0794452495436,40.7910701279346));
#65409=CARTESIAN_POINT('Ctrl Pts',(28.1793658537273,20.1776876147103,40.7836346604546));
#65410=CARTESIAN_POINT('Ctrl Pts',(28.1101139219429,20.3564196104473,40.7703292160787));
#65411=CARTESIAN_POINT('Ctrl Pts',(28.0850625034879,20.4353059110091,40.7645312166492));
#65412=CARTESIAN_POINT('Ctrl Pts',(28.0490635393503,20.5790860263211,40.7542694057252));
#65413=CARTESIAN_POINT('Ctrl Pts',(28.0362883544957,20.6434051887234,40.7497856647631));
#65414=CARTESIAN_POINT('Ctrl Pts',(28.0242684515574,20.7247015329028,40.7443382437101));
#65415=CARTESIAN_POINT('Ctrl Pts',(28.0220408090699,20.7411914216751,40.7432445880336));
#65416=CARTESIAN_POINT('Ctrl Pts',(28.0187637128904,20.7679714350686,40.7414887896749));
#65417=CARTESIAN_POINT('Ctrl Pts',(28.0175875414003,20.7782448738286,40.7408200586066));
#65418=CARTESIAN_POINT('Ctrl Pts',(28.0155275886762,20.7975662029829,40.7395720353089));
#65419=CARTESIAN_POINT('Ctrl Pts',(28.014625673241,20.8066118308211,40.7389917226292));
#65420=CARTESIAN_POINT('Ctrl Pts',(28.0123617647267,20.8310053080897,40.7374367188637));
#65421=CARTESIAN_POINT('Ctrl Pts',(28.0111156738678,20.8463636367657,40.7364682579945));
#65422=CARTESIAN_POINT('Ctrl Pts',(28.0068800068863,20.9073248414323,40.7326606470627));
#65423=CARTESIAN_POINT('Ctrl Pts',(28.0052797412273,20.9530133742082,40.7298876570754));
#65424=CARTESIAN_POINT('Ctrl Pts',(28.0051910645533,21.0912006518033,40.7216374078533));
#65425=CARTESIAN_POINT('Ctrl Pts',(28.0115631701603,21.1835787849369,40.7163033240241));
#65426=CARTESIAN_POINT('Ctrl Pts',(28.0397940707045,21.3862606381217,40.704426295711));
#65427=CARTESIAN_POINT('Ctrl Pts',(28.0646029222984,21.4958217449137,40.6978818965525));
#65428=CARTESIAN_POINT('Ctrl Pts',(28.1084183083359,21.6340563167445,40.6890483566391));
#65429=CARTESIAN_POINT('Ctrl Pts',(28.1191262188896,21.6651483585229,40.6870234220573));
#65430=CARTESIAN_POINT('Ctrl Pts',(28.1372944175485,21.7139495376848,40.6837765497706));
#65431=CARTESIAN_POINT('Ctrl Pts',(28.144250768065,21.7318406769048,40.6825713361627));
#65432=CARTESIAN_POINT('Ctrl Pts',(28.1579470372654,21.7656148167054,40.6802663951532));
#65433=CARTESIAN_POINT('Ctrl Pts',(28.1646369719428,21.7815162759595,40.6791684437462));
#65434=CARTESIAN_POINT('Ctrl Pts',(28.1805000655374,21.817894198495,40.6766262248632));
#65435=CARTESIAN_POINT('Ctrl Pts',(28.1898140004864,21.8383063344212,40.6751772434949));
#65436=CARTESIAN_POINT('Ctrl Pts',(28.2213689507853,21.9044821142122,40.6704035863536));
#65437=CARTESIAN_POINT('Ctrl Pts',(28.2450152866754,21.9495494718544,40.6670312859722));
#65438=CARTESIAN_POINT('Ctrl Pts',(28.3084466381575,22.059963037024,40.6584584848829));
#65439=CARTESIAN_POINT('Ctrl Pts',(28.3503141689958,22.1240147803844,40.653196707343));
#65440=CARTESIAN_POINT('Ctrl Pts',(28.4692940301177,22.2850213052643,40.6392825395962));
#65441=CARTESIAN_POINT('Ctrl Pts',(28.551940481958,22.3774856062171,40.6305634210846));
#65442=CARTESIAN_POINT('Ctrl Pts',(28.6633192486533,22.4809151509201,40.6203127456696));
#65443=CARTESIAN_POINT('Ctrl Pts',(28.6844204863953,22.4996919173322,40.618429649468));
#65444=CARTESIAN_POINT('Ctrl Pts',(28.715410276333,22.5261102520652,40.6157561841209));
#65445=CARTESIAN_POINT('Ctrl Pts',(28.7249820444586,22.5341161925347,40.6149426794435));
#65446=CARTESIAN_POINT('Ctrl Pts',(28.7421323654658,22.5481895225061,40.6135076403695));
#65447=CARTESIAN_POINT('Ctrl Pts',(28.749680926477,22.554292125031,40.6128837071507));
#65448=CARTESIAN_POINT('Ctrl Pts',(28.7666862329129,22.5678359262381,40.6114952590458));
#65449=CARTESIAN_POINT('Ctrl Pts',(28.7761661251457,22.5752469660162,40.6107328078489));
#65450=CARTESIAN_POINT('Ctrl Pts',(28.8055346138781,22.5977810312133,40.6084040510527));
#65451=CARTESIAN_POINT('Ctrl Pts',(28.8256414914497,22.6126171297938,40.6068560220941));
#65452=CARTESIAN_POINT('Ctrl Pts',(28.8746023689811,22.6473419138684,40.6031822266392));
#65453=CARTESIAN_POINT('Ctrl Pts',(28.9037125419554,22.6668561061358,40.6010751782613));
#65454=CARTESIAN_POINT('Ctrl Pts',(28.9645334147829,22.7053447379297,40.596796341949));
#65455=CARTESIAN_POINT('Ctrl Pts',(28.9962740328145,22.7242168613144,40.5946289620116));
#65456=CARTESIAN_POINT('Ctrl Pts',(29.0285071367644,22.7421909135288,40.592474930186));
#65457=CARTESIAN_POINT('',(28.0052500576935,20.9995202415483,40.5704548814432));
#65458=CARTESIAN_POINT('Ctrl Pts',(29.0285070491141,22.7421908646526,40.4352302045579));
#65459=CARTESIAN_POINT('Ctrl Pts',(28.9675807103231,22.7082166831438,40.4396692331823));
#65460=CARTESIAN_POINT('Ctrl Pts',(28.9084339214687,22.6710400771609,40.4441082618066));
#65461=CARTESIAN_POINT('Ctrl Pts',(28.8514141220663,22.6308825964831,40.4485472904309));
#65462=CARTESIAN_POINT('Ctrl Pts',(28.7943395779221,22.5906865605851,40.4529905809692));
#65463=CARTESIAN_POINT('Ctrl Pts',(28.7393965044057,22.5475042143395,40.4574338715075));
#65464=CARTESIAN_POINT('Ctrl Pts',(28.6869020394544,22.5015995832814,40.4618771620457));
#65465=CARTESIAN_POINT('Ctrl Pts',(28.6343838567526,22.4556742118541,40.4663224601262));
#65466=CARTESIAN_POINT('Ctrl Pts',(28.584316838868,22.4070244461456,40.4707677582067));
#65467=CARTESIAN_POINT('Ctrl Pts',(28.5369816920423,22.3559516927533,40.4752130562872));
#65468=CARTESIAN_POINT('Ctrl Pts',(28.4895578967346,22.3047832911511,40.4796666794486));
#65469=CARTESIAN_POINT('Ctrl Pts',(28.4448765108707,22.2511832108462,40.48412030261));
#65470=CARTESIAN_POINT('Ctrl Pts',(28.4031780030416,22.1954861239386,40.4885739257714));
#65471=CARTESIAN_POINT('Ctrl Pts',(28.3633271727297,22.1422569971719,40.4928302071138));
#65472=CARTESIAN_POINT('Ctrl Pts',(28.3262006184482,22.0871131274035,40.4970864884562));
#65473=CARTESIAN_POINT('Ctrl Pts',(28.2919693293639,22.0303682791441,40.5013427697985));
#65474=CARTESIAN_POINT('Ctrl Pts',(28.2549707662894,21.9690361498658,40.5059431309863));
#65475=CARTESIAN_POINT('Ctrl Pts',(28.2212168354539,21.9056053030204,40.510543492174));
#65476=CARTESIAN_POINT('Ctrl Pts',(28.1909430004169,21.8404405599204,40.5151438533617));
#65477=CARTESIAN_POINT('Ctrl Pts',(28.1606106549391,21.7751498724915,40.5197531056978));
#65478=CARTESIAN_POINT('Ctrl Pts',(28.1337721552087,21.708118934563,40.5243623580339));
#65479=CARTESIAN_POINT('Ctrl Pts',(28.1106202090465,21.6397433610727,40.5289716103701));
#65480=CARTESIAN_POINT('Ctrl Pts',(28.087602011715,21.5717627933815,40.533554235048));
#65481=CARTESIAN_POINT('Ctrl Pts',(28.0682280672016,21.5024534966911,40.5381368597258));
#65482=CARTESIAN_POINT('Ctrl Pts',(28.0526408693613,21.4322267678177,40.5427194844037));
#65483=CARTESIAN_POINT('Ctrl Pts',(28.0369178157813,21.3613879530327,40.547342050569));
#65484=CARTESIAN_POINT('Ctrl Pts',(28.0250480438997,21.2896160515693,40.5519646167342));
#65485=CARTESIAN_POINT('Ctrl Pts',(28.0171267005988,21.2173500426085,40.5565871828995));
#65486=CARTESIAN_POINT('Ctrl Pts',(28.0092053572979,21.1450840336476,40.5612097490647));
#65487=CARTESIAN_POINT('Ctrl Pts',(28.005232547557,21.0723243759812,40.56583231523));
#65488=CARTESIAN_POINT('Ctrl Pts',(28.0052500576933,20.9995202423044,40.5704548813952));
#65489=CARTESIAN_POINT('Ctrl Pts',(28.0052500576935,20.9995202415483,40.5704548814432));
#65490=CARTESIAN_POINT('Ctrl Pts',(28.0052683089947,20.9236345912157,40.5752731029087));
#65491=CARTESIAN_POINT('Ctrl Pts',(28.0096214048906,20.8478643416663,40.5800913243742));
#65492=CARTESIAN_POINT('Ctrl Pts',(28.0182431153192,20.7726957710024,40.5849095458397));
#65493=CARTESIAN_POINT('Ctrl Pts',(28.0267660125351,20.6983887054913,40.5896725457867));
#65494=CARTESIAN_POINT('Ctrl Pts',(28.039459995078,20.624669945129,40.5944355457336));
#65495=CARTESIAN_POINT('Ctrl Pts',(28.0562100998338,20.5519951043663,40.5991985456806));
#65496=CARTESIAN_POINT('Ctrl Pts',(28.073251501954,20.4780563915336,40.6040443779053));
#65497=CARTESIAN_POINT('Ctrl Pts',(28.0944912867664,20.4051986394074,40.6088902101301));
#65498=CARTESIAN_POINT('Ctrl Pts',(28.1197571437131,20.3338811188068,40.6137360423549));
#65499=CARTESIAN_POINT('Ctrl Pts',(28.1450230006597,20.2625635982063,40.6185818745797));
#65500=CARTESIAN_POINT('Ctrl Pts',(28.1743146992191,20.1927866475378,40.6234277068045));
#65501=CARTESIAN_POINT('Ctrl Pts',(28.2074114249576,20.1249835640815,40.6282735390293));
#65502=CARTESIAN_POINT('Ctrl Pts',(28.237839065209,20.0626484603724,40.6327285791085));
#65503=CARTESIAN_POINT('Ctrl Pts',(28.2715819464657,20.0017796089535,40.6371836191876));
#65504=CARTESIAN_POINT('Ctrl Pts',(28.3084755457094,19.9427523549154,40.6416386592668));
#65505=CARTESIAN_POINT('Ctrl Pts',(28.3453138869145,19.8838135099876,40.6460870267312));
#65506=CARTESIAN_POINT('Ctrl Pts',(28.3852933225449,19.8267111993866,40.6505353941956));
#65507=CARTESIAN_POINT('Ctrl Pts',(28.4282026904114,19.7717977446405,40.6549837616599));
#65508=CARTESIAN_POINT('Ctrl Pts',(28.4710617211985,19.7169487089962,40.659426910734));
#65509=CARTESIAN_POINT('Ctrl Pts',(28.5168435577483,19.6642838129536,40.6638700598082));
#65510=CARTESIAN_POINT('Ctrl Pts',(28.5652938412495,19.6141263403386,40.6683132088823));
#65511=CARTESIAN_POINT('Ctrl Pts',(28.6137137452349,19.5640003176888,40.672753571993));
#65512=CARTESIAN_POINT('Ctrl Pts',(28.6647984377143,19.5163789505865,40.6771939351037));
#65513=CARTESIAN_POINT('Ctrl Pts',(28.7182543958363,19.4715511887188,40.6816342982144));
#65514=CARTESIAN_POINT('Ctrl Pts',(28.771694976291,19.4267363224464,40.6860733839665));
#65515=CARTESIAN_POINT('Ctrl Pts',(28.8275050934516,19.3847137802471,40.6905124697186));
#65516=CARTESIAN_POINT('Ctrl Pts',(28.8853569331097,19.345733275456,40.6949515554708));
#65517=CARTESIAN_POINT('Ctrl Pts',(28.9432117622251,19.306750756372,40.6993908706099));
#65518=CARTESIAN_POINT('Ctrl Pts',(29.0031081161784,19.2708108581908,40.7038301857489));
#65519=CARTESIAN_POINT('Ctrl Pts',(29.0646893841519,19.238119863787,40.708269500888));
#65520=CARTESIAN_POINT('Ctrl Pts',(29.1263357297013,19.205394322341,40.7127135073866));
#65521=CARTESIAN_POINT('Ctrl Pts',(29.1896701100956,19.1759247671806,40.7171575138852));
#65522=CARTESIAN_POINT('Ctrl Pts',(29.2543123668765,19.1498709460401,40.7216015203838));
#65523=CARTESIAN_POINT('Ctrl Pts',(29.3189924858195,19.123801864696,40.726048129819));
#65524=CARTESIAN_POINT('Ctrl Pts',(29.3849815429722,19.1011526583566,40.7304947392542));
#65525=CARTESIAN_POINT('Ctrl Pts',(29.4518831482747,19.0820335041105,40.7349413486894));
#65526=CARTESIAN_POINT('Ctrl Pts',(29.5189006482926,19.0628812294492,40.7393956610569));
#65527=CARTESIAN_POINT('Ctrl Pts',(29.5868333751877,19.0472713229655,40.7438499734244));
#65528=CARTESIAN_POINT('Ctrl Pts',(29.6552744543684,19.0352629029081,40.7483042857918));
#65529=CARTESIAN_POINT('Ctrl Pts',(29.6906143635875,19.0290622924009,40.7506042932812));
#65530=CARTESIAN_POINT('Ctrl Pts',(29.7260897191631,19.023821071248,40.7529043007707));
#65531=CARTESIAN_POINT('Ctrl Pts',(29.7616442822397,19.0195419433093,40.7552043082601));
#65532=CARTESIAN_POINT('Ctrl Pts',(29.8305123203823,19.0112534109636,40.7596593483394));
#65533=CARTESIAN_POINT('Ctrl Pts',(29.8999488406028,19.0065450387862,40.7641143884188));
#65534=CARTESIAN_POINT('Ctrl Pts',(29.9695493094053,19.0054824347872,40.7685694284981));
#65535=CARTESIAN_POINT('Ctrl Pts',(30.0390455328786,19.0044214223222,40.7730177959627));
#65536=CARTESIAN_POINT('Ctrl Pts',(30.1087047322639,19.0069953474599,40.7774661634272));
#65537=CARTESIAN_POINT('Ctrl Pts',(30.178116388894,19.0132181512538,40.7819145308917));
#65538=CARTESIAN_POINT('Ctrl Pts',(30.2474466185478,19.0194336550621,40.786357679966));
#65539=CARTESIAN_POINT('Ctrl Pts',(30.3165293971986,19.0292894922795,40.7908008290403));
#65540=CARTESIAN_POINT('Ctrl Pts',(30.3849551406269,19.042747562984,40.7952439781146));
#65541=CARTESIAN_POINT('Ctrl Pts',(30.4533379794362,19.0561971951482,40.7996843412254));
#65542=CARTESIAN_POINT('Ctrl Pts',(30.5210641213143,19.0732444857554,40.8041247043363));
#65543=CARTESIAN_POINT('Ctrl Pts',(30.5877315537106,19.093799805038,40.8085650674472));
#65544=CARTESIAN_POINT('Ctrl Pts',(30.6543798078969,19.1143492111752,40.8130041531995));
#65545=CARTESIAN_POINT('Ctrl Pts',(30.7199694898821,19.1384044984893,40.8174432389517));
#65546=CARTESIAN_POINT('Ctrl Pts',(30.7841129210272,19.1658259380369,40.821882324704));
#65547=CARTESIAN_POINT('Ctrl Pts',(30.8482596667434,19.19324879457,40.8263216398433));
#65548=CARTESIAN_POINT('Ctrl Pts',(30.9109595642926,19.2240379541205,40.8307609549825));
#65549=CARTESIAN_POINT('Ctrl Pts',(30.9718457742414,19.2580059260752,40.8352002701218));
#65550=CARTESIAN_POINT('Ctrl Pts',(31.0327963272459,19.2920097945508,40.8396442766205));
#65551=CARTESIAN_POINT('Ctrl Pts',(31.0919289390608,19.3291989413758,40.8440882831193));
#65552=CARTESIAN_POINT('Ctrl Pts',(31.1489030664204,19.3693408368179,40.848532289618));
#65553=CARTESIAN_POINT('Ctrl Pts',(31.2059105645774,19.4095062441086,40.8529788990534));
#65554=CARTESIAN_POINT('Ctrl Pts',(31.2607566771483,19.4526275398672,40.8574255084887));
#65555=CARTESIAN_POINT('Ctrl Pts',(31.3131336781127,19.4984316512705,40.8618721179241));
#65556=CARTESIAN_POINT('Ctrl Pts',(31.3656014125893,19.5443151098649,40.8663264302917));
#65557=CARTESIAN_POINT('Ctrl Pts',(31.415591146707,19.5928903200756,40.8707807426593));
#65558=CARTESIAN_POINT('Ctrl Pts',(31.4628323415477,19.6438476844314,40.875235055027));
#65559=CARTESIAN_POINT('Ctrl Pts',(31.4872255795846,19.6701597860337,40.8775350625149));
#65560=CARTESIAN_POINT('Ctrl Pts',(31.5108866574866,19.6971064860784,40.8798350700029));
#65561=CARTESIAN_POINT('Ctrl Pts',(31.53378277258,19.7246420231807,40.8821350774909));
#65562=CARTESIAN_POINT('Ctrl Pts',(31.5781318066283,19.7779774675345,40.8865901175699));
#65563=CARTESIAN_POINT('Ctrl Pts',(31.6197828555183,19.8337339849531,40.891045157649));
#65564=CARTESIAN_POINT('Ctrl Pts',(31.6584612012166,19.8916074672936,40.895500197728));
#65565=CARTESIAN_POINT('Ctrl Pts',(31.6970816157408,19.9493942686057,40.8999485651922));
#65566=CARTESIAN_POINT('Ctrl Pts',(31.7327378945137,20.0092913380924,40.9043969326564));
#65567=CARTESIAN_POINT('Ctrl Pts',(31.7651954599952,20.0709614913727,40.9088453001207));
#65568=CARTESIAN_POINT('Ctrl Pts',(31.7976149494309,20.1325592992524,40.9132884491947));
#65569=CARTESIAN_POINT('Ctrl Pts',(31.8268429516728,20.1959256287795,40.9177315982686));
#65570=CARTESIAN_POINT('Ctrl Pts',(31.8526891004231,20.2606958273665,40.9221747473426));
#65571=CARTESIAN_POINT('Ctrl Pts',(31.8785190430044,20.3254254134507,40.9266151104532));
#65572=CARTESIAN_POINT('Ctrl Pts',(31.900971157867,20.391556668908,40.9310554735637));
#65573=CARTESIAN_POINT('Ctrl Pts',(31.9199024640449,20.4587033243641,40.9354958366743));
#65574=CARTESIAN_POINT('Ctrl Pts',(31.9388283242568,20.5258306637523,40.9399349224263));
#65575=CARTESIAN_POINT('Ctrl Pts',(31.9542352537796,20.5939723525543,40.9443740081783));
#65576=CARTESIAN_POINT('Ctrl Pts',(31.9660301267147,20.6627269602383,40.9488130939303));
#65577=CARTESIAN_POINT('Ctrl Pts',(31.9778256091424,20.7314851207732,40.9532524090692));
#65578=CARTESIAN_POINT('Ctrl Pts',(31.9860085840666,20.8008557804161,40.9576917242082));
#65579=CARTESIAN_POINT('Ctrl Pts',(31.990537349335,20.8704290796422,40.9621310393471));
#65580=CARTESIAN_POINT('Ctrl Pts',(31.9950709004916,20.9400759022271,40.9665750458456));
#65581=CARTESIAN_POINT('Ctrl Pts',(31.9959425026353,21.0099253025877,40.9710190523441));
#65582=CARTESIAN_POINT('Ctrl Pts',(31.9931625535409,21.0795650530216,40.9754630588425));
#65583=CARTESIAN_POINT('Ctrl Pts',(31.990380976179,21.149245592742,40.9799096682776));
#65584=CARTESIAN_POINT('Ctrl Pts',(31.9839436357183,21.21871575079,40.9843562777126));
#65585=CARTESIAN_POINT('Ctrl Pts',(31.9739127943848,21.2875688485634,40.9888028871477));
#65586=CARTESIAN_POINT('Ctrl Pts',(31.9638645764652,21.3565412216538,40.993257199515));
#65587=CARTESIAN_POINT('Ctrl Pts',(31.9502105275691,21.424893921032,40.9977115118824));
#65588=CARTESIAN_POINT('Ctrl Pts',(31.9330637720797,21.4922316686004,41.0021658242497));
#65589=CARTESIAN_POINT('Ctrl Pts',(31.9242099551909,21.5270018667896,41.0044658317404));
#65590=CARTESIAN_POINT('Ctrl Pts',(31.9144257150367,21.5615017203884,41.006765839231));
#65591=CARTESIAN_POINT('Ctrl Pts',(31.9037316734446,21.5956788379855,41.0090658467216));
#65592=CARTESIAN_POINT('Ctrl Pts',(31.8830176609496,21.6618788087689,41.0135208868007));
#65593=CARTESIAN_POINT('Ctrl Pts',(31.8588057035532,21.7271274120279,41.0179759268797));
#65594=CARTESIAN_POINT('Ctrl Pts',(31.8312020468742,21.7910288401972,41.0224309669588));
#65595=CARTESIAN_POINT('Ctrl Pts',(31.8036397340587,21.8548345588758,41.026879334423));
#65596=CARTESIAN_POINT('Ctrl Pts',(31.7726959971272,21.9172966617358,41.0313277018872));
#65597=CARTESIAN_POINT('Ctrl Pts',(31.7385266512765,21.9780350941051,41.0357760693514));
#65598=CARTESIAN_POINT('Ctrl Pts',(31.7043973895652,22.0387022740778,41.0402192184254));
#65599=CARTESIAN_POINT('Ctrl Pts',(31.6670502732538,22.0976493752445,41.0446623674994));
#65600=CARTESIAN_POINT('Ctrl Pts',(31.6266881875033,22.1545185590267,41.0491055165734));
#65601=CARTESIAN_POINT('Ctrl Pts',(31.5863514097704,22.2113520844361,41.053545879684));
#65602=CARTESIAN_POINT('Ctrl Pts',(31.5430036954772,22.2661098790928,41.0579862427945));
#65603=CARTESIAN_POINT('Ctrl Pts',(31.4968918089427,22.3184621628323,41.0624266059051));
#65604=CARTESIAN_POINT('Ctrl Pts',(31.4507931874074,22.3707993863984,41.0668656916571));
#65605=CARTESIAN_POINT('Ctrl Pts',(31.4019322954712,22.4207321058244,41.071304777409));
#65606=CARTESIAN_POINT('Ctrl Pts',(31.3505956959991,22.4679641781899,41.075743863161));
#65607=CARTESIAN_POINT('Ctrl Pts',(31.2992564437407,22.5151986912429,41.0801831783));
#65608=CARTESIAN_POINT('Ctrl Pts',(31.2454415916704,22.5597319506625,41.0846224934389));
#65609=CARTESIAN_POINT('Ctrl Pts',(31.1894726991707,22.6013064230271,41.0890618085779));
#65610=CARTESIAN_POINT('Ctrl Pts',(31.1334446601159,22.6429248302758,41.0935058150763));
#65611=CARTESIAN_POINT('Ctrl Pts',(31.0752584308543,22.681577917414,41.0979498215748));
#65612=CARTESIAN_POINT('Ctrl Pts',(31.0152658445187,22.7170506187803,41.1023938280732));
#65613=CARTESIAN_POINT('Ctrl Pts',(30.9552381194187,22.7525440971621,41.1068404375083));
#65614=CARTESIAN_POINT('Ctrl Pts',(30.893402365152,22.7848532553943,41.1112870469433));
#65615=CARTESIAN_POINT('Ctrl Pts',(30.8301339118456,22.8138095960998,41.1157336563784));
#65616=CARTESIAN_POINT('Ctrl Pts',(30.7667558575907,22.8428160983352,41.1201879687457));
#65617=CARTESIAN_POINT('Ctrl Pts',(30.7019406050655,22.8684580094109,41.124642281113));
#65618=CARTESIAN_POINT('Ctrl Pts',(30.636081523246,22.8906157352262,41.1290965934804));
#65619=CARTESIAN_POINT('Ctrl Pts',(30.60207484185,22.9020569928546,41.131396600971));
#65620=CARTESIAN_POINT('Ctrl Pts',(30.5677900702718,22.9125701128308,41.1336966084617));
#65621=CARTESIAN_POINT('Ctrl Pts',(30.5332824022933,22.9221439701293,41.1359966159524));
#65622=CARTESIAN_POINT('Ctrl Pts',(30.4664614855868,22.9406828618764,41.140450368349));
#65623=CARTESIAN_POINT('Ctrl Pts',(30.3985411344477,22.9557696878217,41.1449041207455));
#65624=CARTESIAN_POINT('Ctrl Pts',(30.3299110872441,22.9672788915183,41.1493578731421));
#65625=CARTESIAN_POINT('Ctrl Pts',(30.2613748664854,22.9787723605956,41.153805536664));
#65626=CARTESIAN_POINT('Ctrl Pts',(30.1921313521205,22.9866978282039,41.1582532001859));
#65627=CARTESIAN_POINT('Ctrl Pts',(30.1225841092882,22.990979833813,41.1627008637079));
#65628=CARTESIAN_POINT('Ctrl Pts',(30.0531083380928,22.9952574389321,41.167143956498));
#65629=CARTESIAN_POINT('Ctrl Pts',(29.9833299435588,22.9958989814401,41.1715870492882));
#65630=CARTESIAN_POINT('Ctrl Pts',(29.9136595662431,22.9928805513624,41.1760301420784));
#65631=CARTESIAN_POINT('Ctrl Pts',(29.8440371407194,22.9898641987693,41.1804701768363));
#65632=CARTESIAN_POINT('Ctrl Pts',(29.77452307242,22.9831928958928,41.1849102115942));
#65633=CARTESIAN_POINT('Ctrl Pts',(29.7055281883306,22.9728948057695,41.1893502463521));
#65634=CARTESIAN_POINT('Ctrl Pts',(29.6365382419028,22.9625974526353,41.1937899633562));
#65635=CARTESIAN_POINT('Ctrl Pts',(29.5680678916448,22.9486738865793,41.1982296803603));
#65636=CARTESIAN_POINT('Ctrl Pts',(29.5005215894561,22.9312039974846,41.2026693973643));
#65637=CARTESIAN_POINT('Ctrl Pts',(29.4329784865895,22.913734935849,41.2071089040818));
#65638=CARTESIAN_POINT('Ctrl Pts',(29.3663598166088,22.8927200155239,41.2115484107992));
#65639=CARTESIAN_POINT('Ctrl Pts',(29.3010564866216,22.8682894656895,41.2159879175166));
#65640=CARTESIAN_POINT('Ctrl Pts',(29.2357051510874,22.8438409565579,41.2204306877882));
#65641=CARTESIAN_POINT('Ctrl Pts',(29.1716715406158,22.8159719870887,41.2248734580597));
#65642=CARTESIAN_POINT('Ctrl Pts',(29.109326978281,22.7848610956828,41.2293162283312));
#65643=CARTESIAN_POINT('Ctrl Pts',(29.082054240405,22.7712515818034,41.2312597259599));
#65644=CARTESIAN_POINT('Ctrl Pts',(29.0551044216415,22.7570222820631,41.2332032235885));
#65645=CARTESIAN_POINT('Ctrl Pts',(29.0285070491141,22.7421908646526,41.2351467212172));
#65646=CARTESIAN_POINT('Origin',(30.,21.,34.5704548813952));
#65647=CARTESIAN_POINT('',(29.0285070576893,22.7421908694344,42.1950453911705));
#65648=CARTESIAN_POINT('',(29.0271745210922,22.7445458878821,42.0352855536299));
#65649=CARTESIAN_POINT('',(29.0285070491141,22.7421908646526,34.5704548813952));
#65650=CARTESIAN_POINT('',(28.0052507199072,21.0016947180269,41.5280186851748));
#65651=CARTESIAN_POINT('Ctrl Pts',(29.0285070576893,22.7421908694344,42.1950453911705));
#65652=CARTESIAN_POINT('Ctrl Pts',(29.0854792583077,22.7739601157206,42.1907449642306));
#65653=CARTESIAN_POINT('Ctrl Pts',(29.1439752931866,22.8029155541729,42.1863498638858));
#65654=CARTESIAN_POINT('Ctrl Pts',(29.3655541149389,22.8993774258534,42.1698050565103));
#65655=CARTESIAN_POINT('Ctrl Pts',(29.5359371700845,22.9480240136795,42.1572042394495));
#65656=CARTESIAN_POINT('Ctrl Pts',(29.7330985378328,22.9769454511594,42.1438578658572));
#65657=CARTESIAN_POINT('Ctrl Pts',(29.7557635613907,22.9798733229191,42.1423429272947));
#65658=CARTESIAN_POINT('Ctrl Pts',(29.7900295861683,22.9837023878216,42.1400865505333));
#65659=CARTESIAN_POINT('Ctrl Pts',(29.8015955895226,22.9848925522928,42.1393307627143));
#65660=CARTESIAN_POINT('Ctrl Pts',(29.8228757329182,22.9868944507893,42.1379516997219));
#65661=CARTESIAN_POINT('Ctrl Pts',(29.8325859795035,22.9877361785976,42.1373269090836));
#65662=CARTESIAN_POINT('Ctrl Pts',(29.8554941476766,22.9895528973066,42.1358630758892));
#65663=CARTESIAN_POINT('Ctrl Pts',(29.8686961576703,22.9904677832751,42.1350273108511));
#65664=CARTESIAN_POINT('Ctrl Pts',(29.9139391467252,22.9931509670232,42.1321870180222));
#65665=CARTESIAN_POINT('Ctrl Pts',(29.9460148028531,22.994277590147,42.1302142611265));
#65666=CARTESIAN_POINT('Ctrl Pts',(30.0282429090343,22.9951801797665,42.1252300491227));
#65667=CARTESIAN_POINT('Ctrl Pts',(30.0783862285429,22.9938399668942,42.1222600106318));
#65668=CARTESIAN_POINT('Ctrl Pts',(30.2914814672339,22.9800916780811,42.1097421136857));
#65669=CARTESIAN_POINT('Ctrl Pts',(30.4526150172587,22.9495803530892,42.1004796416621));
#65670=CARTESIAN_POINT('Ctrl Pts',(30.6413450741328,22.8891568134121,42.0884860594092));
#65671=CARTESIAN_POINT('Ctrl Pts',(30.6741809894842,22.8776892041139,42.0863578583756));
#65672=CARTESIAN_POINT('Ctrl Pts',(30.7268250480488,22.8577448983522,42.0828678269669));
#65673=CARTESIAN_POINT('Ctrl Pts',(30.7468257299362,22.8497951319066,42.0815232840372));
#65674=CARTESIAN_POINT('Ctrl Pts',(30.782537780389,22.8349269055818,42.0790868726022));
#65675=CARTESIAN_POINT('Ctrl Pts',(30.7982960691763,22.8281262216976,42.0779990805245));
#65676=CARTESIAN_POINT('Ctrl Pts',(30.8319988833424,22.8130625040648,42.0756441557654));
#65677=CARTESIAN_POINT('Ctrl Pts',(30.8499122205849,22.8047345944107,42.0743748801514));
#65678=CARTESIAN_POINT('Ctrl Pts',(30.8998279938788,22.780620782443,42.0707869002768));
#65679=CARTESIAN_POINT('Ctrl Pts',(30.9315334855326,22.7642408804795,42.0684478899974));
#65680=CARTESIAN_POINT('Ctrl Pts',(31.0028444764471,22.7249414697906,42.0630456633661));
#65681=CARTESIAN_POINT('Ctrl Pts',(31.042133918142,22.7014924352787,42.059965722005));
#65682=CARTESIAN_POINT('Ctrl Pts',(31.1883196932924,22.6072811509133,42.0481153513728));
#65683=CARTESIAN_POINT('Ctrl Pts',(31.289110859743,22.5276272236387,42.03909605874));
#65684=CARTESIAN_POINT('Ctrl Pts',(31.4306298341418,22.3917452011373,42.0254970384011));
#65685=CARTESIAN_POINT('Ctrl Pts',(31.4772678700464,22.3421392765494,42.0208337418266));
#65686=CARTESIAN_POINT('Ctrl Pts',(31.532356790015,22.2771857078011,42.0151828808977));
#65687=CARTESIAN_POINT('Ctrl Pts',(31.5432623729052,22.2639865346639,42.0140566645001));
#65688=CARTESIAN_POINT('Ctrl Pts',(31.5605445987023,22.2425124450626,42.0122618131222));
#65689=CARTESIAN_POINT('Ctrl Pts',(31.5670282944917,22.2343253043438,42.0115860717325));
#65690=CARTESIAN_POINT('Ctrl Pts',(31.5797402770202,22.2180119175215,42.0102570952762));
#65691=CARTESIAN_POINT('Ctrl Pts',(31.5859708503648,22.2098879471206,42.0096037272472));
#65692=CARTESIAN_POINT('Ctrl Pts',(31.6018697178634,22.1888237367504,42.0079302731877));
#65693=CARTESIAN_POINT('Ctrl Pts',(31.6114441159566,22.1758130679173,42.0069164367508));
#65694=CARTESIAN_POINT('Ctrl Pts',(31.6549645062409,22.1151428728462,42.0022721767189));
#65695=CARTESIAN_POINT('Ctrl Pts',(31.6869641156262,22.0661165474519,41.9987534821668));
#65696=CARTESIAN_POINT('Ctrl Pts',(31.7975251181402,21.879252442424,41.9859126497666));
#65697=CARTESIAN_POINT('Ctrl Pts',(31.86171905515,21.7336120045203,41.9769581353581));
#65698=CARTESIAN_POINT('Ctrl Pts',(31.9231563421516,21.532166263567,41.9643819188724));
#65699=CARTESIAN_POINT('Ctrl Pts',(31.9363732131816,21.4818603148071,41.9612315449816));
#65700=CARTESIAN_POINT('Ctrl Pts',(31.9521370706143,21.4106426182462,41.9567250727164));
#65701=CARTESIAN_POINT('Ctrl Pts',(31.9563422126151,21.3901174153546,41.955421059717));
#65702=CARTESIAN_POINT('Ctrl Pts',(31.9634539678793,21.3523921606852,41.9530127090358));
#65703=CARTESIAN_POINT('Ctrl Pts',(31.9664597845024,21.3352127735774,41.9519116288995));
#65704=CARTESIAN_POINT('Ctrl Pts',(31.9721450412747,21.3000060011607,41.9496451909598));
#65705=CARTESIAN_POINT('Ctrl Pts',(31.9748034420974,21.281976937325,41.9484792783824));
#65706=CARTESIAN_POINT('Ctrl Pts',(31.9809284737358,21.2360889609737,41.9454972673732));
#65707=CARTESIAN_POINT('Ctrl Pts',(31.9840545994372,21.2081894061873,41.9436706619595));
#65708=CARTESIAN_POINT('Ctrl Pts',(31.997340471984,21.0617489607251,41.9340076080548));
#65709=CARTESIAN_POINT('Ctrl Pts',(31.9974669252414,20.942558243678,41.9258633389905));
#65710=CARTESIAN_POINT('Ctrl Pts',(31.9752852508737,20.692015054224,41.9083652407192));
#65711=CARTESIAN_POINT('Ctrl Pts',(31.9504539000925,20.5614335932811,41.8990215166364));
#65712=CARTESIAN_POINT('Ctrl Pts',(31.9072677427889,20.415410968998,41.8888722698805));
#65713=CARTESIAN_POINT('Ctrl Pts',(31.9014094089873,20.3966287155427,41.8875732460272));
#65714=CARTESIAN_POINT('Ctrl Pts',(31.8918485053776,20.3674990548923,41.8855718905294));
#65715=CARTESIAN_POINT('Ctrl Pts',(31.8883368633434,20.3570908950897,41.884859475448));
#65716=CARTESIAN_POINT('Ctrl Pts',(31.8814923219848,20.3373443577485,41.8835136903615));
#65717=CARTESIAN_POINT('Ctrl Pts',(31.8781755322226,20.3280010926377,41.8828795008129));
#65718=CARTESIAN_POINT('Ctrl Pts',(31.8698514839027,20.3050957048882,41.8813303799502));
#65719=CARTESIAN_POINT('Ctrl Pts',(31.8647660819367,20.2915622540395,41.8804199262898));
#65720=CARTESIAN_POINT('Ctrl Pts',(31.8446814841133,20.2398276596656,41.8769537661241));
#65721=CARTESIAN_POINT('Ctrl Pts',(31.8286509185866,20.2020350341443,41.8744516772497));
#65722=CARTESIAN_POINT('Ctrl Pts',(31.7804508717148,20.0974988447337,41.867543902965));
#65723=CARTESIAN_POINT('Ctrl Pts',(31.7457129571354,20.0320117476545,41.8632305525037));
#65724=CARTESIAN_POINT('Ctrl Pts',(31.6358457186826,19.8501332449017,41.8508947001353));
#65725=CARTESIAN_POINT('Ctrl Pts',(31.5521522836659,19.739443080927,41.8429121443202));
#65726=CARTESIAN_POINT('Ctrl Pts',(31.4356373353596,19.6147146035595,41.8325072146796));
#65727=CARTESIAN_POINT('Ctrl Pts',(31.4130265388364,19.591658419086,41.8305175287726));
#65728=CARTESIAN_POINT('Ctrl Pts',(31.3761837512508,19.5558705935481,41.8273138029325));
#65729=CARTESIAN_POINT('Ctrl Pts',(31.362310872503,19.5427764392133,41.8261157028677));
#65730=CARTESIAN_POINT('Ctrl Pts',(31.3355178742106,19.5182044170064,41.8238158920642));
#65731=CARTESIAN_POINT('Ctrl Pts',(31.3226321637883,19.5066915018879,41.8227158265741));
#65732=CARTESIAN_POINT('Ctrl Pts',(31.2924989673542,19.4804645789996,41.8201560691812));
#65733=CARTESIAN_POINT('Ctrl Pts',(31.2751472438717,19.465874544796,41.8186914407425));
#65734=CARTESIAN_POINT('Ctrl Pts',(31.2168708821208,19.4185452070709,41.8138009479045));
#65735=CARTESIAN_POINT('Ctrl Pts',(31.1749077579804,19.3871252566718,41.8103241287133));
#65736=CARTESIAN_POINT('Ctrl Pts',(31.0657587094978,19.3119212179909,41.80138928608));
#65737=CARTESIAN_POINT('Ctrl Pts',(30.997082897908,19.2704696470217,41.7958627127323));
#65738=CARTESIAN_POINT('Ctrl Pts',(30.8099243345128,19.1723629334995,41.781158929487));
#65739=CARTESIAN_POINT('Ctrl Pts',(30.6880124538335,19.1230668956076,41.7719184413867));
#65740=CARTESIAN_POINT('Ctrl Pts',(30.5431036339228,19.0805053964918,41.7618494411781));
#65741=CARTESIAN_POINT('Ctrl Pts',(30.5239868937176,19.0751989981917,41.7605392394785));
#65742=CARTESIAN_POINT('Ctrl Pts',(30.4941335506915,19.0673901060209,41.7585245907541));
#65743=CARTESIAN_POINT('Ctrl Pts',(30.483450542721,19.0646900623252,41.757809854374));
#65744=CARTESIAN_POINT('Ctrl Pts',(30.4631265598757,19.0597321370007,41.7564625700918));
#65745=CARTESIAN_POINT('Ctrl Pts',(30.453490405073,19.0574573243894,41.7558291625399));
#65746=CARTESIAN_POINT('Ctrl Pts',(30.4298229632205,19.0520558476672,41.7542858809167));
#65747=CARTESIAN_POINT('Ctrl Pts',(30.4157737603982,19.0490088649463,41.7533804023033));
#65748=CARTESIAN_POINT('Ctrl Pts',(30.3621474427258,19.0379840244455,41.7499602719406));
#65749=CARTESIAN_POINT('Ctrl Pts',(30.3223618334492,19.0310559202059,41.7474974240678));
#65750=CARTESIAN_POINT('Ctrl Pts',(30.2110785107331,19.0151416088073,41.7407469865064));
#65751=CARTESIAN_POINT('Ctrl Pts',(30.1392618316289,19.0088133214595,41.7365467832774));
#65752=CARTESIAN_POINT('Ctrl Pts',(29.9255007044258,19.0016019008581,41.7241253509934));
#65753=CARTESIAN_POINT('Ctrl Pts',(29.7836536934932,19.0119519527643,41.7159568533099));
#65754=CARTESIAN_POINT('Ctrl Pts',(29.6126232056761,19.0429638034668,41.7053569066981));
#65755=CARTESIAN_POINT('Ctrl Pts',(29.5812816623526,19.0494292544733,41.7033846051779));
#65756=CARTESIAN_POINT('Ctrl Pts',(29.5315833374115,19.0609344923361,41.7002021564832));
#65757=CARTESIAN_POINT('Ctrl Pts',(29.5131190317759,19.0654881505653,41.6990075682109));
#65758=CARTESIAN_POINT('Ctrl Pts',(29.4779922470621,19.0746858481063,41.6967101892921));
#65759=CARTESIAN_POINT('Ctrl Pts',(29.4613194771584,19.0792840030507,41.6956089782982));
#65760=CARTESIAN_POINT('Ctrl Pts',(29.4228185543607,19.0904428294336,41.6930400463941));
#65761=CARTESIAN_POINT('Ctrl Pts',(29.4010392206151,19.0971618770781,41.6915672727094));
#65762=CARTESIAN_POINT('Ctrl Pts',(29.3288036766819,19.1208099543033,41.686614839902));
#65763=CARTESIAN_POINT('Ctrl Pts',(29.278913983689,19.1393834829689,41.6830824118109));
#65764=CARTESIAN_POINT('Ctrl Pts',(29.1540327948212,19.1916530308638,41.6739508525793));
#65765=CARTESIAN_POINT('Ctrl Pts',(29.0802747338343,19.2280286292672,41.6682790097745));
#65766=CARTESIAN_POINT('Ctrl Pts',(28.89837950467,19.332157149726,41.6536871414908));
#65767=CARTESIAN_POINT('Ctrl Pts',(28.794098402385,19.4059256224598,41.6447204715145));
#65768=CARTESIAN_POINT('Ctrl Pts',(28.6824612400831,19.5021626417024,41.6348886727058));
#65769=CARTESIAN_POINT('Ctrl Pts',(28.6675542896391,19.5154079224363,41.6335710170597));
#65770=CARTESIAN_POINT('Ctrl Pts',(28.6446213914946,19.5364082493885,41.6315397116697));
#65771=CARTESIAN_POINT('Ctrl Pts',(28.6364580753141,19.5440105018075,41.6308157808403));
#65772=CARTESIAN_POINT('Ctrl Pts',(28.6212044328101,19.5584565777869,41.6294621830501));
#65773=CARTESIAN_POINT('Ctrl Pts',(28.6141007309128,19.5652847412564,41.6288315222547));
#65774=CARTESIAN_POINT('Ctrl Pts',(28.596973994507,19.5819930734273,41.6273096827627));
#65775=CARTESIAN_POINT('Ctrl Pts',(28.5870044308445,19.5919271452122,41.626422619032));
#65776=CARTESIAN_POINT('Ctrl Pts',(28.550507486961,19.629072187355,41.623166874149));
#65777=CARTESIAN_POINT('Ctrl Pts',(28.5246525484343,19.6569356231421,41.6208437908591));
#65778=CARTESIAN_POINT('Ctrl Pts',(28.4566557939539,19.7345495922136,41.6146321363021));
#65779=CARTESIAN_POINT('Ctrl Pts',(28.4161298953124,19.7856554791639,41.6108150558015));
#65780=CARTESIAN_POINT('Ctrl Pts',(28.2881610496036,19.9643647665012,41.5980267801062));
#65781=CARTESIAN_POINT('Ctrl Pts',(28.2130735011121,20.1000987145098,41.5891682031628));
#65782=CARTESIAN_POINT('Ctrl Pts',(28.1428416569309,20.2713569466394,41.5778585571733));
#65783=CARTESIAN_POINT('Ctrl Pts',(28.131918387685,20.2998366285736,41.5759757245373));
#65784=CARTESIAN_POINT('Ctrl Pts',(28.1153538122592,20.3461754910199,41.5729027143206));
#65785=CARTESIAN_POINT('Ctrl Pts',(28.1093033232988,20.3638838313413,41.5717261950309));
#65786=CARTESIAN_POINT('Ctrl Pts',(28.0981115402182,20.3982106908914,41.569440098028));
#65787=CARTESIAN_POINT('Ctrl Pts',(28.0929367157205,20.4148165379885,41.5683317491421));
#65788=CARTESIAN_POINT('Ctrl Pts',(28.0812836391893,20.4540081436009,41.5657092578049));
#65789=CARTESIAN_POINT('Ctrl Pts',(28.0749861025505,20.4766444834098,41.5641893847547));
#65790=CARTESIAN_POINT('Ctrl Pts',(28.0624938764999,20.5248280403254,41.560941896681));
#65791=CARTESIAN_POINT('Ctrl Pts',(28.0564014459874,20.5503969265444,41.5592113567689));
#65792=CARTESIAN_POINT('Ctrl Pts',(28.0204000915491,20.7159302500691,41.5479593609565));
#65793=CARTESIAN_POINT('Ctrl Pts',(28.005129170239,20.8586260132183,41.5379938008639));
#65794=CARTESIAN_POINT('Ctrl Pts',(28.0052507199072,21.0016947180269,41.5280186851748));
#65795=CARTESIAN_POINT('Ctrl Pts',(28.0052507211432,21.0016961722432,41.5280185837832));
#65796=CARTESIAN_POINT('Ctrl Pts',(28.0053114286813,21.0730900524378,41.5230408202257));
#65797=CARTESIAN_POINT('Ctrl Pts',(28.0092049813008,21.1444349284456,41.5180794287087));
#65798=CARTESIAN_POINT('Ctrl Pts',(28.0201568552617,21.2452530317649,41.5112009530846));
#65799=CARTESIAN_POINT('Ctrl Pts',(28.024070228267,21.2750084999931,41.5091877146635));
#65800=CARTESIAN_POINT('Ctrl Pts',(28.0304079739908,21.3160169869038,41.5064463739901));
#65801=CARTESIAN_POINT('Ctrl Pts',(28.032260291741,21.3273529287226,41.5056921296246));
#65802=CARTESIAN_POINT('Ctrl Pts',(28.0360428796999,21.34930856676,41.5042389909577));
#65803=CARTESIAN_POINT('Ctrl Pts',(28.0379616299795,21.3599298443959,41.5035395268314));
#65804=CARTESIAN_POINT('Ctrl Pts',(28.0418028948491,21.3802491155316,41.5022088113297));
#65805=CARTESIAN_POINT('Ctrl Pts',(28.0437114354257,21.3899491614671,41.5015768698837));
#65806=CARTESIAN_POINT('Ctrl Pts',(28.0486689221581,21.4141924365203,41.5000049579393));
#65807=CARTESIAN_POINT('Ctrl Pts',(28.0518084789715,21.4287168978923,41.4990699543093));
#65808=CARTESIAN_POINT('Ctrl Pts',(28.064228118828,21.4832172035529,41.4955823287349));
#65809=CARTESIAN_POINT('Ctrl Pts',(28.0745793336854,21.5229411041993,41.493082499017));
#65810=CARTESIAN_POINT('Ctrl Pts',(28.1213620122769,21.6821654399037,41.4831307490119));
#65811=CARTESIAN_POINT('Ctrl Pts',(28.1677557539872,21.7984458236206,41.4760057875152));
#65812=CARTESIAN_POINT('Ctrl Pts',(28.268801882108,21.9956522735064,41.4630809939904));
#65813=CARTESIAN_POINT('Ctrl Pts',(28.3190683852499,22.0783488361528,41.4573661155972));
#65814=CARTESIAN_POINT('Ctrl Pts',(28.3909093586371,22.1792350051902,41.4497638447516));
#65815=CARTESIAN_POINT('Ctrl Pts',(28.4071433317298,22.2010726093318,41.4480779562521));
#65816=CARTESIAN_POINT('Ctrl Pts',(28.4348831101777,22.2368357242988,41.4452446510711));
#65817=CARTESIAN_POINT('Ctrl Pts',(28.4461407761387,22.2509496255342,41.4441070502393));
#65818=CARTESIAN_POINT('Ctrl Pts',(28.4687232730475,22.278486409935,41.441847652925));
#65819=CARTESIAN_POINT('Ctrl Pts',(28.4800368777491,22.2919164018396,41.4407263740635));
#65820=CARTESIAN_POINT('Ctrl Pts',(28.5055595812257,22.3214141673056,41.4382192448285));
#65821=CARTESIAN_POINT('Ctrl Pts',(28.5198533369712,22.3374054595144,41.4368299550113));
#65822=CARTESIAN_POINT('Ctrl Pts',(28.5730084646564,22.3949772993208,41.4317148626857));
#65823=CARTESIAN_POINT('Ctrl Pts',(28.6133835493182,22.4351168174772,41.4279258127185));
#65824=CARTESIAN_POINT('Ctrl Pts',(28.768491774527,22.5766573031777,41.4137119258405));
#65825=CARTESIAN_POINT('Ctrl Pts',(28.8930648978236,22.6664772578702,41.4028930290831));
#65826=CARTESIAN_POINT('Ctrl Pts',(29.0272737978734,22.7415027409708,41.3922841321572));
#65827=CARTESIAN_POINT('Ctrl Pts',(29.0278903335763,22.7418469673163,41.3922354182994));
#65828=CARTESIAN_POINT('Ctrl Pts',(29.0285070491341,22.7421908646638,41.392186712139));
#65829=CARTESIAN_POINT('',(28.0044538746745,20.9984594462732,41.3704548663374));
#65830=CARTESIAN_POINT('Ctrl Pts',(29.0285070491141,22.7421908646526,41.2351467212172));
#65831=CARTESIAN_POINT('Ctrl Pts',(28.9651425374846,22.7068570917387,41.2397768318782));
#65832=CARTESIAN_POINT('Ctrl Pts',(28.9037810321329,22.6681026511783,41.2444069425392));
#65833=CARTESIAN_POINT('Ctrl Pts',(28.8447961328331,22.6262015827635,41.2490370532002));
#65834=CARTESIAN_POINT('Ctrl Pts',(28.7858112335333,22.5843005143488,41.2536671638612));
#65835=CARTESIAN_POINT('Ctrl Pts',(28.7292033575836,22.5392532443536,41.2582972745222));
#65836=CARTESIAN_POINT('Ctrl Pts',(28.6753044888271,22.4913783440758,41.2629273851832));
#65837=CARTESIAN_POINT('Ctrl Pts',(28.6231494286428,22.4450523568536,41.2674076962872));
#65838=CARTESIAN_POINT('Ctrl Pts',(28.5733076698616,22.3958804966255,41.2718880073913));
#65839=CARTESIAN_POINT('Ctrl Pts',(28.5261114495448,22.3441280085382,41.2763683184953));
#65840=CARTESIAN_POINT('Ctrl Pts',(28.4799540166452,22.2935145911874,41.2807500180841));
#65841=CARTESIAN_POINT('Ctrl Pts',(28.436327239288,22.2404333591896,41.2851317176728));
#65842=CARTESIAN_POINT('Ctrl Pts',(28.3955086691601,22.1851730387414,41.2895134172616));
#65843=CARTESIAN_POINT('Ctrl Pts',(28.3547289586535,22.129965326582,41.2938909454356));
#65844=CARTESIAN_POINT('Ctrl Pts',(28.3167524558851,22.0725830411258,41.2982684736096));
#65845=CARTESIAN_POINT('Ctrl Pts',(28.2818174815142,22.0133490986179,41.3026460017836));
#65846=CARTESIAN_POINT('Ctrl Pts',(28.246903085809,21.9541500482354,41.3070209513471));
#65847=CARTESIAN_POINT('Ctrl Pts',(28.2150269218007,21.8931019378278,41.3113959009107));
#65848=CARTESIAN_POINT('Ctrl Pts',(28.1863837422199,21.830556218456,41.3157708504743));
#65849=CARTESIAN_POINT('Ctrl Pts',(28.1565486617622,21.7654078446699,41.3203278505747));
#65850=CARTESIAN_POINT('Ctrl Pts',(28.1302218414353,21.69863498356,41.3248848506752));
#65851=CARTESIAN_POINT('Ctrl Pts',(28.1075691378912,21.6306607603444,41.3294418507757));
#65852=CARTESIAN_POINT('Ctrl Pts',(28.0858128238294,21.565376343166,41.3338185259559));
#65853=CARTESIAN_POINT('Ctrl Pts',(28.0674454079982,21.4989843838444,41.3381952011361));
#65854=CARTESIAN_POINT('Ctrl Pts',(28.0525629153372,21.4318754030736,41.3425718763163));
#65855=CARTESIAN_POINT('Ctrl Pts',(28.0376744065389,21.3647392939949,41.346950320735));
#65856=CARTESIAN_POINT('Ctrl Pts',(28.0262737087772,21.296886084571,41.3513287651536));
#65857=CARTESIAN_POINT('Ctrl Pts',(28.0184053946828,21.2287146315338,41.3557072095723));
#65858=CARTESIAN_POINT('Ctrl Pts',(28.0105272702415,21.1604581811784,41.3600911131094));
#65859=CARTESIAN_POINT('Ctrl Pts',(28.0061903409452,21.0918831990938,41.3644750166465));
#65860=CARTESIAN_POINT('Ctrl Pts',(28.0053871417482,21.0233903440865,41.3688589201836));
#65861=CARTESIAN_POINT('Ctrl Pts',(28.0052896752714,21.015078885006,41.369390897349));
#65862=CARTESIAN_POINT('Ctrl Pts',(28.0052441811847,21.0067686302078,41.3699228745145));
#65863=CARTESIAN_POINT('Ctrl Pts',(28.0052505942364,20.9984602903498,41.3704548516799));
#65864=CARTESIAN_POINT('Ctrl Pts',(28.0036353960762,20.9984585791442,41.3704548813952));
#65865=CARTESIAN_POINT('Ctrl Pts',(28.0027728315258,20.8973635887888,41.3769226390681));
#65866=CARTESIAN_POINT('Ctrl Pts',(28.0556922101652,20.1358392039252,41.4257006531513));
#65867=CARTESIAN_POINT('Ctrl Pts',(29.0356112395522,18.849087513172,41.5167889236447));
#65868=CARTESIAN_POINT('Ctrl Pts',(31.2827680785228,19.0223811625417,41.6437196928755));
#65869=CARTESIAN_POINT('Ctrl Pts',(32.3572138429301,21.0036208900697,41.7706504621062));
#65870=CARTESIAN_POINT('Ctrl Pts',(31.2766864430049,22.9815503837979,41.8975812313371));
#65871=CARTESIAN_POINT('Ctrl Pts',(29.7146416622772,23.0971840712568,41.9857929285116));
#65872=CARTESIAN_POINT('Ctrl Pts',(29.0759511139292,22.7721646846317,42.0316943692759));
#65873=CARTESIAN_POINT('Ctrl Pts',(29.0271745210922,22.7445458878821,42.0352855536299));
#65874=CARTESIAN_POINT('Origin',(30.,21.,34.5704548813952));
#65875=CARTESIAN_POINT('',(29.0285070614011,22.7421908715042,42.9937555338539));
#65876=CARTESIAN_POINT('',(29.0285070491141,22.7421908646526,42.8352639371872));
#65877=CARTESIAN_POINT('',(29.0285070491141,22.7421908646526,34.5704548813952));
#65878=CARTESIAN_POINT('Ctrl Pts',(29.0285070614011,22.7421908715042,42.9937555338539));
#65879=CARTESIAN_POINT('Ctrl Pts',(29.1131722975557,22.789402506242,42.9881031452504));
#65880=CARTESIAN_POINT('Ctrl Pts',(29.2011688053936,22.8303812505968,42.9823747536447));
#65881=CARTESIAN_POINT('Ctrl Pts',(29.3176329582475,22.8746109505119,42.9747325540344));
#65882=CARTESIAN_POINT('Ctrl Pts',(29.3436632446347,22.8838824121997,42.9730214274946));
#65883=CARTESIAN_POINT('Ctrl Pts',(29.387083207794,22.8983386021807,42.97015763768));
#65884=CARTESIAN_POINT('Ctrl Pts',(29.404366512354,22.9038322289906,42.9690152592499));
#65885=CARTESIAN_POINT('Ctrl Pts',(29.4384672122926,22.9141615985903,42.9667553504867));
#65886=CARTESIAN_POINT('Ctrl Pts',(29.4552781085389,22.9190132167238,42.9656384597143));
#65887=CARTESIAN_POINT('Ctrl Pts',(29.4964416297771,22.9303085331049,42.9628958171125));
#65888=CARTESIAN_POINT('Ctrl Pts',(29.5208561416033,22.9365131374907,42.9612625008648));
#65889=CARTESIAN_POINT('Ctrl Pts',(29.6106466262219,22.9575302119213,42.9552287150087));
#65890=CARTESIAN_POINT('Ctrl Pts',(29.6766342778022,22.9695059083136,42.9507407771113));
#65891=CARTESIAN_POINT('Ctrl Pts',(29.8834078112605,22.9963601773623,42.9365274387593));
#65892=CARTESIAN_POINT('Ctrl Pts',(30.0252591816151,22.9996010059475,42.926532055402));
#65893=CARTESIAN_POINT('Ctrl Pts',(30.2222874831598,22.9831235738724,42.9129008700715));
#65894=CARTESIAN_POINT('Ctrl Pts',(30.2781167819911,22.9760675666802,42.9090725541263));
#65895=CARTESIAN_POINT('Ctrl Pts',(30.3493263429887,22.9639892623982,42.9042913762256));
#65896=CARTESIAN_POINT('Ctrl Pts',(30.3650429114489,22.9611288658656,42.9032426112948));
#65897=CARTESIAN_POINT('Ctrl Pts',(30.3907365660481,22.9561330577973,42.9015405719646));
#65898=CARTESIAN_POINT('Ctrl Pts',(30.400734389264,22.9541094052906,42.9008813991574));
#65899=CARTESIAN_POINT('Ctrl Pts',(30.4209794052883,22.9498497097683,42.8995535462777));
#65900=CARTESIAN_POINT('Ctrl Pts',(30.4312252942863,22.9476093828033,42.8988851131931));
#65901=CARTESIAN_POINT('Ctrl Pts',(30.4583512260463,22.9414535689799,42.8971238137276));
#65902=CARTESIAN_POINT('Ctrl Pts',(30.4751991289391,22.9373986793428,42.8960385034249));
#65903=CARTESIAN_POINT('Ctrl Pts',(30.5629886020416,22.9150556904737,42.8904182960012));
#65904=CARTESIAN_POINT('Ctrl Pts',(30.6329429564656,22.8930874051847,42.8860590350621));
#65905=CARTESIAN_POINT('Ctrl Pts',(30.8174735051296,22.8237607399634,42.8745025201636));
#65906=CARTESIAN_POINT('Ctrl Pts',(30.9291007369645,22.769502311156,42.86743442197));
#65907=CARTESIAN_POINT('Ctrl Pts',(31.0917911560647,22.6707592904019,42.856175996487));
#65908=CARTESIAN_POINT('Ctrl Pts',(31.1468420845006,22.6334615060652,42.8521810270802));
#65909=CARTESIAN_POINT('Ctrl Pts',(31.2195295868456,22.5787265069676,42.8465720621092));
#65910=CARTESIAN_POINT('Ctrl Pts',(31.2388587252173,22.5636044171007,42.8450462444082));
#65911=CARTESIAN_POINT('Ctrl Pts',(31.2715324401546,22.5370560184561,42.8424042989606));
#65912=CARTESIAN_POINT('Ctrl Pts',(31.2850143521467,22.5258027503827,42.8412951787559));
#65913=CARTESIAN_POINT('Ctrl Pts',(31.3106187295469,22.5038508763105,42.8391509224679));
#65914=CARTESIAN_POINT('Ctrl Pts',(31.3227631881306,22.4931799741157,42.838116984273));
#65915=CARTESIAN_POINT('Ctrl Pts',(31.3546353440804,22.4644810643633,42.8353574067444));
#65916=CARTESIAN_POINT('Ctrl Pts',(31.3741321788921,22.4462027324033,42.833621288892));
#65917=CARTESIAN_POINT('Ctrl Pts',(31.4503245480043,22.3718401991719,42.8266385167874));
#65918=CARTESIAN_POINT('Ctrl Pts',(31.5039957008964,22.3127760842138,42.8212641658102));
#65919=CARTESIAN_POINT('Ctrl Pts',(31.6341491941339,22.1510570282978,42.8070089010727));
#65920=CARTESIAN_POINT('Ctrl Pts',(31.7045473017537,22.0439788512633,42.7979868552629));
#65921=CARTESIAN_POINT('Ctrl Pts',(31.7894396706236,21.8830942431126,42.7854603258962));
#65922=CARTESIAN_POINT('Ctrl Pts',(31.8127155072493,21.8342741149423,42.7817856040501));
#65923=CARTESIAN_POINT('Ctrl Pts',(31.8401922657388,21.7700450556076,42.7771629158989));
#65924=CARTESIAN_POINT('Ctrl Pts',(31.8462312440186,21.7554516489772,42.7761263825407));
#65925=CARTESIAN_POINT('Ctrl Pts',(31.8558711027405,21.7313503404955,42.7744388623434));
#65926=CARTESIAN_POINT('Ctrl Pts',(31.8595736652151,21.7218841108678,42.7737821642907));
#65927=CARTESIAN_POINT('Ctrl Pts',(31.8669665885131,21.7025484516337,42.77245378526));
#65928=CARTESIAN_POINT('Ctrl Pts',(31.8706514043428,21.692677345632,42.7717824195852));
#65929=CARTESIAN_POINT('Ctrl Pts',(31.8802665718077,21.6662832262171,42.7700041426011));
#65930=CARTESIAN_POINT('Ctrl Pts',(31.8860574616923,21.6497099502773,42.7689050487369));
#65931=CARTESIAN_POINT('Ctrl Pts',(31.9167087922599,21.558121808924,42.7629158811781));
#65932=CARTESIAN_POINT('Ctrl Pts',(31.9373159251227,21.481749177919,42.7582308773455));
#65933=CARTESIAN_POINT('Ctrl Pts',(31.9853651822983,21.249631006113,42.7443691853903));
#65934=CARTESIAN_POINT('Ctrl Pts',(31.9988962142559,21.0916675219693,42.7353857118885));
#65935=CARTESIAN_POINT('Ctrl Pts',(31.9923824142054,20.8956111834969,42.7235083064355));
#65936=CARTESIAN_POINT('Ctrl Pts',(31.9900200671759,20.8575059524926,42.7211687020365));
#65937=CARTESIAN_POINT('Ctrl Pts',(31.9847349135814,20.7993400669061,42.717537201912));
#65938=CARTESIAN_POINT('Ctrl Pts',(31.9825971572836,20.779216055518,42.7162697488233));
#65939=CARTESIAN_POINT('Ctrl Pts',(31.9780851562366,20.7421238305339,42.7139115173781));
#65940=CARTESIAN_POINT('Ctrl Pts',(31.9757977418035,20.7251468435659,42.7128235801213));
#65941=CARTESIAN_POINT('Ctrl Pts',(31.9702335003833,20.687518527539,42.7103922134088));
#65942=CARTESIAN_POINT('Ctrl Pts',(31.9668500786955,20.6668852609935,42.7090455168679));
#65943=CARTESIAN_POINT('Ctrl Pts',(31.9559753712531,20.6065256703112,42.7050647689384));
#65944=CARTESIAN_POINT('Ctrl Pts',(31.9476004514592,20.5669713713321,42.7024032861881));
#65945=CARTESIAN_POINT('Ctrl Pts',(31.9029670289558,20.3838227163736,42.6898265640264));
#65946=CARTESIAN_POINT('Ctrl Pts',(31.8519944708731,20.2443133884576,42.6794647148638));
#65947=CARTESIAN_POINT('Ctrl Pts',(31.7604616976154,20.060260984309,42.6651552178724));
#65948=CARTESIAN_POINT('Ctrl Pts',(31.7326372664186,20.0098971597511,42.661173137791));
#65949=CARTESIAN_POINT('Ctrl Pts',(31.6843804189731,19.9308305998077,42.6548813651991));
#65950=CARTESIAN_POINT('Ctrl Pts',(31.6652973239925,19.9013436554057,42.6525255883577));
#65951=CARTESIAN_POINT('Ctrl Pts',(31.6377114738966,19.8610900754056,42.6493123636865));
#65952=CARTESIAN_POINT('Ctrl Pts',(31.6298624274414,19.8498855791709,42.6484182833558));
#65953=CARTESIAN_POINT('Ctrl Pts',(31.6161947907119,19.8307960163526,42.6468967694563));
#65954=CARTESIAN_POINT('Ctrl Pts',(31.6104323687032,19.8228716472115,42.6462657359877));
#65955=CARTESIAN_POINT('Ctrl Pts',(31.5978651039826,19.8058544328849,42.6449121583486));
#65956=CARTESIAN_POINT('Ctrl Pts',(31.5910406992015,19.796776814382,42.6441909489661));
#65957=CARTESIAN_POINT('Ctrl Pts',(31.5714518561759,19.7711784258222,42.6421580080922));
#65958=CARTESIAN_POINT('Ctrl Pts',(31.5585046905944,19.7547985677908,42.640858165872));
#65959=CARTESIAN_POINT('Ctrl Pts',(31.4531020366705,19.625670549647,42.6305917799314));
#65960=CARTESIAN_POINT('Ctrl Pts',(31.348783583765,19.5231517071789,42.6222972106831));
#65961=CARTESIAN_POINT('Ctrl Pts',(31.1522192550037,19.3683413067374,42.607733877715));
#65962=CARTESIAN_POINT('Ctrl Pts',(31.065299046134,19.3103095943194,42.6015870998899));
#65963=CARTESIAN_POINT('Ctrl Pts',(30.950210931497,19.2458947260354,42.5934954889346));
#65964=CARTESIAN_POINT('Ctrl Pts',(30.9259022214463,19.2329428170392,42.5917896427069));
#65965=CARTESIAN_POINT('Ctrl Pts',(30.8851705828402,19.2123118602091,42.5889321914148));
#65966=CARTESIAN_POINT('Ctrl Pts',(30.868896778849,19.2043457463301,42.5877907713088));
#65967=CARTESIAN_POINT('Ctrl Pts',(30.8366861879101,19.189118885503,42.5855308771848));
#65968=CARTESIAN_POINT('Ctrl Pts',(30.8207578137248,19.181844130218,42.5844130170794));
#65969=CARTESIAN_POINT('Ctrl Pts',(30.7816198418871,19.1645882685318,42.5816645212597));
#65970=CARTESIAN_POINT('Ctrl Pts',(30.7583129424412,19.1548368133841,42.5800262465445));
#65971=CARTESIAN_POINT('Ctrl Pts',(30.6717441441524,19.1205341771257,42.5739328612329));
#65972=CARTESIAN_POINT('Ctrl Pts',(30.607432564907,19.0987751506924,42.5693878513425));
#65973=CARTESIAN_POINT('Ctrl Pts',(30.4068035182065,19.0421143495591,42.5551699072351));
#65974=CARTESIAN_POINT('Ctrl Pts',(30.2678041893015,19.0183136036796,42.5452358089471));
#65975=CARTESIAN_POINT('Ctrl Pts',(30.0714759004091,19.0057413075797,42.5316735555465));
#65976=CARTESIAN_POINT('Ctrl Pts',(30.0153432144867,19.0045195430497,42.5278542043979));
#65977=CARTESIAN_POINT('Ctrl Pts',(29.9432685360821,19.0059929913088,42.5230821992983));
#65978=CARTESIAN_POINT('Ctrl Pts',(29.9273118104667,19.0065108789484,42.5220340858442));
#65979=CARTESIAN_POINT('Ctrl Pts',(29.9011739047343,19.0076734763786,42.5203327910777));
#65980=CARTESIAN_POINT('Ctrl Pts',(29.8909886550382,19.0082048008787,42.519673722085));
#65981=CARTESIAN_POINT('Ctrl Pts',(29.8703360291569,19.0094410676705,42.5183458022797));
#65982=CARTESIAN_POINT('Ctrl Pts',(29.8598693169807,19.0101505051507,42.5176772020547));
#65983=CARTESIAN_POINT('Ctrl Pts',(29.832117055019,19.0122516296517,42.515914913564));
#65984=CARTESIAN_POINT('Ctrl Pts',(29.8148428197703,19.013786231623,42.514828796724));
#65985=CARTESIAN_POINT('Ctrl Pts',(29.7244158106905,19.0230095849694,42.5091896341956));
#65986=CARTESIAN_POINT('Ctrl Pts',(29.6517023006379,19.0345156504993,42.5048136743417));
#65987=CARTESIAN_POINT('Ctrl Pts',(29.4589537320812,19.0760523840173,42.4932558560802));
#65988=CARTESIAN_POINT('Ctrl Pts',(29.3408069734412,19.1132646027896,42.4862010601942));
#65989=CARTESIAN_POINT('Ctrl Pts',(29.1656538300955,19.1869079081937,42.4749603253847));
#65990=CARTESIAN_POINT('Ctrl Pts',(29.105772867818,19.2156813548934,42.4709688687707));
#65991=CARTESIAN_POINT('Ctrl Pts',(29.0258867155234,19.2591000209484,42.4653640466749));
#65992=CARTESIAN_POINT('Ctrl Pts',(29.0045504669284,19.2712115304458,42.4638386821372));
#65993=CARTESIAN_POINT('Ctrl Pts',(28.9683356797835,19.2926615387827,42.4611972968128));
#65994=CARTESIAN_POINT('Ctrl Pts',(28.9533468636485,19.3018088826655,42.460088276503));
#65995=CARTESIAN_POINT('Ctrl Pts',(28.9247932172954,19.3197561735811,42.4579440574575));
#65996=CARTESIAN_POINT('Ctrl Pts',(28.9112107428233,19.3285255401895,42.456910054544));
#65997=CARTESIAN_POINT('Ctrl Pts',(28.8754577595284,19.3522297362244,42.4541499307802));
#65998=CARTESIAN_POINT('Ctrl Pts',(28.8534789418347,19.3674463436564,42.4524133227249));
#65999=CARTESIAN_POINT('Ctrl Pts',(28.7649288137391,19.4314224938838,42.4452483329025));
#66000=CARTESIAN_POINT('Ctrl Pts',(28.7011153259588,19.4838430678112,42.4396819082959));
#66001=CARTESIAN_POINT('Ctrl Pts',(28.5488401263398,19.6256172376125,42.4253779806786));
#66002=CARTESIAN_POINT('Ctrl Pts',(28.4652322333037,19.719656794287,42.4165202552595));
#66003=CARTESIAN_POINT('Ctrl Pts',(28.3593068162179,19.8642042347369,42.4041826393878));
#66004=CARTESIAN_POINT('Ctrl Pts',(28.3293495268052,19.9087465220196,42.4005363403406));
#66005=CARTESIAN_POINT('Ctrl Pts',(28.2929634341359,19.9678653145508,42.3959431402898));
#66006=CARTESIAN_POINT('Ctrl Pts',(28.2848633239259,19.9813822767893,42.3949089930114));
#66007=CARTESIAN_POINT('Ctrl Pts',(28.2718067787299,20.0037676429474,42.3932243320278));
#66008=CARTESIAN_POINT('Ctrl Pts',(28.2667565152647,20.0125802526857,42.3925681427503));
#66009=CARTESIAN_POINT('Ctrl Pts',(28.2566004007,20.0306205070616,42.39123970046));
#66010=CARTESIAN_POINT('Ctrl Pts',(28.2515000166501,20.0398507487754,42.3905677761661));
#66011=CARTESIAN_POINT('Ctrl Pts',(28.2380841581283,20.0645910968275,42.3887862430811));
#66012=CARTESIAN_POINT('Ctrl Pts',(28.2299001268923,20.0801718969074,42.3876845024781));
#66013=CARTESIAN_POINT('Ctrl Pts',(28.1853895700378,20.1677060834377,42.3815954340543));
#66014=CARTESIAN_POINT('Ctrl Pts',(28.1532401306453,20.241709148683,42.3768216717605));
#66015=CARTESIAN_POINT('Ctrl Pts',(28.0714331083094,20.4663627700938,42.3628489353929));
#66016=CARTESIAN_POINT('Ctrl Pts',(28.0351501701656,20.6211831355658,42.3538334567775));
#66017=CARTESIAN_POINT('Ctrl Pts',(28.0134736397754,20.8153329423209,42.3419885792054));
#66018=CARTESIAN_POINT('Ctrl Pts',(28.0103980253634,20.8521060429817,42.3397247170649));
#66019=CARTESIAN_POINT('Ctrl Pts',(28.0072309898124,20.9089017966257,42.3361856363779));
#66020=CARTESIAN_POINT('Ctrl Pts',(28.0064181275642,20.9288769909065,42.3349328828233));
#66021=CARTESIAN_POINT('Ctrl Pts',(28.0054661545743,20.9659974713025,42.3325883072163));
#66022=CARTESIAN_POINT('Ctrl Pts',(28.0052476073107,20.9831389711664,42.331499083713));
#66023=CARTESIAN_POINT('Ctrl Pts',(28.005253003867,21.0214845179922,42.3290469129572));
#66024=CARTESIAN_POINT('Ctrl Pts',(28.0055940749041,21.0426861968483,42.3276804180085));
#66025=CARTESIAN_POINT('Ctrl Pts',(28.0076641472113,21.1072964704847,42.3234819558119));
#66026=CARTESIAN_POINT('Ctrl Pts',(28.010473113702,21.1506551381818,42.3206170513258));
#66027=CARTESIAN_POINT('Ctrl Pts',(28.0205526017937,21.2538651082452,42.3136814387831));
#66028=CARTESIAN_POINT('Ctrl Pts',(28.0291249580706,21.3135442893453,42.3095764977217));
#66029=CARTESIAN_POINT('Ctrl Pts',(28.054235753666,21.4455599737151,42.3003112452953));
#66030=CARTESIAN_POINT('Ctrl Pts',(28.072134807481,21.5175493049864,42.2951315120848));
#66031=CARTESIAN_POINT('Ctrl Pts',(28.1194852205853,21.6709385020492,42.2839412389321));
#66032=CARTESIAN_POINT('Ctrl Pts',(28.1503132283133,21.7517683944049,42.2779460280712));
#66033=CARTESIAN_POINT('Ctrl Pts',(28.1953214898201,21.8500787316112,42.2707137719031));
#66034=CARTESIAN_POINT('Ctrl Pts',(28.2046755049513,21.8696599470592,42.2692766013212));
#66035=CARTESIAN_POINT('Ctrl Pts',(28.2194867133324,21.8994069941687,42.2671027127666));
#66036=CARTESIAN_POINT('Ctrl Pts',(28.2247153626845,21.9096839986581,42.2663534286036));
#66037=CARTESIAN_POINT('Ctrl Pts',(28.2340824457752,21.9277067737325,42.2650432659876));
#66038=CARTESIAN_POINT('Ctrl Pts',(28.2381831741793,21.9354710807231,42.2644801822454));
#66039=CARTESIAN_POINT('Ctrl Pts',(28.2483629493168,21.9544410444534,42.2631074549902));
#66040=CARTESIAN_POINT('Ctrl Pts',(28.2544983358024,21.9656158788313,42.2623013267773));
#66041=CARTESIAN_POINT('Ctrl Pts',(28.2749674002502,22.0020650085302,42.25967770656));
#66042=CARTESIAN_POINT('Ctrl Pts',(28.2897468288469,22.0270861895767,42.2578858049856));
#66043=CARTESIAN_POINT('Ctrl Pts',(28.3279251125272,22.0886102370481,42.2534799003766));
#66044=CARTESIAN_POINT('Ctrl Pts',(28.3519776719149,22.1246908536007,42.2508961110191));
#66045=CARTESIAN_POINT('Ctrl Pts',(28.4358582534647,22.2420417026369,42.2423947371187));
#66046=CARTESIAN_POINT('Ctrl Pts',(28.5006723639967,22.3195547728393,42.2366100866802));
#66047=CARTESIAN_POINT('Ctrl Pts',(28.6365159271607,22.4590185863475,42.2252465133458));
#66048=CARTESIAN_POINT('Ctrl Pts',(28.7066072725647,22.521498094724,42.2196959689649));
#66049=CARTESIAN_POINT('Ctrl Pts',(28.8025535613142,22.5955886164734,42.2122576568857));
#66050=CARTESIAN_POINT('Ctrl Pts',(28.8246220369402,22.6119142460568,42.2105573881615));
#66051=CARTESIAN_POINT('Ctrl Pts',(28.8617900261346,22.6382408986469,42.2077066846107));
#66052=CARTESIAN_POINT('Ctrl Pts',(28.8767018211409,22.6485012445305,42.206566331019));
#66053=CARTESIAN_POINT('Ctrl Pts',(28.9064919807364,22.6684070549241,42.2042935859165));
#66054=CARTESIAN_POINT('Ctrl Pts',(28.9213634255931,22.6780598904598,42.2031616131502));
#66055=CARTESIAN_POINT('Ctrl Pts',(28.9579321128833,22.701109121116,42.2003833646784));
#66056=CARTESIAN_POINT('Ctrl Pts',(28.97976088241,22.7142898722787,42.198729356614));
#66057=CARTESIAN_POINT('Ctrl Pts',(29.0106880438982,22.7321645307402,42.1963909704906));
#66058=CARTESIAN_POINT('Ctrl Pts',(29.0195788375064,22.7372122513924,42.1957193191245));
#66059=CARTESIAN_POINT('Ctrl Pts',(29.0285070576893,22.7421908694344,42.1950453911705));
#66060=CARTESIAN_POINT('',(28.0052505793236,21.0015202668116,42.170454911886));
#66061=CARTESIAN_POINT('Ctrl Pts',(29.0271745210922,22.7445458878821,42.0352855536299));
#66062=CARTESIAN_POINT('Ctrl Pts',(28.5012799340924,22.4467683092264,42.0740046256861));
#66063=CARTESIAN_POINT('Ctrl Pts',(28.0506268393321,21.8039662264705,42.1190610682745));
#66064=CARTESIAN_POINT('Ctrl Pts',(28.0027407180406,21.1005716660941,42.164117510863));
#66065=CARTESIAN_POINT('Ctrl Pts',(28.0035787417433,21.0015220175284,42.1704548813952));
#66066=CARTESIAN_POINT('Ctrl Pts',(28.0052505793236,21.0015202668116,42.170454911886));
#66067=CARTESIAN_POINT('Ctrl Pts',(28.0051970620983,20.9313000572674,42.1749515213504));
#66068=CARTESIAN_POINT('Ctrl Pts',(28.0088561147499,20.860941689876,42.1794481308147));
#66069=CARTESIAN_POINT('Ctrl Pts',(28.0162421748609,20.7908769412538,42.183944740279));
#66070=CARTESIAN_POINT('Ctrl Pts',(28.0234347506374,20.722647600285,42.1883235571074));
#66071=CARTESIAN_POINT('Ctrl Pts',(28.0341614141149,20.6546972225173,42.1927023739358));
#66072=CARTESIAN_POINT('Ctrl Pts',(28.0483828520568,20.5874250730424,42.1970811907641));
#66073=CARTESIAN_POINT('Ctrl Pts',(28.0625948263002,20.520197690021,42.2014570936958));
#66074=CARTESIAN_POINT('Ctrl Pts',(28.080296861765,20.453648133581,42.2058329966274));
#66075=CARTESIAN_POINT('Ctrl Pts',(28.1013981649582,20.3881678052964,42.210208899559));
#66076=CARTESIAN_POINT('Ctrl Pts',(28.1224930810841,20.3227072969848,42.2145834779664));
#66077=CARTESIAN_POINT('Ctrl Pts',(28.1469850689486,20.258315855221,42.2189580563738));
#66078=CARTESIAN_POINT('Ctrl Pts',(28.1747333854154,20.1953700551291,42.2233326347813));
#66079=CARTESIAN_POINT('Ctrl Pts',(28.2038274734137,20.129371433224,42.2279193768019));
#66080=CARTESIAN_POINT('Ctrl Pts',(28.2365015891748,20.0649628169976,42.2325061188226));
#66081=CARTESIAN_POINT('Ctrl Pts',(28.2725375752561,20.0025526913175,42.2370928608433));
#66082=CARTESIAN_POINT('Ctrl Pts',(28.306945100685,19.9429628695902,42.2414723286995));
#66083=CARTESIAN_POINT('Ctrl Pts',(28.3444168594674,19.8851952172695,42.2458517965558));
#66084=CARTESIAN_POINT('Ctrl Pts',(28.3847181329207,19.8295761227722,42.250231264412));
#66085=CARTESIAN_POINT('Ctrl Pts',(28.425045663941,19.7739207906584,42.2546135856315));
#66086=CARTESIAN_POINT('Ctrl Pts',(28.468206055754,19.720417189919,42.2589959068509));
#66087=CARTESIAN_POINT('Ctrl Pts',(28.5139250492059,19.6693577478817,42.2633782280704));
#66088=CARTESIAN_POINT('Ctrl Pts',(28.559717170636,19.6182166357664,42.2677675588556));
#66089=CARTESIAN_POINT('Ctrl Pts',(28.6080756938063,19.5695278285746,42.2721568896408));
#66090=CARTESIAN_POINT('Ctrl Pts',(28.6586913580752,19.52354522941,42.276546220426));
#66091=CARTESIAN_POINT('Ctrl Pts',(28.6657152795995,19.5171642370299,42.2771553266271));
#66092=CARTESIAN_POINT('Ctrl Pts',(28.6727826196441,19.5108352911583,42.2777644328282));
#66093=CARTESIAN_POINT('Ctrl Pts',(28.6798925075052,19.5045590045879,42.2783735390293));
#66094=CARTESIAN_POINT('Ctrl Pts',(28.7318946680379,19.4586538555678,42.2828285795406));
#66095=CARTESIAN_POINT('Ctrl Pts',(28.7863965406452,19.4153739995667,42.2872836200518));
#66096=CARTESIAN_POINT('Ctrl Pts',(28.8431022646294,19.3750030177276,42.2917386605631));
#66097=CARTESIAN_POINT('Ctrl Pts',(28.8997230566527,19.3346925022121,42.2961870284618));
#66098=CARTESIAN_POINT('Ctrl Pts',(28.9585407531584,19.297282494972,42.3006353963605));
#66099=CARTESIAN_POINT('Ctrl Pts',(29.0192252459494,19.2630174311994,42.3050837642592));
#66100=CARTESIAN_POINT('Ctrl Pts',(29.0798385496435,19.22879256384,42.3095269137688));
#66101=CARTESIAN_POINT('Ctrl Pts',(29.1423138760186,19.1977055517645,42.3139700632784));
#66102=CARTESIAN_POINT('Ctrl Pts',(29.2062923547168,19.1699574495879,42.318413212788));
#66103=CARTESIAN_POINT('Ctrl Pts',(29.2702307173509,19.142226746147,42.3228535763347));
#66104=CARTESIAN_POINT('Ctrl Pts',(29.3356699146653,19.1178309935652,42.3272939398814));
#66105=CARTESIAN_POINT('Ctrl Pts',(29.4022280692487,19.096924520334,42.3317343034281));
#66106=CARTESIAN_POINT('Ctrl Pts',(29.4687670770573,19.076024061265,42.336173389616));
#66107=CARTESIAN_POINT('Ctrl Pts',(29.5364239365347,19.058611035403,42.3406124758039));
#66108=CARTESIAN_POINT('Ctrl Pts',(29.6048001430737,19.044790385768,42.3450515619919));
#66109=CARTESIAN_POINT('Ctrl Pts',(29.6731798828965,19.0309690219623,42.3494908775659));
#66110=CARTESIAN_POINT('Ctrl Pts',(29.7422785635095,19.0207404975009,42.35393019314));
#66111=CARTESIAN_POINT('Ctrl Pts',(29.8116877359986,19.0141586030786,42.358369508714));
#66112=CARTESIAN_POINT('Ctrl Pts',(29.881170258328,19.0075697530785,42.3628135156433));
#66113=CARTESIAN_POINT('Ctrl Pts',(29.9509634393632,19.0046352709168,42.3672575225727));
#66114=CARTESIAN_POINT('Ctrl Pts',(30.02065492408,19.0053569400489,42.371701529502));
#66115=CARTESIAN_POINT('Ctrl Pts',(30.0903872283532,19.0060790318755,42.3761481393661));
#66116=CARTESIAN_POINT('Ctrl Pts',(30.1600172292947,19.0104615066311,42.3805947492303));
#66117=CARTESIAN_POINT('Ctrl Pts',(30.2291365865459,19.0184541420381,42.3850413590944));
#66118=CARTESIAN_POINT('Ctrl Pts',(30.2983756802342,19.0264606232,42.3894956718835));
#66119=CARTESIAN_POINT('Ctrl Pts',(30.3671018821523,19.0380896669233,42.3939499846726));
#66120=CARTESIAN_POINT('Ctrl Pts',(30.4349167450651,19.053239874211,42.3984042974617));
#66121=CARTESIAN_POINT('Ctrl Pts',(30.4699332417016,19.0610627490167,42.4007043010611));
#66122=CARTESIAN_POINT('Ctrl Pts',(30.504706996052,19.069823623548,42.4030043046606));
#66123=CARTESIAN_POINT('Ctrl Pts',(30.5391850306961,19.0795034326578,42.4053043082601));
#66124=CARTESIAN_POINT('Ctrl Pts',(30.6059679644354,19.0982529367134,42.4097593472311));
#66125=CARTESIAN_POINT('Ctrl Pts',(30.6719032715288,19.1205269599281,42.4142143862021));
#66126=CARTESIAN_POINT('Ctrl Pts',(30.7365921789036,19.1462309948437,42.4186694251731));
#66127=CARTESIAN_POINT('Ctrl Pts',(30.8011841973056,19.1718965310795,42.4231177915295));
#66128=CARTESIAN_POINT('Ctrl Pts',(30.864533070189,19.2009817031991,42.4275661578858));
#66129=CARTESIAN_POINT('Ctrl Pts',(30.9262543062639,19.2333419904725,42.4320145242422));
#66130=CARTESIAN_POINT('Ctrl Pts',(30.9879031370722,19.2656643158487,42.4364576722139));
#66131=CARTESIAN_POINT('Ctrl Pts',(31.0479276921306,19.3012538993587,42.4409008201857));
#66132=CARTESIAN_POINT('Ctrl Pts',(31.1059642961495,19.3399185146076,42.4453439681574));
#66133=CARTESIAN_POINT('Ctrl Pts',(31.1639645098387,19.3785588862242,42.4497843301698));
#66134=CARTESIAN_POINT('Ctrl Pts',(31.2199788390351,19.4202701938765,42.4542246921821));
#66135=CARTESIAN_POINT('Ctrl Pts',(31.2736703584782,19.4648155223447,42.4586650541945));
#66136=CARTESIAN_POINT('Ctrl Pts',(31.3273464325552,19.5093480365189,42.463104138854));
#66137=CARTESIAN_POINT('Ctrl Pts',(31.3787006470321,19.5567126407671,42.4675432235135));
#66138=CARTESIAN_POINT('Ctrl Pts',(31.4274285236126,19.6066316450855,42.471982308173));
#66139=CARTESIAN_POINT('Ctrl Pts',(31.4761589182559,19.6565532290195,42.4764216222267));
#66140=CARTESIAN_POINT('Ctrl Pts',(31.5222623655039,19.7090291232722,42.4808609362804));
#66141=CARTESIAN_POINT('Ctrl Pts',(31.5654719459578,19.7637455161178,42.4853002503341));
#66142=CARTESIAN_POINT('Ctrl Pts',(31.6087271894286,19.8185197321484,42.4897442557658));
#66143=CARTESIAN_POINT('Ctrl Pts',(31.6490821584572,19.8755387877348,42.4941882611975));
#66144=CARTESIAN_POINT('Ctrl Pts',(31.6863114886263,19.9344573561669,42.4986322666291));
#66145=CARTESIAN_POINT('Ctrl Pts',(31.7235626247804,19.9934104344173,42.5030788750062));
#66146=CARTESIAN_POINT('Ctrl Pts',(31.757684238794,20.0542648131004,42.5075254833834));
#66147=CARTESIAN_POINT('Ctrl Pts',(31.7884968201451,20.1166503032032,42.5119720917605));
#66148=CARTESIAN_POINT('Ctrl Pts',(31.819362778807,20.1791438650597,42.5164264030949));
#66149=CARTESIAN_POINT('Ctrl Pts',(31.8469080691786,20.2431733833983,42.5208807144293));
#66150=CARTESIAN_POINT('Ctrl Pts',(31.8710015298326,20.3083491936938,42.5253350257637));
#66151=CARTESIAN_POINT('Ctrl Pts',(31.8834423699025,20.342003214756,42.5276350430061));
#66152=CARTESIAN_POINT('Ctrl Pts',(31.8949636840046,20.3759626233232,42.5299350602484));
#66153=CARTESIAN_POINT('Ctrl Pts',(31.905552721466,20.4101725776012,42.5322350774908));
#66154=CARTESIAN_POINT('Ctrl Pts',(31.9260632604963,20.4764358810417,42.5366901182433));
#66155=CARTESIAN_POINT('Ctrl Pts',(31.9431537360617,20.5439008045752,42.5411451589958));
#66156=CARTESIAN_POINT('Ctrl Pts',(31.9566870221979,20.6121811509711,42.5456001997483));
#66157=CARTESIAN_POINT('Ctrl Pts',(31.9702000385908,20.6803592291454,42.5500485678766));
#66158=CARTESIAN_POINT('Ctrl Pts',(31.9801663458684,20.7493498300388,42.5544969360049));
#66159=CARTESIAN_POINT('Ctrl Pts',(31.9864985726956,20.8187515981357,42.5589453041332));
#66160=CARTESIAN_POINT('Ctrl Pts',(31.9928233711497,20.8880719506041,42.5633884538542));
#66161=CARTESIAN_POINT('Ctrl Pts',(31.9955225122191,20.9578020273226,42.5678316035753));
#66162=CARTESIAN_POINT('Ctrl Pts',(31.9945599886851,21.0275320547108,42.5722747532963));
#66163=CARTESIAN_POINT('Ctrl Pts',(31.9935980686792,21.0972183594982,42.5767151170431));
#66164=CARTESIAN_POINT('Ctrl Pts',(31.9889790455858,21.166904126889,42.5811554807899));
#66165=CARTESIAN_POINT('Ctrl Pts',(31.9807189643372,21.2361777864553,42.5855958445367));
#66166=CARTESIAN_POINT('Ctrl Pts',(31.9724612592863,21.3054315178991,42.5900349309133));
#66167=CARTESIAN_POINT('Ctrl Pts',(31.9605646333799,21.374272891263,42.5944740172898));
#66168=CARTESIAN_POINT('Ctrl Pts',(31.9450969895518,21.4422954484692,42.5989131036663));
#66169=CARTESIAN_POINT('Ctrl Pts',(31.9296285464868,21.5103215205051,42.6033524194172));
#66170=CARTESIAN_POINT('Ctrl Pts',(31.910588830009,21.5775282158087,42.6077917351682));
#66171=CARTESIAN_POINT('Ctrl Pts',(31.888096468681,21.6435210077802,42.6122310509191));
#66172=CARTESIAN_POINT('Ctrl Pts',(31.8655803380961,21.7095835389667,42.6166750580065));
#66173=CARTESIAN_POINT('Ctrl Pts',(31.8396044384882,21.7744291424106,42.621119065094));
#66174=CARTESIAN_POINT('Ctrl Pts',(31.8103364247849,21.8376810798848,42.6255630721814));
#66175=CARTESIAN_POINT('Ctrl Pts',(31.7810512683487,21.900970065007,42.6300096821932));
#66176=CARTESIAN_POINT('Ctrl Pts',(31.7484703884075,21.9626630934782,42.634456292205));
#66177=CARTESIAN_POINT('Ctrl Pts',(31.7128072132218,22.0224084373846,42.6389029022169));
#66178=CARTESIAN_POINT('Ctrl Pts',(31.6770822583582,22.0822572787527,42.643357215136));
#66179=CARTESIAN_POINT('Ctrl Pts',(31.6382646224775,22.1401512943898,42.6478115280552));
#66180=CARTESIAN_POINT('Ctrl Pts',(31.5966103379953,22.1957687866417,42.6522658409744));
#66181=CARTESIAN_POINT('Ctrl Pts',(31.5751019851143,22.2244870965245,42.6545658428901));
#66182=CARTESIAN_POINT('Ctrl Pts',(31.5528379692989,22.2525989922404,42.6568658448059));
#66183=CARTESIAN_POINT('Ctrl Pts',(31.5298574234629,22.2800639930783,42.6591658467216));
#66184=CARTESIAN_POINT('Ctrl Pts',(31.4853447119195,22.3332629757552,42.663620889807));
#66185=CARTESIAN_POINT('Ctrl Pts',(31.4379661326844,22.3842421481272,42.6680759328923));
#66186=CARTESIAN_POINT('Ctrl Pts',(31.3879715687025,22.4326766861276,42.6725309759777));
#66187=CARTESIAN_POINT('Ctrl Pts',(31.3380518846869,22.4810386807096,42.6769793464681));
#66188=CARTESIAN_POINT('Ctrl Pts',(31.2855243411721,22.5268632677637,42.6814277169585));
#66189=CARTESIAN_POINT('Ctrl Pts',(31.2306785626744,22.5698591777206,42.6858760874489));
#66190=CARTESIAN_POINT('Ctrl Pts',(31.1758971236654,22.6128046492493,42.6903192395635));
#66191=CARTESIAN_POINT('Ctrl Pts',(31.1188032342992,22.652927733948,42.694762391678));
#66192=CARTESIAN_POINT('Ctrl Pts',(31.059721474027,22.6899757276322,42.6992055437926));
#66193=CARTESIAN_POINT('Ctrl Pts',(31.0006767593462,22.7270004913918,42.703645909951));
#66194=CARTESIAN_POINT('Ctrl Pts',(30.9396470600594,22.760953729899,42.7080862761093));
#66195=CARTESIAN_POINT('Ctrl Pts',(30.8769867235981,22.7916254768039,42.7125266422677));
#66196=CARTESIAN_POINT('Ctrl Pts',(30.8143444125776,22.8222884003957,42.71696573107));
#66197=CARTESIAN_POINT('Ctrl Pts',(30.750072834872,22.8496714914036,42.7214048198724));
#66198=CARTESIAN_POINT('Ctrl Pts',(30.6845501981602,22.8736111092483,42.7258439086747));
#66199=CARTESIAN_POINT('Ctrl Pts',(30.6190241756402,22.8975519641458,42.730283226862));
#66200=CARTESIAN_POINT('Ctrl Pts',(30.5522474261718,22.9180488269678,42.7347225450492));
#66201=CARTESIAN_POINT('Ctrl Pts',(30.4846156762315,22.9349871340272,42.7391618632364));
#66202=CARTESIAN_POINT('Ctrl Pts',(30.4169124551307,22.9519433409703,42.7436058727591));
#66203=CARTESIAN_POINT('Ctrl Pts',(30.3483529057536,22.9653333673321,42.7480498822817));
#66204=CARTESIAN_POINT('Ctrl Pts',(30.2793444322409,22.9750934789716,42.7524938918044));
#66205=CARTESIAN_POINT('Ctrl Pts',(30.2102955393635,22.9848593072643,42.7569405042544));
#66206=CARTESIAN_POINT('Ctrl Pts',(30.1407976865188,22.9909909460442,42.7613871167043));
#66207=CARTESIAN_POINT('Ctrl Pts',(30.0712621244812,22.9934766796014,42.7658337291543));
#66208=CARTESIAN_POINT('Ctrl Pts',(30.0016061056918,22.9959667192053,42.7702880444901));
#66209=CARTESIAN_POINT('Ctrl Pts',(29.9319127364352,22.9947982547328,42.7747423598258));
#66210=CARTESIAN_POINT('Ctrl Pts',(29.8625911778383,22.9900116527529,42.7791966751616));
#66211=CARTESIAN_POINT('Ctrl Pts',(29.8267970760302,22.9875400966878,42.7814966554252));
#66212=CARTESIAN_POINT('Ctrl Pts',(29.7911019902177,22.9841047330446,42.7837966356888));
#66213=CARTESIAN_POINT('Ctrl Pts',(29.7555611596385,22.9797164483387,42.7860966159524));
#66214=CARTESIAN_POINT('Ctrl Pts',(29.6867386212903,22.9712188165295,42.7905503801811));
#66215=CARTESIAN_POINT('Ctrl Pts',(29.618224219805,22.9591113772544,42.7950041444097));
#66216=CARTESIAN_POINT('Ctrl Pts',(29.5504260531578,22.9434275980393,42.7994579086384));
#66217=CARTESIAN_POINT('Ctrl Pts',(29.4827165833195,22.9277643370953,42.8039058462394));
#66218=CARTESIAN_POINT('Ctrl Pts',(29.4157219628788,22.9085341218107,42.8083537838404));
#66219=CARTESIAN_POINT('Ctrl Pts',(29.3498439234632,22.8858220060871,42.8128017214414));
#66220=CARTESIAN_POINT('Ctrl Pts',(29.2840380275424,22.8631347625579,42.8172447880753));
#66221=CARTESIAN_POINT('Ctrl Pts',(29.2193467454641,22.8369733467923,42.8216878547091));
#66222=CARTESIAN_POINT('Ctrl Pts',(29.1561584967993,22.8074731201254,42.826130921343));
#66223=CARTESIAN_POINT('Ctrl Pts',(29.1128626290442,22.7872599010618,42.8291752599577));
#66224=CARTESIAN_POINT('Ctrl Pts',(29.0702721587262,22.7654802242769,42.8322195985724));
#66225=CARTESIAN_POINT('Ctrl Pts',(29.0285070491141,22.7421908646526,42.8352639371872));
#66226=CARTESIAN_POINT('Origin',(30.,21.,34.5704548813952));
#66227=CARTESIAN_POINT('',(29.028507049119,22.7421908646553,43.7914234503344));
#66228=CARTESIAN_POINT('',(29.0285070491141,22.7421908646526,43.6351577566542));
#66229=CARTESIAN_POINT('',(29.0285070491141,22.7421908646526,34.5704548813952));
#66230=CARTESIAN_POINT('',(28.0052507762699,20.9981806434564,43.1283622955703));
#66231=CARTESIAN_POINT('Ctrl Pts',(29.0285070491189,22.7421908646553,43.7914234503344));
#66232=CARTESIAN_POINT('Ctrl Pts',(29.0340273848418,22.7452691538084,43.7910133702931));
#66233=CARTESIAN_POINT('Ctrl Pts',(29.0395624335134,22.7483212509773,43.7906048846172));
#66234=CARTESIAN_POINT('Ctrl Pts',(29.0537612093712,22.7560628579687,43.7895640570721));
#66235=CARTESIAN_POINT('Ctrl Pts',(29.0624452059104,22.7607145201542,43.7889342315292));
#66236=CARTESIAN_POINT('Ctrl Pts',(29.0821081154594,22.7710604162975,43.7875226205212));
#66237=CARTESIAN_POINT('Ctrl Pts',(29.0931064029216,22.7767173471975,43.7867430971221));
#66238=CARTESIAN_POINT('Ctrl Pts',(29.1338241456339,22.7971837588092,43.7838913701655));
#66239=CARTESIAN_POINT('Ctrl Pts',(29.1638610224724,22.8113536287464,43.7818542848881));
#66240=CARTESIAN_POINT('Ctrl Pts',(29.3160179525479,22.8785413743455,43.7717959176446));
#66241=CARTESIAN_POINT('Ctrl Pts',(29.4428836549757,22.9199939837615,43.7642179727341));
#66242=CARTESIAN_POINT('Ctrl Pts',(29.651716483836,22.9657643593753,43.7517609748197));
#66243=CARTESIAN_POINT('Ctrl Pts',(29.7314590819623,22.9782353345783,43.7470120566413));
#66244=CARTESIAN_POINT('Ctrl Pts',(29.8484626241887,22.9893278339625,43.7398884212674));
#66245=CARTESIAN_POINT('Ctrl Pts',(29.8852805793769,22.9917901492472,43.7376252659074));
#66246=CARTESIAN_POINT('Ctrl Pts',(29.9420485298013,22.9940075191057,43.73409144637));
#66247=CARTESIAN_POINT('Ctrl Pts',(29.9619630338499,22.9944867767253,43.7328434158399));
#66248=CARTESIAN_POINT('Ctrl Pts',(29.9989185556292,22.9948224736714,43.7305103597175));
#66249=CARTESIAN_POINT('Ctrl Pts',(30.0159571248355,22.9947589356791,43.729427960581));
#66250=CARTESIAN_POINT('Ctrl Pts',(30.0540024418684,22.9941295953132,43.7269951208517));
#66251=CARTESIAN_POINT('Ctrl Pts',(30.0750050120175,22.9934500992956,43.7256412157507));
#66252=CARTESIAN_POINT('Ctrl Pts',(30.1387078797509,22.9903810048485,43.7215000096877));
#66253=CARTESIAN_POINT('Ctrl Pts',(30.1813433050626,22.9869500656659,43.7186807099601));
#66254=CARTESIAN_POINT('Ctrl Pts',(30.2824167806174,22.9755364208924,43.7118807382848));
#66255=CARTESIAN_POINT('Ctrl Pts',(30.3406738782713,22.9663274651409,43.7078673643025));
#66256=CARTESIAN_POINT('Ctrl Pts',(30.4733184724307,22.9392879990787,43.6985373903687));
#66257=CARTESIAN_POINT('Ctrl Pts',(30.5472616256829,22.9197323239257,43.6931933372861));
#66258=CARTESIAN_POINT('Ctrl Pts',(30.7030379367426,22.8688008233273,43.6817588242744));
#66259=CARTESIAN_POINT('Ctrl Pts',(30.7843081090591,22.8361759992622,43.6756835567845));
#66260=CARTESIAN_POINT('Ctrl Pts',(30.8827700000907,22.7889150029293,43.6683753942372));
#66261=CARTESIAN_POINT('Ctrl Pts',(30.9022062758258,22.7791918639423,43.6669356887867));
#66262=CARTESIAN_POINT('Ctrl Pts',(30.9316720992258,22.7638442971712,43.6647618579755));
#66263=CARTESIAN_POINT('Ctrl Pts',(30.9418177474226,22.7584478813632,43.6640149904719));
#66264=CARTESIAN_POINT('Ctrl Pts',(30.9596077181047,22.748787348043,43.6627090189521));
#66265=CARTESIAN_POINT('Ctrl Pts',(30.967271096338,22.7445603431741,43.6621477128134));
#66266=CARTESIAN_POINT('Ctrl Pts',(30.9859657770612,22.7340875783383,43.6607811848628));
#66267=CARTESIAN_POINT('Ctrl Pts',(30.996965742365,22.7277868999449,43.6599794320797));
#66268=CARTESIAN_POINT('Ctrl Pts',(31.0326055503892,22.7069190404219,43.6573868350295));
#66269=CARTESIAN_POINT('Ctrl Pts',(31.0569931660467,22.6919256694566,43.6556207495053));
#66270=CARTESIAN_POINT('Ctrl Pts',(31.1167032477845,22.6534210215687,43.6512949769937));
#66271=CARTESIAN_POINT('Ctrl Pts',(31.1516151086528,22.6292974777441,43.6487640962835));
#66272=CARTESIAN_POINT('Ctrl Pts',(31.2686821724623,22.5427615951591,43.6401770480633));
#66273=CARTESIAN_POINT('Ctrl Pts',(31.3467523299261,22.4751024562536,43.6342661234127));
#66274=CARTESIAN_POINT('Ctrl Pts',(31.4848108660949,22.3353169195962,43.6227967418756));
#66275=CARTESIAN_POINT('Ctrl Pts',(31.5456345966708,22.2644150647385,43.6172730168325));
#66276=CARTESIAN_POINT('Ctrl Pts',(31.6176464029118,22.1674767146497,43.6098629474364));
#66277=CARTESIAN_POINT('Ctrl Pts',(31.6335654845117,22.1450962658228,43.6081617725193));
#66278=CARTESIAN_POINT('Ctrl Pts',(31.6592155570573,22.107411317016,43.6053085806497));
#66279=CARTESIAN_POINT('Ctrl Pts',(31.6692092342644,22.0922896077635,43.6041666298346));
#66280=CARTESIAN_POINT('Ctrl Pts',(31.6885883553778,22.0620793774653,43.6018898434879));
#66281=CARTESIAN_POINT('Ctrl Pts',(31.6979810113567,22.0469974638815,43.6007554162696));
#66282=CARTESIAN_POINT('Ctrl Pts',(31.7204028198375,22.0098990598059,43.597969305621));
#66283=CARTESIAN_POINT('Ctrl Pts',(31.7332120151956,21.9877540094034,43.5963098388384));
#66284=CARTESIAN_POINT('Ctrl Pts',(31.7824419432471,21.8987359405158,43.5896504570738));
#66285=CARTESIAN_POINT('Ctrl Pts',(31.8154427331912,21.8300547352672,43.5845340171021));
#66286=CARTESIAN_POINT('Ctrl Pts',(31.8764962800721,21.6818187765773,43.5735569566942));
#66287=CARTESIAN_POINT('Ctrl Pts',(31.90359579206,21.6020272022508,43.5676849094183));
#66288=CARTESIAN_POINT('Ctrl Pts',(31.951384729378,21.4253243950347,43.5549249165706));
#66289=CARTESIAN_POINT('Ctrl Pts',(31.9700678350653,21.32808486326,43.5480545005772));
#66290=CARTESIAN_POINT('Ctrl Pts',(31.9835296442544,21.2120363407314,43.5402927020212));
#66291=CARTESIAN_POINT('Ctrl Pts',(31.9853560760063,21.1941920816117,43.5391114915081));
#66292=CARTESIAN_POINT('Ctrl Pts',(31.9878819023384,21.1657294547423,43.5372494680481));
#66293=CARTESIAN_POINT('Ctrl Pts',(31.9887374213521,21.155126372079,43.5365606831562));
#66294=CARTESIAN_POINT('Ctrl Pts',(31.9902420389055,21.1344128517457,43.5352252778318));
#66295=CARTESIAN_POINT('Ctrl Pts',(31.9908990016263,21.1243034951469,43.5345782986958));
#66296=CARTESIAN_POINT('Ctrl Pts',(31.9923707061805,21.0986367658887,43.5329468400452));
#66297=CARTESIAN_POINT('Ctrl Pts',(31.9930802915876,21.0830736382594,43.5319679792066));
#66298=CARTESIAN_POINT('Ctrl Pts',(31.9953517571622,21.0159892800327,43.527787203557));
#66299=CARTESIAN_POINT('Ctrl Pts',(31.9950988573542,20.9644224949877,43.524671268508));
#66300=CARTESIAN_POINT('Ctrl Pts',(31.9878505935331,20.7985454912254,43.5148003657302));
#66301=CARTESIAN_POINT('Ctrl Pts',(31.9730158214738,20.6848095369619,43.5082551062922));
#66302=CARTESIAN_POINT('Ctrl Pts',(31.9283014350427,20.480781310097,43.4960647628718));
#66303=CARTESIAN_POINT('Ctrl Pts',(31.9015829706425,20.3901526504345,43.4904806667342));
#66304=CARTESIAN_POINT('Ctrl Pts',(31.8589352006138,20.2760231828673,43.4830045821435));
#66305=CARTESIAN_POINT('Ctrl Pts',(31.8487870602047,20.2504876226934,43.4813025943932));
#66306=CARTESIAN_POINT('Ctrl Pts',(31.8310797665129,20.2084808921122,43.4784493971274));
#66307=CARTESIAN_POINT('Ctrl Pts',(31.8238176276996,20.1918881045496,43.4773082886313));
#66308=CARTESIAN_POINT('Ctrl Pts',(31.8089987390734,20.1592469417025,43.4750343079978));
#66309=CARTESIAN_POINT('Ctrl Pts',(31.8014518725999,20.1431959032608,43.4739018586037));
#66310=CARTESIAN_POINT('Ctrl Pts',(31.782534687863,20.1043170371959,43.471122900093));
#66311=CARTESIAN_POINT('Ctrl Pts',(31.770938953892,20.0816030243807,43.4694686639209));
#66312=CARTESIAN_POINT('Ctrl Pts',(31.7233421620989,19.9926241996373,43.4628628046646));
#66313=CARTESIAN_POINT('Ctrl Pts',(31.6840350887696,19.9282081847288,43.4577968185174));
#66314=CARTESIAN_POINT('Ctrl Pts',(31.5413784611171,19.7217161722009,43.4406146360501));
#66315=CARTESIAN_POINT('Ctrl Pts',(31.4229490004582,19.5910752817616,43.4280771356335));
#66316=CARTESIAN_POINT('Ctrl Pts',(31.2709972643198,19.4624216554745,43.4147291983983));
#66317=CARTESIAN_POINT('Ctrl Pts',(31.2527710256067,19.4475354808809,43.4131679682555));
#66318=CARTESIAN_POINT('Ctrl Pts',(31.2250472564142,19.4256985506448,43.4108573565383));
#66319=CARTESIAN_POINT('Ctrl Pts',(31.2157453348637,19.4185041475645,43.4100926319294));
#66320=CARTESIAN_POINT('Ctrl Pts',(31.1986340863152,19.4055099590714,43.4087058441411));
#66321=CARTESIAN_POINT('Ctrl Pts',(31.1908454628857,19.3996846394145,43.4080821205776));
#66322=CARTESIAN_POINT('Ctrl Pts',(31.1725200444757,19.3861864484507,43.4066317361962));
#66323=CARTESIAN_POINT('Ctrl Pts',(31.1619502316944,19.3785595555996,43.4058081575944));
#66324=CARTESIAN_POINT('Ctrl Pts',(31.1261208434795,19.3532363396745,43.4030569789227));
#66325=CARTESIAN_POINT('Ctrl Pts',(31.1005246078938,19.33602147598,43.4011585570759));
#66326=CARTESIAN_POINT('Ctrl Pts',(31.0346986335612,19.2939336725087,43.3964156204727));
#66327=CARTESIAN_POINT('Ctrl Pts',(30.9939637494232,19.269884347901,43.3936076573272));
#66328=CARTESIAN_POINT('Ctrl Pts',(30.8489025580446,19.1910584671423,43.383909854898));
#66329=CARTESIAN_POINT('Ctrl Pts',(30.7406158838818,19.1440921324093,43.3771827697945));
#66330=CARTESIAN_POINT('Ctrl Pts',(30.5586975361323,19.0836639849032,43.3658981599773));
#66331=CARTESIAN_POINT('Ctrl Pts',(30.4873455567504,19.0642884203696,43.3614792345496));
#66332=CARTESIAN_POINT('Ctrl Pts',(30.3898087282433,19.0435377101883,43.3553456285742));
#66333=CARTESIAN_POINT('Ctrl Pts',(30.3644281339738,19.0386515925899,43.3537415699144));
#66334=CARTESIAN_POINT('Ctrl Pts',(30.3231856491976,19.0315399804467,43.3511186350178));
#66335=CARTESIAN_POINT('Ctrl Pts',(30.3073788591667,19.0290098870719,43.3501094953364));
#66336=CARTESIAN_POINT('Ctrl Pts',(30.2740533736098,19.0240863127295,43.3479729721359));
#66337=CARTESIAN_POINT('Ctrl Pts',(30.2565299557451,19.0217349773851,43.346844349799));
#66338=CARTESIAN_POINT('Ctrl Pts',(30.2138821295975,19.016588551608,43.3440839754862));
#66339=CARTESIAN_POINT('Ctrl Pts',(30.1887319229865,19.0140375878038,43.3424447043373));
#66340=CARTESIAN_POINT('Ctrl Pts',(30.0904452194266,19.00595226514,43.3359910516247));
#66341=CARTESIAN_POINT('Ctrl Pts',(30.0170817699942,19.0039757621825,43.3310689079429));
#66342=CARTESIAN_POINT('Ctrl Pts',(29.7843679209693,19.0105368229914,43.3151489816202));
#66343=CARTESIAN_POINT('Ctrl Pts',(29.6260817985685,19.0341309674039,43.3038147911729));
#66344=CARTESIAN_POINT('Ctrl Pts',(29.4377187319013,19.0858022009012,43.2905305088687));
#66345=CARTESIAN_POINT('Ctrl Pts',(29.4033967692643,19.096219976235,43.2881215268011));
#66346=CARTESIAN_POINT('Ctrl Pts',(29.3559646359744,19.1120260238118,43.2848255770495));
#66347=CARTESIAN_POINT('Ctrl Pts',(29.3426045357498,19.1166363823728,43.2839009580244));
#66348=CARTESIAN_POINT('Ctrl Pts',(29.3200101810381,19.1247030671766,43.2823449731727));
#66349=CARTESIAN_POINT('Ctrl Pts',(29.3107506811249,19.1280865047484,43.2817095546446));
#66350=CARTESIAN_POINT('Ctrl Pts',(29.2910993191093,19.1354327417787,43.2803661908165));
#66351=CARTESIAN_POINT('Ctrl Pts',(29.2807149857724,19.1394139852677,43.2796593137605));
#66352=CARTESIAN_POINT('Ctrl Pts',(29.2514427676125,19.1509183489061,43.2776737386625));
#66353=CARTESIAN_POINT('Ctrl Pts',(29.2326352716421,19.1586438881002,43.2764063304131));
#66354=CARTESIAN_POINT('Ctrl Pts',(29.1895969138712,19.1770967107957,43.2735180699403));
#66355=CARTESIAN_POINT('Ctrl Pts',(29.1654547828793,19.1880220824636,43.2719068328023));
#66356=CARTESIAN_POINT('Ctrl Pts',(29.0813298082701,19.2281305227763,43.2662997701629));
#66357=CARTESIAN_POINT('Ctrl Pts',(29.0225969355971,19.2598388824206,43.2623976737636));
#66358=CARTESIAN_POINT('Ctrl Pts',(28.8357247808209,19.3731782763768,43.249687921577));
#66359=CARTESIAN_POINT('Ctrl Pts',(28.715318195442,19.4664831235668,43.2409774235967));
#66360=CARTESIAN_POINT('Ctrl Pts',(28.58462819906,19.5940489199549,43.2298230006952));
#66361=CARTESIAN_POINT('Ctrl Pts',(28.5630944216885,19.6160643166225,43.2279226427976));
#66362=CARTESIAN_POINT('Ctrl Pts',(28.5292651093641,19.6522912138913,43.2248280116066));
#66363=CARTESIAN_POINT('Ctrl Pts',(28.5166452869764,19.666193849358,43.2236477555485));
#66364=CARTESIAN_POINT('Ctrl Pts',(28.4927276307034,19.6933020587124,43.2213590918447));
#66365=CARTESIAN_POINT('Ctrl Pts',(28.4814023913869,19.7064812422387,43.2202519819266));
#66366=CARTESIAN_POINT('Ctrl Pts',(28.4552608911049,19.7377186513514,43.2176398380794));
#66367=CARTESIAN_POINT('Ctrl Pts',(28.4405870448702,19.7558921766655,43.216129211817));
#66368=CARTESIAN_POINT('Ctrl Pts',(28.3914121465172,19.8190322978477,43.2109092976681));
#66369=CARTESIAN_POINT('Ctrl Pts',(28.358512638366,19.8652058332883,43.2071392820906));
#66370=CARTESIAN_POINT('Ctrl Pts',(28.2776772929377,19.9895401042565,43.1971085462961));
#66371=CARTESIAN_POINT('Ctrl Pts',(28.2330863828662,20.0697106599523,43.1907536704131));
#66372=CARTESIAN_POINT('Ctrl Pts',(28.1471594836605,20.2528350855162,43.1766482753025));
#66373=CARTESIAN_POINT('Ctrl Pts',(28.108566446692,20.356761116617,43.1689034170037));
#66374=CARTESIAN_POINT('Ctrl Pts',(28.0730720104802,20.4838333496819,43.1600844304603));
#66375=CARTESIAN_POINT('Ctrl Pts',(28.0676802889236,20.5043992455265,43.1586771868361));
#66376=CARTESIAN_POINT('Ctrl Pts',(28.0598942369577,20.5361594384987,43.1565387148991));
#66377=CARTESIAN_POINT('Ctrl Pts',(28.0572658950715,20.547294078642,43.1557955172322));
#66378=CARTESIAN_POINT('Ctrl Pts',(28.0525678977407,20.5679913466663,43.1544268973397));
#66379=CARTESIAN_POINT('Ctrl Pts',(28.0504726747473,20.5775470653204,43.1538001653878));
#66380=CARTESIAN_POINT('Ctrl Pts',(28.0456444465739,20.6003684754785,43.1523151272805));
#66381=CARTESIAN_POINT('Ctrl Pts',(28.0429761116337,20.6136471700731,43.1514604052235));
#66382=CARTESIAN_POINT('Ctrl Pts',(28.0375339726221,20.6422338227295,43.1496383806582));
#66383=CARTESIAN_POINT('Ctrl Pts',(28.0348035627497,20.6575492134602,43.1486732776327));
#66384=CARTESIAN_POINT('Ctrl Pts',(28.0143824897498,20.780395314158,43.1410090841369));
#66385=CARTESIAN_POINT('Ctrl Pts',(28.0053502109873,20.8891881959974,43.1346859693093));
#66386=CARTESIAN_POINT('Ctrl Pts',(28.0052508292294,20.9981811514481,43.1283621734979));
#66387=CARTESIAN_POINT('Ctrl Pts',(28.0052508296975,20.9981806381507,43.1283622032795));
#66388=CARTESIAN_POINT('Ctrl Pts',(28.0051575468002,21.100456049772,43.1224281608178));
#66389=CARTESIAN_POINT('Ctrl Pts',(28.0129302759012,21.2025865436209,43.1165093493538));
#66390=CARTESIAN_POINT('Ctrl Pts',(28.0348692664432,21.3450208815619,43.1078833761945));
#66391=CARTESIAN_POINT('Ctrl Pts',(28.0425379878242,21.3861610186594,43.1053486980223));
#66392=CARTESIAN_POINT('Ctrl Pts',(28.057019440693,21.4522391565893,43.1011874450745));
#66393=CARTESIAN_POINT('Ctrl Pts',(28.0630332747366,21.4773400446866,43.0995854429704));
#66394=CARTESIAN_POINT('Ctrl Pts',(28.0740113161425,21.5195301039075,43.0968530359029));
#66395=CARTESIAN_POINT('Ctrl Pts',(28.078720336925,21.5366827390298,43.0957309424151));
#66396=CARTESIAN_POINT('Ctrl Pts',(28.0886634353991,21.5710912275362,43.093456247345));
#66397=CARTESIAN_POINT('Ctrl Pts',(28.0939033635702,21.5883436331431,43.092303545833));
#66398=CARTESIAN_POINT('Ctrl Pts',(28.1075990639989,21.6313319391092,43.0893996912599));
#66399=CARTESIAN_POINT('Ctrl Pts',(28.116346347439,21.656970408273,43.0876391223986));
#66400=CARTESIAN_POINT('Ctrl Pts',(28.1553294756208,21.7640441893786,43.0801614552955));
#66401=CARTESIAN_POINT('Ctrl Pts',(28.1903421633059,21.8436278410252,43.0742899891985));
#66402=CARTESIAN_POINT('Ctrl Pts',(28.3002606114928,22.0548971436403,43.0578838579579));
#66403=CARTESIAN_POINT('Ctrl Pts',(28.3851390032103,22.1807392304034,43.0471438130278));
#66404=CARTESIAN_POINT('Ctrl Pts',(28.5026476520882,22.3182712363283,43.0349254220984));
#66405=CARTESIAN_POINT('Ctrl Pts',(28.5223682166808,22.3403386262353,43.0329498539754));
#66406=CARTESIAN_POINT('Ctrl Pts',(28.5513376477725,22.3713386570934,43.0301624731613));
#66407=CARTESIAN_POINT('Ctrl Pts',(28.5601922592514,22.3806324688641,43.0293251988895));
#66408=CARTESIAN_POINT('Ctrl Pts',(28.5752607218007,22.3961457004857,43.0279258671541));
#66409=CARTESIAN_POINT('Ctrl Pts',(28.5814268631953,22.4024104585032,43.0273603147149));
#66410=CARTESIAN_POINT('Ctrl Pts',(28.5957329398242,22.4167544249713,43.0260644996492));
#66411=CARTESIAN_POINT('Ctrl Pts',(28.6039013996792,22.4248044744791,43.0253364793193));
#66412=CARTESIAN_POINT('Ctrl Pts',(28.6275141550667,22.4476768850051,43.0232640588527));
#66413=CARTESIAN_POINT('Ctrl Pts',(28.6431286927497,22.4623221598299,43.0219322806814));
#66414=CARTESIAN_POINT('Ctrl Pts',(28.7646585951437,22.5726850625445,43.0118306323689));
#66415=CARTESIAN_POINT('Ctrl Pts',(28.8803508011276,22.6570463917626,43.0036987174494));
#66416=CARTESIAN_POINT('Ctrl Pts',(29.0121854654742,22.7330140496434,42.9948466360735));
#66417=CARTESIAN_POINT('Ctrl Pts',(29.0203307266711,22.7376315252329,42.9943013992332));
#66418=CARTESIAN_POINT('Ctrl Pts',(29.0285070614011,22.7421908715042,42.9937555338539));
#66419=CARTESIAN_POINT('',(28.0052500657895,21.0005123153922,42.9704548813466));
#66420=CARTESIAN_POINT('Ctrl Pts',(29.0285070491141,22.7421908646526,42.8352639371872));
#66421=CARTESIAN_POINT('Ctrl Pts',(28.9676043214511,22.7082298493501,42.8397032533362));
#66422=CARTESIAN_POINT('Ctrl Pts',(28.9084579756291,22.6710567323345,42.8441425694852));
#66423=CARTESIAN_POINT('Ctrl Pts',(28.8514195787486,22.630886439461,42.8485818856342));
#66424=CARTESIAN_POINT('Ctrl Pts',(28.7943843275944,22.5907183620206,42.8530209569504));
#66425=CARTESIAN_POINT('Ctrl Pts',(28.7394571936289,22.5475537200229,42.8574600282666));
#66426=CARTESIAN_POINT('Ctrl Pts',(28.6869597943234,22.5016500859976,42.8618990995827));
#66427=CARTESIAN_POINT('Ctrl Pts',(28.6344105100008,22.4557010838044,42.8663425581884));
#66428=CARTESIAN_POINT('Ctrl Pts',(28.5842961259823,22.407008005524,42.8707860167941));
#66429=CARTESIAN_POINT('Ctrl Pts',(28.5369035317666,22.3558673560282,42.8752294753998));
#66430=CARTESIAN_POINT('Ctrl Pts',(28.4894877185934,22.3047016512978,42.8796751109802));
#66431=CARTESIAN_POINT('Ctrl Pts',(28.4447966652341,22.2510863630922,42.8841207465606));
#66432=CARTESIAN_POINT('Ctrl Pts',(28.4030770036123,22.1953512061767,42.8885663821409));
#66433=CARTESIAN_POINT('Ctrl Pts',(28.3612809330586,22.1395139711608,42.8930201598359));
#66434=CARTESIAN_POINT('Ctrl Pts',(28.3224673990012,22.0815495186362,42.8974739375308));
#66435=CARTESIAN_POINT('Ctrl Pts',(28.2868393962484,22.0218161812447,42.9019277152258));
#66436=CARTESIAN_POINT('Ctrl Pts',(28.2572421195932,21.9721938624023,42.9056276052116));
#66437=CARTESIAN_POINT('Ctrl Pts',(28.2298424575127,21.9213514203603,42.9093274951974));
#66438=CARTESIAN_POINT('Ctrl Pts',(28.2047316173072,21.8695050296597,42.9130273851831));
#66439=CARTESIAN_POINT('Ctrl Pts',(28.172226069602,21.802390774921,42.9178168286845));
#66440=CARTESIAN_POINT('Ctrl Pts',(28.1434437524186,21.7333607547642,42.9226062721859));
#66441=CARTESIAN_POINT('Ctrl Pts',(28.1185963344277,21.6628331688072,42.9273957156873));
#66442=CARTESIAN_POINT('Ctrl Pts',(28.0938078213605,21.5924727801853,42.9321738050188));
#66443=CARTESIAN_POINT('Ctrl Pts',(28.0729357673716,21.5206222383229,42.9369518943504));
#66444=CARTESIAN_POINT('Ctrl Pts',(28.0561447218307,21.4477211409275,42.9417299836819));
#66445=CARTESIAN_POINT('Ctrl Pts',(28.0393206654845,21.3746767216689,42.946517466626));
#66446=CARTESIAN_POINT('Ctrl Pts',(28.026593877544,21.3005779437398,42.9513049495702));
#66447=CARTESIAN_POINT('Ctrl Pts',(28.018081031935,21.2258866231632,42.9560924325143));
#66448=CARTESIAN_POINT('Ctrl Pts',(28.009568186326,21.1511953025866,42.9608799154584));
#66449=CARTESIAN_POINT('Ctrl Pts',(28.0052694307819,21.0759118017932,42.9656673984025));
#66450=CARTESIAN_POINT('Ctrl Pts',(28.0052500657895,21.0005123153922,42.9704548813466));
#66451=CARTESIAN_POINT('Ctrl Pts',(28.0052500657893,21.0005123146269,42.9704548813952));
#66452=CARTESIAN_POINT('Ctrl Pts',(28.0052315890006,20.9285710288132,42.9750227862344));
#66453=CARTESIAN_POINT('Ctrl Pts',(28.0091093251767,20.8566709192213,42.9795906910737));
#66454=CARTESIAN_POINT('Ctrl Pts',(28.0168438583246,20.7852460006537,42.9841585959129));
#66455=CARTESIAN_POINT('Ctrl Pts',(28.0247173355178,20.7125379966142,42.9888085591213));
#66456=CARTESIAN_POINT('Ctrl Pts',(28.0365874783279,20.6403229044772,42.9934585223298));
#66457=CARTESIAN_POINT('Ctrl Pts',(28.0523582884808,20.5690483483606,42.9981084855382));
#66458=CARTESIAN_POINT('Ctrl Pts',(28.0678961341488,20.4988266512979,43.0026897600569));
#66459=CARTESIAN_POINT('Ctrl Pts',(28.0872199703106,20.4295183000286,43.0072710345757));
#66460=CARTESIAN_POINT('Ctrl Pts',(28.110187832642,20.3615350169306,43.0118523090945));
#66461=CARTESIAN_POINT('Ctrl Pts',(28.1336722430523,20.2920227872651,43.0165366166477));
#66462=CARTESIAN_POINT('Ctrl Pts',(28.1609663851651,20.2238964124189,43.021220924201));
#66463=CARTESIAN_POINT('Ctrl Pts',(28.1918677488796,20.1575717686602,43.0259052317542));
#66464=CARTESIAN_POINT('Ctrl Pts',(28.2227691125942,20.0912471249015,43.0305895393075));
#66465=CARTESIAN_POINT('Ctrl Pts',(28.2572774009503,20.0267246113575,43.0352738468607));
#66466=CARTESIAN_POINT('Ctrl Pts',(28.2951427975274,19.9643893194461,43.0399581544139));
#66467=CARTESIAN_POINT('Ctrl Pts',(28.3311550803602,19.9051046858306,43.0444132142768));
#66468=CARTESIAN_POINT('Ctrl Pts',(28.370334308345,19.8475839752533,43.0488682741397));
#66469=CARTESIAN_POINT('Ctrl Pts',(28.4124822494109,19.7921858776846,43.0533233340026));
#66470=CARTESIAN_POINT('Ctrl Pts',(28.4545670645535,19.7368707510979,43.0577717214217));
#66471=CARTESIAN_POINT('Ctrl Pts',(28.4996114739023,19.6836723139527,43.0622201088408));
#66472=CARTESIAN_POINT('Ctrl Pts',(28.5473729125965,19.6329220550964,43.0666684962599));
#66473=CARTESIAN_POINT('Ctrl Pts',(28.5950783241406,19.582231329463,43.0711116654428));
#66474=CARTESIAN_POINT('Ctrl Pts',(28.6454941009277,19.5339834327497,43.0755548346257));
#66475=CARTESIAN_POINT('Ctrl Pts',(28.6983373245162,19.488476979417,43.0799980038085));
#66476=CARTESIAN_POINT('Ctrl Pts',(28.7511474152525,19.4429990587606,43.0844383871116));
#66477=CARTESIAN_POINT('Ctrl Pts',(28.806381563471,19.4002594900602,43.0888787704147));
#66478=CARTESIAN_POINT('Ctrl Pts',(28.8637209981286,19.3605191088621,43.0933191537178));
#66479=CARTESIAN_POINT('Ctrl Pts',(28.921043938715,19.3207901592502,43.097758259715));
#66480=CARTESIAN_POINT('Ctrl Pts',(28.9804705615396,19.2840589629842,43.1021973657121));
#66481=CARTESIAN_POINT('Ctrl Pts',(29.041651544354,19.2505441417227,43.1066364717093));
#66482=CARTESIAN_POINT('Ctrl Pts',(29.1028356889423,19.2170275884477,43.1110758071152));
#66483=CARTESIAN_POINT('Ctrl Pts',(29.1657739432408,19.1867279731321,43.1155151425211));
#66484=CARTESIAN_POINT('Ctrl Pts',(29.2300922897317,19.1598180306911,43.1199544779269));
#66485=CARTESIAN_POINT('Ctrl Pts',(29.2944786044112,19.1328796512622,43.124398504585));
#66486=CARTESIAN_POINT('Ctrl Pts',(29.3602474698537,19.109338283279,43.1288425312431));
#66487=CARTESIAN_POINT('Ctrl Pts',(29.4270056846385,19.0893181643551,43.1332865579012));
#66488=CARTESIAN_POINT('Ctrl Pts',(29.4938030002935,19.0692863194725,43.1377331874646));
#66489=CARTESIAN_POINT('Ctrl Pts',(29.5615903431448,19.0527799444847,43.1421798170279));
#66490=CARTESIAN_POINT('Ctrl Pts',(29.6299628912134,19.0398724274627,43.1466264465913));
#66491=CARTESIAN_POINT('Ctrl Pts',(29.6984538775444,19.0269425514103,43.1510807788233));
#66492=CARTESIAN_POINT('Ctrl Pts',(29.7675316077972,19.0176240426951,43.1555351110552));
#66493=CARTESIAN_POINT('Ctrl Pts',(29.836785498685,19.0119384845884,43.1599894432872));
#66494=CARTESIAN_POINT('Ctrl Pts',(29.8725421385118,19.0090029606659,43.162289270073));
#66495=CARTESIAN_POINT('Ctrl Pts',(29.9083457252291,19.0070350495679,43.1645890968589));
#66496=CARTESIAN_POINT('Ctrl Pts',(29.9441400223946,19.0060322907825,43.1668889236447));
#66497=CARTESIAN_POINT('Ctrl Pts',(30.013476684111,19.0040898599434,43.1713438878285));
#66498=CARTESIAN_POINT('Ctrl Pts',(30.0830513640872,19.0057644992935,43.1757988520123));
#66499=CARTESIAN_POINT('Ctrl Pts',(30.1524552307818,19.0110844751204,43.1802538161961));
#66500=CARTESIAN_POINT('Ctrl Pts',(30.2217551433558,19.0163964826101,43.1847021076697));
#66501=CARTESIAN_POINT('Ctrl Pts',(30.2908842665054,19.025342952452,43.1891503991434));
#66502=CARTESIAN_POINT('Ctrl Pts',(30.3594325425419,19.0379001529326,43.1935986906171));
#66503=CARTESIAN_POINT('Ctrl Pts',(30.4279004065346,19.0504426229165,43.1980417639258));
#66504=CARTESIAN_POINT('Ctrl Pts',(30.4957882977253,19.0665873231396,43.2024848372346));
#66505=CARTESIAN_POINT('Ctrl Pts',(30.5626918572463,19.0862587854444,43.2069279105433));
#66506=CARTESIAN_POINT('Ctrl Pts',(30.6295534686227,19.1059179138562,43.2113681980708));
#66507=CARTESIAN_POINT('Ctrl Pts',(30.6954315043164,19.1290992798999,43.2158084855983));
#66508=CARTESIAN_POINT('Ctrl Pts',(30.7599338670361,19.1556767961576,43.2202487731258));
#66509=CARTESIAN_POINT('Ctrl Pts',(30.8244176783201,19.1822466684924,43.2246877835883));
#66510=CARTESIAN_POINT('Ctrl Pts',(30.8875261499109,19.212210565625,43.2291267940508));
#66511=CARTESIAN_POINT('Ctrl Pts',(30.9488860490246,19.2453938252512,43.2335658045134));
#66512=CARTESIAN_POINT('Ctrl Pts',(31.0102491245282,19.2785788026602,43.2380050447681));
#66513=CARTESIAN_POINT('Ctrl Pts',(31.0698630185928,19.3149832385465,43.2424442850229));
#66514=CARTESIAN_POINT('Ctrl Pts',(31.1273796268829,19.3543868196355,43.2468835252776));
#66515=CARTESIAN_POINT('Ctrl Pts',(31.1849570328943,19.3938320521364,43.2513274580151));
#66516=CARTESIAN_POINT('Ctrl Pts',(31.2404323239127,19.4362824802109,43.2557713907526));
#66517=CARTESIAN_POINT('Ctrl Pts',(31.2934877086317,19.481475350836,43.2602153234901));
#66518=CARTESIAN_POINT('Ctrl Pts',(31.3465741757035,19.5266946975814,43.2646618596935));
#66519=CARTESIAN_POINT('Ctrl Pts',(31.3972375592853,19.5746593482535,43.269108395897));
#66520=CARTESIAN_POINT('Ctrl Pts',(31.4451964630248,19.6250691851003,43.2735549321004));
#66521=CARTESIAN_POINT('Ctrl Pts',(31.4932384653383,19.6755663672623,43.2780091728339));
#66522=CARTESIAN_POINT('Ctrl Pts',(31.5385663157919,19.728516821037,43.2824634135674));
#66523=CARTESIAN_POINT('Ctrl Pts',(31.5809389961577,19.7835874659771,43.2869176543009));
#66524=CARTESIAN_POINT('Ctrl Pts',(31.6028250961605,19.8120322476614,43.2892183338258));
#66525=CARTESIAN_POINT('Ctrl Pts',(31.6239235044829,19.841042193907,43.2915190133506));
#66526=CARTESIAN_POINT('Ctrl Pts',(31.64420572578,19.8705686856598,43.2938196928755));
#66527=CARTESIAN_POINT('Ctrl Pts',(31.6834810122304,19.9277449389153,43.2982748186748));
#66528=CARTESIAN_POINT('Ctrl Pts',(31.7198476813952,19.987084883945,43.3027299444742));
#66529=CARTESIAN_POINT('Ctrl Pts',(31.7530600371333,20.0482605037583,43.3071850702736));
#66530=CARTESIAN_POINT('Ctrl Pts',(31.7862226458395,20.1093444918449,43.3116335229755));
#66531=CARTESIAN_POINT('Ctrl Pts',(31.816240087075,20.1722582708793,43.3160819756775));
#66532=CARTESIAN_POINT('Ctrl Pts',(31.842909667823,20.2366445659166,43.3205304283794));
#66533=CARTESIAN_POINT('Ctrl Pts',(31.8695479563459,20.3009553145682,43.3249736615774));
#66534=CARTESIAN_POINT('Ctrl Pts',(31.8928459999688,20.3667346977639,43.3294168947754));
#66535=CARTESIAN_POINT('Ctrl Pts',(31.9126476483465,20.4336021400337,43.3338601279733));
#66536=CARTESIAN_POINT('Ctrl Pts',(31.9324368775625,20.5004276445029,43.3383005744724));
#66537=CARTESIAN_POINT('Ctrl Pts',(31.9487339231779,20.5683393862088,43.3427410209715));
#66538=CARTESIAN_POINT('Ctrl Pts',(31.9614318018113,20.6369396064796,43.3471814674706));
#66539=CARTESIAN_POINT('Ctrl Pts',(31.9741260252756,20.7055200797189,43.3516206357575));
#66540=CARTESIAN_POINT('Ctrl Pts',(31.9832230495419,20.7747881572225,43.3560598040443));
#66541=CARTESIAN_POINT('Ctrl Pts',(31.9886669258629,20.8443355516529,43.3604989723312));
#66542=CARTESIAN_POINT('Ctrl Pts',(31.9941110822947,20.9138865245966,43.3649383690325));
#66543=CARTESIAN_POINT('Ctrl Pts',(31.9959016818207,20.9837163550337,43.3693777657337));
#66544=CARTESIAN_POINT('Ctrl Pts',(31.9940347554633,21.0534130742823,43.373817162435));
#66545=CARTESIAN_POINT('Ctrl Pts',(31.992165857069,21.1231834142757,43.3782612484774));
#66546=CARTESIAN_POINT('Ctrl Pts',(31.986631734867,21.1928198723889,43.3827053345197));
#66547=CARTESIAN_POINT('Ctrl Pts',(31.9774805175999,21.2619128958506,43.3871494205621));
#66548=CARTESIAN_POINT('Ctrl Pts',(31.9683239425112,21.3310463716458,43.3915961085119));
#66549=CARTESIAN_POINT('Ctrl Pts',(31.9555461468695,21.3996352983827,43.3960427964617));
#66550=CARTESIAN_POINT('Ctrl Pts',(31.9392463972668,21.467280401031,43.4004894844115));
#66551=CARTESIAN_POINT('Ctrl Pts',(31.9229184207272,21.5350426474448,43.404943872871));
#66552=CARTESIAN_POINT('Ctrl Pts',(31.9030564551207,21.6018573383214,43.4093982613305));
#66553=CARTESIAN_POINT('Ctrl Pts',(31.8798093706742,21.6673412113945,43.41385264979));
#66554=CARTESIAN_POINT('Ctrl Pts',(31.8678096669461,21.7011427436964,43.4161519205621));
#66555=CARTESIAN_POINT('Ctrl Pts',(31.8549088062018,21.7345900268675,43.4184511913341));
#66556=CARTESIAN_POINT('Ctrl Pts',(31.8411320983547,21.7676328281854,43.4207504621062));
#66557=CARTESIAN_POINT('Ctrl Pts',(31.8144377949317,21.8316578894787,43.4252056216641));
#66558=CARTESIAN_POINT('Ctrl Pts',(31.7843472742764,21.8944148897016,43.4296607812221));
#66559=CARTESIAN_POINT('Ctrl Pts',(31.7510026322809,21.955519410711,43.43411594078));
#66560=CARTESIAN_POINT('Ctrl Pts',(31.7177079207047,22.0165324335313,43.4385644291616));
#66561=CARTESIAN_POINT('Ctrl Pts',(31.6811689916526,22.0758974623613,43.4430129175432));
#66562=CARTESIAN_POINT('Ctrl Pts',(31.6415758573719,22.1332503108289,43.4474614059249));
#66563=CARTESIAN_POINT('Ctrl Pts',(31.6020291550945,22.1905358999674,43.4519046774367));
#66564=CARTESIAN_POINT('Ctrl Pts',(31.5594356381618,22.2458135948522,43.4563479489484));
#66565=CARTESIAN_POINT('Ctrl Pts',(31.5140301536994,22.2987456472261,43.4607912204603));
#66566=CARTESIAN_POINT('Ctrl Pts',(31.4686531299256,22.3516445211707,43.4652317068775));
#66567=CARTESIAN_POINT('Ctrl Pts',(31.4204679530832,22.4022002988704,43.4696721932948));
#66568=CARTESIAN_POINT('Ctrl Pts',(31.3697505923319,22.4501071951088,43.4741126797121));
#66569=CARTESIAN_POINT('Ctrl Pts',(31.3190478133056,22.4980003176575,43.4785518894471));
#66570=CARTESIAN_POINT('Ctrl Pts',(31.2658146511744,22.5432457348615,43.4829910991822));
#66571=CARTESIAN_POINT('Ctrl Pts',(31.2103636225341,22.5855748054715,43.4874303089173));
#66572=CARTESIAN_POINT('Ctrl Pts',(31.1549097225232,22.6279060679697,43.4918697485239));
#66573=CARTESIAN_POINT('Ctrl Pts',(31.0972381183589,22.6673203891063,43.4963091881306));
#66574=CARTESIAN_POINT('Ctrl Pts',(31.0376926367861,22.7035907824533,43.5007486277373));
#66575=CARTESIAN_POINT('Ctrl Pts',(30.9780842325639,22.739899503297,43.5051927585698));
#66576=CARTESIAN_POINT('Ctrl Pts',(30.9165984174146,22.7730574104877,43.5096368894023));
#66577=CARTESIAN_POINT('Ctrl Pts',(30.8536052719579,22.802882581364,43.5140810202348));
#66578=CARTESIAN_POINT('Ctrl Pts',(30.7905752297746,22.8327252216199,43.5185277541105));
#66579=CARTESIAN_POINT('Ctrl Pts',(30.7260365526935,22.8592310542391,43.5229744879862));
#66580=CARTESIAN_POINT('Ctrl Pts',(30.6603784516242,22.8822666822558,43.5274212218619));
#66581=CARTESIAN_POINT('Ctrl Pts',(30.5946066304212,22.9053422080865,43.5318756575012));
#66582=CARTESIAN_POINT('Ctrl Pts',(30.5277119845147,22.9249353943831,43.5363300931405));
#66583=CARTESIAN_POINT('Ctrl Pts',(30.4600972060717,22.9409631947734,43.5407845287798));
#66584=CARTESIAN_POINT('Ctrl Pts',(30.4252017256148,22.9492350224443,43.5430834296322));
#66585=CARTESIAN_POINT('Ctrl Pts',(30.3901145785427,22.9565580456331,43.5453823304846));
#66586=CARTESIAN_POINT('Ctrl Pts',(30.3548916630846,22.9629262517917,43.547681231337));
#66587=CARTESIAN_POINT('Ctrl Pts',(30.2866570000519,22.9752628910422,43.5521347163188));
#66588=CARTESIAN_POINT('Ctrl Pts',(30.2176437364889,22.9840616924254,43.5565882013007));
#66589=CARTESIAN_POINT('Ctrl Pts',(30.1482514638409,22.9892332859594,43.5610416862825));
#66590=CARTESIAN_POINT('Ctrl Pts',(30.0789558713456,22.9943976742178,43.5654889664869));
#66591=CARTESIAN_POINT('Ctrl Pts',(30.0092828009534,22.9959448432096,43.5699362466913));
#66592=CARTESIAN_POINT('Ctrl Pts',(29.939641000981,22.9938365915334,43.5743835268957));
#66593=CARTESIAN_POINT('Ctrl Pts',(29.8700725681683,22.9917305608859,43.5788261219209));
#66594=CARTESIAN_POINT('Ctrl Pts',(29.8005358271373,22.9859767667221,43.583268716946));
#66595=CARTESIAN_POINT('Ctrl Pts',(29.7314418222075,22.9765889981584,43.5877113119711));
#66596=CARTESIAN_POINT('Ctrl Pts',(29.6623891556608,22.9672068462205,43.5921512490277));
#66597=CARTESIAN_POINT('Ctrl Pts',(29.5937791838954,22.954195096957,43.5965911860842));
#66598=CARTESIAN_POINT('Ctrl Pts',(29.5260184772164,22.9376194359471,43.6010311231407));
#66599=CARTESIAN_POINT('Ctrl Pts',(29.4582822691053,22.9210497677901,43.6054694549587));
#66600=CARTESIAN_POINT('Ctrl Pts',(29.3913951906568,22.9009188664662,43.6099077867767));
#66601=CARTESIAN_POINT('Ctrl Pts',(29.325752376959,22.8773432571918,43.6143461185947));
#66602=CARTESIAN_POINT('Ctrl Pts',(29.2600881752145,22.8537599664028,43.6187858965306));
#66603=CARTESIAN_POINT('Ctrl Pts',(29.1956695092175,22.826729890824,43.6232256744665));
#66604=CARTESIAN_POINT('Ctrl Pts',(29.1328738433149,22.7964186012432,43.6276654524023));
#66605=CARTESIAN_POINT('Ctrl Pts',(29.0975504373971,22.7793680935312,43.630162887153));
#66606=CARTESIAN_POINT('Ctrl Pts',(29.0627402181288,22.7612802096027,43.6326603219036));
#66607=CARTESIAN_POINT('Ctrl Pts',(29.0285070491141,22.7421908646526,43.6351577566542));
#66608=CARTESIAN_POINT('Origin',(30.,21.,36.25));
#66609=CARTESIAN_POINT('',(28.0000000001618,21.,36.5000000001618));
#66610=CARTESIAN_POINT('',(27.6389480828464,21.,36.1389480828464));
#66611=CARTESIAN_POINT('',(27.75,21.,36.25));
#66612=CARTESIAN_POINT('',(30.5154785150505,22.9324290162917,36.5000000000579));
#66613=CARTESIAN_POINT('Origin',(30.,21.,36.5));
#66614=CARTESIAN_POINT('Ctrl Pts',(30.5154785148818,22.9324290155263,36.5000000001618));
#66615=CARTESIAN_POINT('Ctrl Pts',(30.6725470225254,22.896963831748,36.493784254721));
#66616=CARTESIAN_POINT('Ctrl Pts',(30.8251103005109,22.8429178203948,36.4872213037502));
#66617=CARTESIAN_POINT('Ctrl Pts',(31.1331843487363,22.6910303567306,36.4725748213189));
#66618=CARTESIAN_POINT('Ctrl Pts',(31.2856502416904,22.5886637756194,36.464438023848));
#66619=CARTESIAN_POINT('Ctrl Pts',(31.6661050171744,22.2496122793256,36.4431572700421));
#66620=CARTESIAN_POINT('Ctrl Pts',(31.8103111325502,22.0141644029362,36.4343345358605));
#66621=CARTESIAN_POINT('Ctrl Pts',(32.00016320241,21.6224137148118,36.4188105171623));
#66622=CARTESIAN_POINT('Ctrl Pts',(32.0670581843828,21.3910802024333,36.4097864347362));
#66623=CARTESIAN_POINT('Ctrl Pts',(32.1218713381998,20.9151685390699,36.3901049253534));
#66624=CARTESIAN_POINT('Ctrl Pts',(32.1136324505546,20.6320256169199,36.3776789419417));
#66625=CARTESIAN_POINT('Ctrl Pts',(31.951644176216,20.0746445603385,36.3565413848938));
#66626=CARTESIAN_POINT('Ctrl Pts',(31.8286906741857,19.8349686552164,36.3481325716929));
#66627=CARTESIAN_POINT('Ctrl Pts',(31.5113517074335,19.4215656049671,36.3295587365625));
#66628=CARTESIAN_POINT('Ctrl Pts',(31.321691587591,19.2472068145484,36.3195469325908));
#66629=CARTESIAN_POINT('Ctrl Pts',(30.94481536976,19.00542470332,36.3014090707333));
#66630=CARTESIAN_POINT('Ctrl Pts',(30.7179098068827,18.8887223990991,36.2911367581791));
#66631=CARTESIAN_POINT('Ctrl Pts',(30.1336842972584,18.7558473108252,36.2709813071793));
#66632=CARTESIAN_POINT('Ctrl Pts',(29.8370876005783,18.7487109423105,36.261878322807));
#66633=CARTESIAN_POINT('Ctrl Pts',(29.250115499477,18.8471938271965,36.2404374312578));
#66634=CARTESIAN_POINT('Ctrl Pts',(28.9634161890183,18.9559319623666,36.2281041314165));
#66635=CARTESIAN_POINT('Ctrl Pts',(28.4570688608167,19.2758936012752,36.2053867063752));
#66636=CARTESIAN_POINT('Ctrl Pts',(28.2858618512514,19.4533624013602,36.1980121961921));
#66637=CARTESIAN_POINT('Ctrl Pts',(27.9798579491602,19.8253250174455,36.1831156023108));
#66638=CARTESIAN_POINT('Ctrl Pts',(27.8339165836195,20.0979204036427,36.1734663861722));
#66639=CARTESIAN_POINT('Ctrl Pts',(27.6821082997652,20.5873295890753,36.1548008720659));
#66640=CARTESIAN_POINT('Ctrl Pts',(27.6467202808314,20.7929343118159,36.1467202808314));
#66641=CARTESIAN_POINT('Ctrl Pts',(27.6389480828464,21.,36.1389480828464));
#66642=CARTESIAN_POINT('Origin',(30.,21.,36.25));
#66643=CARTESIAN_POINT('',(28.9249115396486,23.2020751695661,36.0495));
#66644=CARTESIAN_POINT('Ctrl Pts',(27.6389480828464,21.,36.1389480828464));
#66645=CARTESIAN_POINT('Ctrl Pts',(27.6350634289606,21.1034943437831,36.1350634289606));
#66646=CARTESIAN_POINT('Ctrl Pts',(27.6380797522175,21.2073543905297,36.1312731650575));
#66647=CARTESIAN_POINT('Ctrl Pts',(27.6738431552335,21.573368653005,36.1187710246431));
#66648=CARTESIAN_POINT('Ctrl Pts',(27.7446488307736,21.8299158156141,36.1113213734728));
#66649=CARTESIAN_POINT('Ctrl Pts',(27.9565827158724,22.2893220308902,36.0959653167334));
#66650=CARTESIAN_POINT('Ctrl Pts',(28.090608564173,22.4931862828733,36.0881804309061));
#66651=CARTESIAN_POINT('Ctrl Pts',(28.4431040524274,22.8879945187574,36.0697652258806));
#66652=CARTESIAN_POINT('Ctrl Pts',(28.6710763004339,23.0676251036898,36.0589567700887));
#66653=CARTESIAN_POINT('Ctrl Pts',(28.9249115396486,23.202075169566,36.0495));
#66654=CARTESIAN_POINT('',(31.0750884603512,23.2020751695661,36.0495));
#66655=CARTESIAN_POINT('Origin',(30.,21.,36.0495));
#66656=CARTESIAN_POINT('',(28.2709700121084,22.006441477355,36.4978425793705));
#66657=CARTESIAN_POINT('Ctrl Pts',(31.0750884603512,23.2020751695661,36.0495000000001));
#66658=CARTESIAN_POINT('Ctrl Pts',(30.7766255492167,23.3049251530177,36.0880189295469));
#66659=CARTESIAN_POINT('Ctrl Pts',(30.4645526145668,23.3541452362613,36.1209468496696));
#66660=CARTESIAN_POINT('Ctrl Pts',(29.8990342120443,23.3201776314801,36.1910429955509));
#66661=CARTESIAN_POINT('Ctrl Pts',(29.6557904663614,23.2623988165233,36.2250071891161));
#66662=CARTESIAN_POINT('Ctrl Pts',(29.3141204560412,23.1149875707035,36.2798402082991));
#66663=CARTESIAN_POINT('Ctrl Pts',(29.2069006842352,23.0575773165827,36.2981495320029));
#66664=CARTESIAN_POINT('Ctrl Pts',(28.9421107872916,22.8873688916963,36.3448128907834));
#66665=CARTESIAN_POINT('Ctrl Pts',(28.770120719906,22.7481449934132,36.3747716297848));
#66666=CARTESIAN_POINT('Ctrl Pts',(28.5396314493269,22.4860562450386,36.4198294545293));
#66667=CARTESIAN_POINT('Ctrl Pts',(28.4689142907509,22.3904700508477,36.435114483917));
#66668=CARTESIAN_POINT('Ctrl Pts',(28.353116026781,22.1991945540512,36.4654153193861));
#66669=CARTESIAN_POINT('Ctrl Pts',(28.3064636933393,22.1056760884109,36.4801215118855));
#66670=CARTESIAN_POINT('Ctrl Pts',(28.2679218920155,22.0085551104088,36.495685158741));
#66671=CARTESIAN_POINT('Origin',(30.,21.,36.5));
#66672=CARTESIAN_POINT('Origin',(30.,21.,40.25));
#66673=CARTESIAN_POINT('',(27.5481783129142,21.0004035148025,36.3073275271523));
#66674=CARTESIAN_POINT('Ctrl Pts',(27.5451094726466,21.0004046124501,36.3073274962121));
#66675=CARTESIAN_POINT('Ctrl Pts',(27.5450545228292,21.0257377592651,36.3060055102952));
#66676=CARTESIAN_POINT('Ctrl Pts',(27.5572991467173,21.8618031372997,36.2623732679693));
#66677=CARTESIAN_POINT('Ctrl Pts',(28.5079104395216,23.4802670136419,36.1764307692296));
#66678=CARTESIAN_POINT('Ctrl Pts',(30.3433301243472,23.5593313403256,36.0918102564103));
#66679=CARTESIAN_POINT('Ctrl Pts',(31.0750884603513,23.2020751695661,36.0495));
#66680=CARTESIAN_POINT('',(27.549294249036,21.0022449162321,36.1916725037879));
#66681=CARTESIAN_POINT('Ctrl Pts',(28.9249115396486,23.2020751695661,36.0495));
#66682=CARTESIAN_POINT('Ctrl Pts',(28.192355923267,22.8444297537228,36.0918563551502));
#66683=CARTESIAN_POINT('Ctrl Pts',(27.5953569563779,22.006174763075,36.1392471897461));
#66684=CARTESIAN_POINT('Ctrl Pts',(27.5465802851334,21.0987581685929,36.1866380243421));
#66685=CARTESIAN_POINT('Ctrl Pts',(27.5473247562997,21.0022467203435,36.1916725037879));
#66686=CARTESIAN_POINT('',(27.5495002532104,21.0011139947484,36.9916725037394));
#66687=CARTESIAN_POINT('Ctrl Pts',(27.5495010281166,21.0022447268166,36.1916725037879));
#66688=CARTESIAN_POINT('Ctrl Pts',(27.549428428816,20.9229903114318,36.195810481644));
#66689=CARTESIAN_POINT('Ctrl Pts',(27.553204866294,20.8435626405268,36.1999484595));
#66690=CARTESIAN_POINT('Ctrl Pts',(27.5608542041623,20.7643773426696,36.2040864373561));
#66691=CARTESIAN_POINT('Ctrl Pts',(27.5685220450517,20.6850005031061,36.2082344245871));
#66692=CARTESIAN_POINT('Ctrl Pts',(27.5800816086064,20.6058676998867,36.2123824118181));
#66693=CARTESIAN_POINT('Ctrl Pts',(27.5955043182853,20.5273999930013,36.2165303990492));
#66694=CARTESIAN_POINT('Ctrl Pts',(27.6108544724337,20.4493014343532,36.2206588722376));
#66695=CARTESIAN_POINT('Ctrl Pts',(27.6300314369191,20.3718622124444,36.2247873454261));
#66696=CARTESIAN_POINT('Ctrl Pts',(27.6529551516149,20.295492562375,36.2289158186145));
#66697=CARTESIAN_POINT('Ctrl Pts',(27.6758677400832,20.2191599789903,36.233042288012));
#66698=CARTESIAN_POINT('Ctrl Pts',(27.7025233332778,20.1438964028512,36.2371687574095));
#66699=CARTESIAN_POINT('Ctrl Pts',(27.7327913448585,20.0700993794758,36.241295226807));
#66700=CARTESIAN_POINT('Ctrl Pts',(27.7630547940436,19.9963134797649,36.2454210742084));
#66701=CARTESIAN_POINT('Ctrl Pts',(27.796929395648,19.9239941434461,36.2495469216097));
#66702=CARTESIAN_POINT('Ctrl Pts',(27.8342361287632,19.8535196887669,36.2536727690111));
#66703=CARTESIAN_POINT('Ctrl Pts',(27.8718858574065,19.7823972968176,36.2578365491686));
#66704=CARTESIAN_POINT('Ctrl Pts',(27.9130309380522,19.7131543408591,36.2620003293261));
#66705=CARTESIAN_POINT('Ctrl Pts',(27.9574405506607,19.6461532044154,36.2661641094836));
#66706=CARTESIAN_POINT('Ctrl Pts',(28.0015021788096,19.5796770748988,36.2702952631284));
#66707=CARTESIAN_POINT('Ctrl Pts',(28.0487770158858,19.5154081132134,36.2744264167733));
#66708=CARTESIAN_POINT('Ctrl Pts',(28.0989980217184,19.4536682993066,36.2785575704181));
#66709=CARTESIAN_POINT('Ctrl Pts',(28.1498139713933,19.3911970838377,36.282737663832));
#66710=CARTESIAN_POINT('Ctrl Pts',(28.203646008288,19.3313157126013,36.2869177572458));
#66711=CARTESIAN_POINT('Ctrl Pts',(28.2601795210837,19.2743189891688,36.2910978506596));
#66712=CARTESIAN_POINT('Ctrl Pts',(28.3167130338795,19.2173222657362,36.2952779440734));
#66713=CARTESIAN_POINT('Ctrl Pts',(28.3759475971239,19.1632104753326,36.2994580374872));
#66714=CARTESIAN_POINT('Ctrl Pts',(28.4375364339365,19.1122346928911,36.303638130901));
#66715=CARTESIAN_POINT('Ctrl Pts',(28.499918561709,19.0606023202381,36.307872065733));
#66716=CARTESIAN_POINT('Ctrl Pts',(28.5649795566333,19.0119687699261,36.312106000565));
#66717=CARTESIAN_POINT('Ctrl Pts',(28.632399355623,18.9666238106293,36.316339935397));
#66718=CARTESIAN_POINT('Ctrl Pts',(28.6997218908088,18.9213442686624,36.3205677621032));
#66719=CARTESIAN_POINT('Ctrl Pts',(28.7693960893656,18.8793441517372,36.3247955888095));
#66720=CARTESIAN_POINT('Ctrl Pts',(28.8410686199956,18.840873253734,36.3290234155158));
#66721=CARTESIAN_POINT('Ctrl Pts',(28.9128936812984,18.8023204834724,36.3332602397173));
#66722=CARTESIAN_POINT('Ctrl Pts',(28.9867252206828,18.7673122618253,36.3374970639188));
#66723=CARTESIAN_POINT('Ctrl Pts',(29.0621781153025,18.7360564577308,36.3417338881202));
#66724=CARTESIAN_POINT('Ctrl Pts',(29.1373332467312,18.7049239998381,36.3459539923496));
#66725=CARTESIAN_POINT('Ctrl Pts',(29.2140965340676,18.6775145881152,36.350174096579));
#66726=CARTESIAN_POINT('Ctrl Pts',(29.29206414284,18.653986983807,36.3543942008084));
#66727=CARTESIAN_POINT('Ctrl Pts',(29.3700050755609,18.6304674292978,36.3586128611597));
#66728=CARTESIAN_POINT('Ctrl Pts',(29.4491490673368,18.6108271786092,36.362831521511));
#66729=CARTESIAN_POINT('Ctrl Pts',(29.5290758863624,18.5951755304816,36.3670501818624));
#66730=CARTESIAN_POINT('Ctrl Pts',(29.6089997573466,18.5795244596534,36.3712686866116));
#66731=CARTESIAN_POINT('Ctrl Pts',(29.6897059423986,18.5678617870917,36.3754871913607));
#66732=CARTESIAN_POINT('Ctrl Pts',(29.7707641540447,18.5602456728332,36.3797056961099));
#66733=CARTESIAN_POINT('Ctrl Pts',(29.8524299465205,18.5525724711443,36.38395582113));
#66734=CARTESIAN_POINT('Ctrl Pts',(29.934452591178,18.5490068081063,36.3882059461502));
#66735=CARTESIAN_POINT('Ctrl Pts',(30.016388781063,18.5495548041519,36.3924560711703));
#66736=CARTESIAN_POINT('Ctrl Pts',(30.0978305074078,18.5500994931842,36.3966805477942));
#66737=CARTESIAN_POINT('Ctrl Pts',(30.1791863549369,18.5547082439169,36.4009050244181));
#66738=CARTESIAN_POINT('Ctrl Pts',(30.2600248042397,18.56333478886,36.405129501042));
#66739=CARTESIAN_POINT('Ctrl Pts',(30.3415994547678,18.5720398963312,36.4093924502602));
#66740=CARTESIAN_POINT('Ctrl Pts',(30.4226467581714,18.5848362767889,36.4136553994785));
#66741=CARTESIAN_POINT('Ctrl Pts',(30.5027343439812,18.6016237931922,36.4179183486967));
#66742=CARTESIAN_POINT('Ctrl Pts',(30.582821929791,18.6184113095955,36.422181297915));
#66743=CARTESIAN_POINT('Ctrl Pts',(30.6619493505619,18.639189779902,36.4264442471332));
#66744=CARTESIAN_POINT('Ctrl Pts',(30.7397022172849,18.663808466811,36.4307071963514));
#66745=CARTESIAN_POINT('Ctrl Pts',(30.8169981552416,18.6882824775595,36.4349450935786));
#66746=CARTESIAN_POINT('Ctrl Pts',(30.893217937062,18.7166410105943,36.4391829908057));
#66747=CARTESIAN_POINT('Ctrl Pts',(30.9679441397284,18.7487704709725,36.4434208880328));
#66748=CARTESIAN_POINT('Ctrl Pts',(31.0425656986694,18.7808549384793,36.4476528506702));
#66749=CARTESIAN_POINT('Ctrl Pts',(31.1156974107722,18.8166996628448,36.4518848133076));
#66750=CARTESIAN_POINT('Ctrl Pts',(31.1869376197398,18.8561414839485,36.4561167759451));
#66751=CARTESIAN_POINT('Ctrl Pts',(31.2582426267828,18.8956191802151,36.4603525878558));
#66752=CARTESIAN_POINT('Ctrl Pts',(31.3276522509388,18.9387003571713,36.4645883997665));
#66753=CARTESIAN_POINT('Ctrl Pts',(31.3947844469337,18.9851733085469,36.4688242116772));
#66754=CARTESIAN_POINT('Ctrl Pts',(31.4617394788274,19.031523616256,36.4730488451392));
#66755=CARTESIAN_POINT('Ctrl Pts',(31.5264286954501,19.0812475704348,36.4772734786011));
#66756=CARTESIAN_POINT('Ctrl Pts',(31.5884998541784,19.1340904461161,36.4814981120631));
#66757=CARTESIAN_POINT('Ctrl Pts',(31.6505518312119,19.1869169918959,36.4857214399972));
#66758=CARTESIAN_POINT('Ctrl Pts',(31.7099870047576,19.2428602448719,36.4899447679313));
#66759=CARTESIAN_POINT('Ctrl Pts',(31.7664859421674,19.3016249924928,36.4941680958654));
#66760=CARTESIAN_POINT('Ctrl Pts',(31.8229845685898,19.3603894166546,36.498391400553));
#66761=CARTESIAN_POINT('Ctrl Pts',(31.8765466708863,19.4219749698148,36.5026147052406));
#66762=CARTESIAN_POINT('Ctrl Pts',(31.9268904472431,19.4860503791991,36.5068380099283));
#66763=CARTESIAN_POINT('Ctrl Pts',(31.9774911053774,19.5504527367435,36.5110828642511));
#66764=CARTESIAN_POINT('Ctrl Pts',(32.0248402008895,19.6173700673117,36.5153277185739));
#66765=CARTESIAN_POINT('Ctrl Pts',(32.0686944067583,19.6864347365103,36.5195725728967));
#66766=CARTESIAN_POINT('Ctrl Pts',(32.112390543616,19.7552504675797,36.5238021269783));
#66767=CARTESIAN_POINT('Ctrl Pts',(32.1526167538075,19.8261976542578,36.52803168106));
#66768=CARTESIAN_POINT('Ctrl Pts',(32.1891783485836,19.8988876496502,36.5322612351417));
#66769=CARTESIAN_POINT('Ctrl Pts',(32.2259383334994,19.9719720747285,36.5365137395851));
#66770=CARTESIAN_POINT('Ctrl Pts',(32.258993628189,20.0468178436806,36.5407662440284));
#66771=CARTESIAN_POINT('Ctrl Pts',(32.2881959469411,20.1230110842193,36.5450187484718));
#66772=CARTESIAN_POINT('Ctrl Pts',(32.3173982656932,20.199204324758,36.5492712529152));
#66773=CARTESIAN_POINT('Ctrl Pts',(32.3427475219628,20.2767445716513,36.5535237573586));
#66774=CARTESIAN_POINT('Ctrl Pts',(32.3641469546119,20.3552059034085,36.557776261802));
#66775=CARTESIAN_POINT('Ctrl Pts',(32.3854168641285,20.4331923367125,36.5620030273529));
#66776=CARTESIAN_POINT('Ctrl Pts',(32.4028644942027,20.5123815769929,36.5662297929038));
#66777=CARTESIAN_POINT('Ctrl Pts',(32.4163574191108,20.5923640434059,36.5704565584547));
#66778=CARTESIAN_POINT('Ctrl Pts',(32.4298307746883,20.6722305080378,36.5746771937579));
#66779=CARTESIAN_POINT('Ctrl Pts',(32.4393607388843,20.7528874585296,36.578897829061));
#66780=CARTESIAN_POINT('Ctrl Pts',(32.4448649901705,20.8339113795637,36.5831184643642));
#66781=CARTESIAN_POINT('Ctrl Pts',(32.4503926948848,20.9152805407766,36.5873570836512));
#66782=CARTESIAN_POINT('Ctrl Pts',(32.4518601720758,20.9970193484073,36.5915957029382));
#66783=CARTESIAN_POINT('Ctrl Pts',(32.4492362431956,21.0786897389583,36.5958343222252));
#66784=CARTESIAN_POINT('Ctrl Pts',(32.4466282274135,21.1598648306634,36.6000472359508));
#66785=CARTESIAN_POINT('Ctrl Pts',(32.4399783047359,21.2409718618635,36.6042601496764));
#66786=CARTESIAN_POINT('Ctrl Pts',(32.4293080078248,21.3215786888434,36.608473063402));
#66787=CARTESIAN_POINT('Ctrl Pts',(32.4186413254627,21.4021582103671,36.6126845500086));
#66788=CARTESIAN_POINT('Ctrl Pts',(32.4039570342971,21.4822374024858,36.6168960366152));
#66789=CARTESIAN_POINT('Ctrl Pts',(32.3853284935868,21.5613895507426,36.6211075232219));
#66790=CARTESIAN_POINT('Ctrl Pts',(32.3667005227754,21.6405392775149,36.6253188809874));
#66791=CARTESIAN_POINT('Ctrl Pts',(32.3441286501096,21.7187615633856,36.6295302387529));
#66792=CARTESIAN_POINT('Ctrl Pts',(32.3177369713169,21.7956416164272,36.6337415965184));
#66793=CARTESIAN_POINT('Ctrl Pts',(32.2910489583739,21.8733849031178,36.6380002407463));
#66794=CARTESIAN_POINT('Ctrl Pts',(32.2604549617917,21.9497551595125,36.6422588849741));
#66795=CARTESIAN_POINT('Ctrl Pts',(32.2261338987918,22.0243427720495,36.6465175292019));
#66796=CARTESIAN_POINT('Ctrl Pts',(32.1921446677931,22.0982092368547,36.6507349988765));
#66797=CARTESIAN_POINT('Ctrl Pts',(32.1545004036852,22.1703269912888,36.6549524685511));
#66798=CARTESIAN_POINT('Ctrl Pts',(32.1134209899573,22.2403233325258,36.6591699382257));
#66799=CARTESIAN_POINT('Ctrl Pts',(32.0717399975677,22.3113447201659,36.6634491697301));
#66800=CARTESIAN_POINT('Ctrl Pts',(32.0265227061001,22.3801816435532,36.6677284012346));
#66801=CARTESIAN_POINT('Ctrl Pts',(31.9780429219995,22.4464772548255,36.6720076327391));
#66802=CARTESIAN_POINT('Ctrl Pts',(31.9295631378989,22.5127728660979,36.6762868642435));
#66803=CARTESIAN_POINT('Ctrl Pts',(31.8778212239518,22.5765268236252,36.680566095748));
#66804=CARTESIAN_POINT('Ctrl Pts',(31.8231303902993,22.6374204805019,36.6848453272525));
#66805=CARTESIAN_POINT('Ctrl Pts',(31.7690469632885,22.6976378410205,36.6890770328104));
#66806=CARTESIAN_POINT('Ctrl Pts',(31.71187556473,22.755285608444,36.6933087383683));
#66807=CARTESIAN_POINT('Ctrl Pts',(31.6518899209919,22.8100303696141,36.6975404439262));
#66808=CARTESIAN_POINT('Ctrl Pts',(31.5919903334818,22.8646965931983,36.7017660786212));
#66809=CARTESIAN_POINT('Ctrl Pts',(31.529284859754,22.9164677712883,36.7059917133163));
#66810=CARTESIAN_POINT('Ctrl Pts',(31.4640860108728,22.9650451401346,36.7102173480113));
#66811=CARTESIAN_POINT('Ctrl Pts',(31.3987059878403,23.013757495468,36.7144547248734));
#66812=CARTESIAN_POINT('Ctrl Pts',(31.3308190323845,23.0592579186859,36.7186921017356));
#66813=CARTESIAN_POINT('Ctrl Pts',(31.2607759414872,23.1012839587659,36.7229294785978));
#66814=CARTESIAN_POINT('Ctrl Pts',(31.1910527978004,23.1431180296722,36.7271474997049));
#66815=CARTESIAN_POINT('Ctrl Pts',(31.1191935713334,23.1815091424984,36.7313655208121));
#66816=CARTESIAN_POINT('Ctrl Pts',(31.0455741187681,23.2162411899796,36.7355835419192));
#66817=CARTESIAN_POINT('Ctrl Pts',(30.9719790620954,23.2509617280123,36.7398001652655));
#66818=CARTESIAN_POINT('Ctrl Pts',(30.8966253577217,23.2820254104759,36.7440167886118));
#66819=CARTESIAN_POINT('Ctrl Pts',(30.8199123304505,23.3092626572946,36.7482334119581));
#66820=CARTESIAN_POINT('Ctrl Pts',(30.7432012379335,23.3364992171715,36.7524499289583));
#66821=CARTESIAN_POINT('Ctrl Pts',(30.6651313290609,23.3599093787962,36.7566664459585));
#66822=CARTESIAN_POINT('Ctrl Pts',(30.586119361691,23.3793726786384,36.7608829629587));
#66823=CARTESIAN_POINT('Ctrl Pts',(30.5064308877364,23.3990026247615,36.765135582104));
#66824=CARTESIAN_POINT('Ctrl Pts',(30.4257846079184,23.4146176654465,36.7693882012494));
#66825=CARTESIAN_POINT('Ctrl Pts',(30.3446191376693,23.4261467185544,36.7736408203948));
#66826=CARTESIAN_POINT('Ctrl Pts',(30.2640260045932,23.4375944747063,36.777863452256));
#66827=CARTESIAN_POINT('Ctrl Pts',(30.1829214530076,23.4450137026212,36.7820860841172));
#66828=CARTESIAN_POINT('Ctrl Pts',(30.1017387329028,23.4483871181305,36.7863087159784));
#66829=CARTESIAN_POINT('Ctrl Pts',(30.0196912265546,23.4517964684215,36.7905763287658));
#66830=CARTESIAN_POINT('Ctrl Pts',(29.9375643634526,23.451073303568,36.7948439415532));
#66831=CARTESIAN_POINT('Ctrl Pts',(29.8558020879835,23.4462537096896,36.7991115543407));
#66832=CARTESIAN_POINT('Ctrl Pts',(29.7740398125144,23.4414341158111,36.8033791671281));
#66833=CARTESIAN_POINT('Ctrl Pts',(29.6926425978752,23.4325182093514,36.8076467799155));
#66834=CARTESIAN_POINT('Ctrl Pts',(29.6120438764149,23.4195950686371,36.811914392703));
#66835=CARTESIAN_POINT('Ctrl Pts',(29.5321215868013,23.4067803865159,36.8161461891754));
#66836=CARTESIAN_POINT('Ctrl Pts',(29.4526855303043,23.3899775974669,36.8203779856478));
#66837=CARTESIAN_POINT('Ctrl Pts',(29.3741642773118,23.3692361423478,36.8246097821202));
#66838=CARTESIAN_POINT('Ctrl Pts',(29.2957553799135,23.3485243660537,36.8288355233401));
#66839=CARTESIAN_POINT('Ctrl Pts',(29.218259131837,23.3238852346488,36.8330612645601));
#66840=CARTESIAN_POINT('Ctrl Pts',(29.1420959899604,23.2954195606812,36.8372870057801));
#66841=CARTESIAN_POINT('Ctrl Pts',(29.0657235765456,23.2668756723014,36.8415243579623));
#66842=CARTESIAN_POINT('Ctrl Pts',(28.9906920707856,23.2344842641582,36.8457617101445));
#66843=CARTESIAN_POINT('Ctrl Pts',(28.9174121060829,23.1983979853394,36.8499990623268));
#66844=CARTESIAN_POINT('Ctrl Pts',(28.8444639585092,23.1624751078742,36.8542172274632));
#66845=CARTESIAN_POINT('Ctrl Pts',(28.7732519469577,23.1228909491638,36.8584353925997));
#66846=CARTESIAN_POINT('Ctrl Pts',(28.7041613718838,23.079844345109,36.8626535577362));
#66847=CARTESIAN_POINT('Ctrl Pts',(28.6350934641233,23.0368118638324,36.8668703389723));
#66848=CARTESIAN_POINT('Ctrl Pts',(28.5681460048312,22.9903194386782,36.8710871202084));
#66849=CARTESIAN_POINT('Ctrl Pts',(28.5036779004829,22.9406108379829,36.8753039014445));
#66850=CARTESIAN_POINT('Ctrl Pts',(28.439211212496,22.8909033293833,36.8795205900381));
#66851=CARTESIAN_POINT('Ctrl Pts',(28.3772241385323,22.8379800704191,36.8837372786318));
#66852=CARTESIAN_POINT('Ctrl Pts',(28.3180437454976,22.7821260920429,36.8879539672254));
#66853=CARTESIAN_POINT('Ctrl Pts',(28.2583613418289,22.725798320073,36.8922064248027));
#66854=CARTESIAN_POINT('Ctrl Pts',(28.2015338236149,22.6664901878068,36.8964588823801));
#66855=CARTESIAN_POINT('Ctrl Pts',(28.1478585223756,22.6045317687298,36.9007113399574));
#66856=CARTESIAN_POINT('Ctrl Pts',(28.0945571147198,22.5430049421135,36.9049341755938));
#66857=CARTESIAN_POINT('Ctrl Pts',(28.044364387583,22.4788650428754,36.9091570112302));
#66858=CARTESIAN_POINT('Ctrl Pts',(27.9975296225177,22.4124668623744,36.9133798468667));
#66859=CARTESIAN_POINT('Ctrl Pts',(27.95020205945,22.3453700365259,36.9176471154145));
#66860=CARTESIAN_POINT('Ctrl Pts',(27.9063037987182,22.2759675382794,36.9219143839623));
#66861=CARTESIAN_POINT('Ctrl Pts',(27.8660449782421,22.2046519062013,36.9261816525101));
#66862=CARTESIAN_POINT('Ctrl Pts',(27.8257861577661,22.1333362741232,36.9304489210579));
#66863=CARTESIAN_POINT('Ctrl Pts',(27.7891669358602,22.0601079687253,36.9347161896056));
#66864=CARTESIAN_POINT('Ctrl Pts',(27.7563472401053,21.9853793903959,36.9389834581534));
#66865=CARTESIAN_POINT('Ctrl Pts',(27.7205636960295,21.9039022982149,36.9436360909293));
#66866=CARTESIAN_POINT('Ctrl Pts',(27.6891806545381,21.8203795186194,36.9482887237052));
#66867=CARTESIAN_POINT('Ctrl Pts',(27.6624130257218,21.7352804823228,36.9529413564811));
#66868=CARTESIAN_POINT('Ctrl Pts',(27.6357210655907,21.6504220101879,36.9575808368553));
#66869=CARTESIAN_POINT('Ctrl Pts',(27.6136186222774,21.5639964464178,36.9622203172296));
#66870=CARTESIAN_POINT('Ctrl Pts',(27.5962726571912,21.4764925093148,36.9668597976038));
#66871=CARTESIAN_POINT('Ctrl Pts',(27.5790101229767,21.3894094499039,36.9714769629388));
#66872=CARTESIAN_POINT('Ctrl Pts',(27.5664585478923,21.3012586502107,36.9760941282738));
#66873=CARTESIAN_POINT('Ctrl Pts',(27.5587346158157,21.2125407584051,36.9807112936088));
#66874=CARTESIAN_POINT('Ctrl Pts',(27.5526223776505,21.1423349514595,36.984365030319));
#66875=CARTESIAN_POINT('Ctrl Pts',(27.5495323753805,21.0717744441211,36.9880187670292));
#66876=CARTESIAN_POINT('Ctrl Pts',(27.5495002532104,21.0011139947484,36.9916725037394));
#66877=CARTESIAN_POINT('',(27.5495009409694,20.9978525154208,37.7916725038249));
#66878=CARTESIAN_POINT('Ctrl Pts',(27.54950025321,21.0011139938109,36.9916725037879));
#66879=CARTESIAN_POINT('Ctrl Pts',(27.5494625484464,20.9181732154581,36.9959612363013));
#66880=CARTESIAN_POINT('Ctrl Pts',(27.5536400688284,20.8352469267231,37.0002499688148));
#66881=CARTESIAN_POINT('Ctrl Pts',(27.5620020596278,20.7527829036236,37.0045387013282));
#66882=CARTESIAN_POINT('Ctrl Pts',(27.5703679671343,20.6702802548621,37.0088294426586));
#66883=CARTESIAN_POINT('Ctrl Pts',(27.582922197871,20.5882407421637,37.0131201839891));
#66884=CARTESIAN_POINT('Ctrl Pts',(27.5995823369894,20.5071051906271,37.0174109253195));
#66885=CARTESIAN_POINT('Ctrl Pts',(27.616268339477,20.4258436834359,37.0217083276404));
#66886=CARTESIAN_POINT('Ctrl Pts',(27.6370728896858,20.3454893738916,37.0260057299613));
#66887=CARTESIAN_POINT('Ctrl Pts',(27.6618628128603,20.2664710338954,37.0303031322822));
#66888=CARTESIAN_POINT('Ctrl Pts',(27.6866728284728,20.1873886488805,37.0346040176832));
#66889=CARTESIAN_POINT('Ctrl Pts',(27.7154744977915,20.10964480498,37.0389049030842));
#66890=CARTESIAN_POINT('Ctrl Pts',(27.7480861756485,20.0336489366206,37.0432057884853));
#66891=CARTESIAN_POINT('Ctrl Pts',(27.7807657956125,19.9574947409454,37.0475156342108));
#66892=CARTESIAN_POINT('Ctrl Pts',(27.8172710887893,19.8830961945644,37.0518254799363));
#66893=CARTESIAN_POINT('Ctrl Pts',(27.8573740094553,19.8108389029898,37.0561353256619));
#66894=CARTESIAN_POINT('Ctrl Pts',(27.8881337030832,19.7554162027401,37.0594410583092));
#66895=CARTESIAN_POINT('Ctrl Pts',(27.9210089886355,19.7012527444393,37.0627467909566));
#66896=CARTESIAN_POINT('Ctrl Pts',(27.9558803703251,19.648510011292,37.066052523604));
#66897=CARTESIAN_POINT('Ctrl Pts',(28.0005141389927,19.5810017326942,37.070283709726));
#66898=CARTESIAN_POINT('Ctrl Pts',(28.0485794793119,19.515580281312,37.074514895848));
#66899=CARTESIAN_POINT('Ctrl Pts',(28.0998547638172,19.4526156484532,37.0787460819699));
#66900=CARTESIAN_POINT('Ctrl Pts',(28.1510564908356,19.3897413421562,37.0829711982004));
#66901=CARTESIAN_POINT('Ctrl Pts',(28.2054587253515,19.3293172120294,37.0871963144308));
#66902=CARTESIAN_POINT('Ctrl Pts',(28.262796377712,19.2716846859703,37.0914214306612));
#66903=CARTESIAN_POINT('Ctrl Pts',(28.3203021756688,19.2138831495828,37.0956589372609));
#66904=CARTESIAN_POINT('Ctrl Pts',(28.3807603696501,19.1588900069677,37.0998964438606));
#66905=CARTESIAN_POINT('Ctrl Pts',(28.4438625134499,19.1070165418172,37.1041339504603));
#66906=CARTESIAN_POINT('Ctrl Pts',(28.5066668664837,19.0553878772074,37.1083514594774));
#66907=CARTESIAN_POINT('Ctrl Pts',(28.5720899129141,19.0068498136686,37.1125689684945));
#66908=CARTESIAN_POINT('Ctrl Pts',(28.6397917395243,18.9616713370671,37.1167864775115));
#66909=CARTESIAN_POINT('Ctrl Pts',(28.7074711859686,18.9165077950967,37.1210025923483));
#66910=CARTESIAN_POINT('Ctrl Pts',(28.7774275302302,18.8747018924866,37.1252187071851));
#66911=CARTESIAN_POINT('Ctrl Pts',(28.8492908033865,18.8364800451974,37.1294348220219));
#66912=CARTESIAN_POINT('Ctrl Pts',(28.9211523372027,18.7982591230092,37.1336508348141));
#66913=CARTESIAN_POINT('Ctrl Pts',(28.9949202971459,18.7636223010184,37.1378668476063));
#66914=CARTESIAN_POINT('Ctrl Pts',(29.0702002488022,18.7327499757035,37.1420828603985));
#66915=CARTESIAN_POINT('Ctrl Pts',(29.146144693929,18.7016051414651,37.1463360877865));
#66916=CARTESIAN_POINT('Ctrl Pts',(29.2236275173701,18.6742917902894,37.1505893151745));
#66917=CARTESIAN_POINT('Ctrl Pts',(29.302225073654,18.6509447852035,37.1548425425625));
#66918=CARTESIAN_POINT('Ctrl Pts',(29.3802482153376,18.6277684070585,37.1590646860845));
#66919=CARTESIAN_POINT('Ctrl Pts',(29.4593693789546,18.6085006425033,37.1632868296064));
#66920=CARTESIAN_POINT('Ctrl Pts',(29.5391626477447,18.5932222402627,37.1675089731284));
#66921=CARTESIAN_POINT('Ctrl Pts',(29.6198370862289,18.5777751162084,37.1717777424494));
#66922=CARTESIAN_POINT('Ctrl Pts',(29.7011980821515,18.566406074593,37.1760465117704));
#66923=CARTESIAN_POINT('Ctrl Pts',(29.7828007895734,18.5591446677466,37.1803152810914));
#66924=CARTESIAN_POINT('Ctrl Pts',(29.8644034969953,18.5518832609002,37.1845840504124));
#66925=CARTESIAN_POINT('Ctrl Pts',(29.9462474296876,18.5487294429638,37.1888528197334));
#66926=CARTESIAN_POINT('Ctrl Pts',(30.0278903659876,18.5496587222419,37.1931215890545));
#66927=CARTESIAN_POINT('Ctrl Pts',(30.1088136713796,18.5505798105102,37.1973527318706));
#66928=CARTESIAN_POINT('Ctrl Pts',(30.1898430919246,18.5555157117039,37.2015838746867));
#66929=CARTESIAN_POINT('Ctrl Pts',(30.2705475791037,18.5644807006634,37.2058150175028));
#66930=CARTESIAN_POINT('Ctrl Pts',(30.3511363101597,18.5734328309529,37.2100400915028));
#66931=CARTESIAN_POINT('Ctrl Pts',(30.4314005752773,18.5864025205923,37.2142651655029));
#66932=CARTESIAN_POINT('Ctrl Pts',(30.5109097747488,18.6033520383531,37.2184902395029));
#66933=CARTESIAN_POINT('Ctrl Pts',(30.5906531372581,18.6203514742441,37.2227277567947));
#66934=CARTESIAN_POINT('Ctrl Pts',(30.6696365071895,18.6413542062004,37.2269652740864));
#66935=CARTESIAN_POINT('Ctrl Pts',(30.7474311038938,18.6662697253255,37.2312027913782));
#66936=CARTESIAN_POINT('Ctrl Pts',(30.8248576571974,18.6910673700381,37.2354202611301));
#66937=CARTESIAN_POINT('Ctrl Pts',(30.9011062121426,18.7197407256736,37.2396377308821));
#66938=CARTESIAN_POINT('Ctrl Pts',(30.9757664962261,18.752149917178,37.243855200634));
#66939=CARTESIAN_POINT('Ctrl Pts',(31.0504021211007,18.7845484043966,37.2480712774169));
#66940=CARTESIAN_POINT('Ctrl Pts',(31.1234500906999,18.8206800921638,37.2522873541997));
#66941=CARTESIAN_POINT('Ctrl Pts',(31.1945196187994,18.8603567749965,37.2565034309826));
#66942=CARTESIAN_POINT('Ctrl Pts',(31.2655874481501,18.9000325094521,37.2607194069901));
#66943=CARTESIAN_POINT('Ctrl Pts',(31.3346765246005,18.943252842894,37.2649353829977));
#66944=CARTESIAN_POINT('Ctrl Pts',(31.4014214770758,18.9897840679194,37.2691513590052));
#66945=CARTESIAN_POINT('Ctrl Pts',(31.4687569202096,19.0367269533429,37.2734046336302));
#66946=CARTESIAN_POINT('Ctrl Pts',(31.5337061518539,19.0870393434789,37.2776579082552));
#66947=CARTESIAN_POINT('Ctrl Pts',(31.5959262161907,19.1404382875324,37.2819111828801));
#66948=CARTESIAN_POINT('Ctrl Pts',(31.6576903850589,19.1934459697497,37.2861332931428));
#66949=CARTESIAN_POINT('Ctrl Pts',(31.7167649504446,19.2494947557925,37.2903554034055));
#66950=CARTESIAN_POINT('Ctrl Pts',(31.772851223516,19.3082704739593,37.2945775136681));
#66951=CARTESIAN_POINT('Ctrl Pts',(31.8295584750173,19.3676969476709,37.2988463704743));
#66952=CARTESIAN_POINT('Ctrl Pts',(31.8832105353156,19.4299107406748,37.3031152272804));
#66953=CARTESIAN_POINT('Ctrl Pts',(31.9335414607419,19.4945539964541,37.3073840840866));
#66954=CARTESIAN_POINT('Ctrl Pts',(31.9838723861681,19.5591972522335,37.3116529408927));
#66955=CARTESIAN_POINT('Ctrl Pts',(32.030881951721,19.6262695372291,37.3159217976988));
#66956=CARTESIAN_POINT('Ctrl Pts',(32.0743510604301,19.695385908365,37.320190654505));
#66957=CARTESIAN_POINT('Ctrl Pts',(32.1174346839632,19.763889353741,37.324421654979));
#66958=CARTESIAN_POINT('Ctrl Pts',(32.1572021458296,19.8346578788659,37.328652655453));
#66959=CARTESIAN_POINT('Ctrl Pts',(32.1934078163849,19.9073370139783,37.332883655927));
#66960=CARTESIAN_POINT('Ctrl Pts',(32.229561531102,19.979911853125,37.3371085848334));
#66961=CARTESIAN_POINT('Ctrl Pts',(32.2621634001933,20.0543914442578,37.3413335137398));
#66962=CARTESIAN_POINT('Ctrl Pts',(32.2910117400239,20.1303935044674,37.3455584426463));
#66963=CARTESIAN_POINT('Ctrl Pts',(32.3199462802455,20.2066226629204,37.3497959958675));
#66964=CARTESIAN_POINT('Ctrl Pts',(32.3451045767018,20.2843830005105,37.3540335490887));
#66965=CARTESIAN_POINT('Ctrl Pts',(32.3663302640897,20.3632651012758,37.3582711023099));
#66966=CARTESIAN_POINT('Ctrl Pts',(32.3874545993782,20.4417705420834,37.3624884213259));
#66967=CARTESIAN_POINT('Ctrl Pts',(32.4046836691473,20.5213866067705,37.3667057403418));
#66968=CARTESIAN_POINT('Ctrl Pts',(32.4179126465887,20.6016927273245,37.3709230593578));
#66969=CARTESIAN_POINT('Ctrl Pts',(32.4311372489152,20.681972288871,37.3751389836133));
#66970=CARTESIAN_POINT('Ctrl Pts',(32.4403643105116,20.7629409946457,37.3793549078687));
#66971=CARTESIAN_POINT('Ctrl Pts',(32.4455401815834,20.8441684555014,37.3835708321242));
#66972=CARTESIAN_POINT('Ctrl Pts',(32.4507159269834,20.925393944127,37.3877866540155));
#66973=CARTESIAN_POINT('Ctrl Pts',(32.4518406489614,21.0068777112335,37.3920024759069));
#66974=CARTESIAN_POINT('Ctrl Pts',(32.4489127114645,21.0881860625473,37.3962182977983));
#66975=CARTESIAN_POINT('Ctrl Pts',(32.4459586395247,21.170220163118,37.4004717496447));
#66976=CARTESIAN_POINT('Ctrl Pts',(32.4388791979954,21.2520752191937,37.4047252014912));
#66977=CARTESIAN_POINT('Ctrl Pts',(32.4277262971736,21.3333095798381,37.4089786533376));
#66978=CARTESIAN_POINT('Ctrl Pts',(32.4166559868236,21.4139423764337,37.413200607137));
#66979=CARTESIAN_POINT('Ctrl Pts',(32.4015724942055,21.4939631896608,37.4174225609363));
#66980=CARTESIAN_POINT('Ctrl Pts',(32.3825779496656,21.5729507516071,37.4216445147357));
#66981=CARTESIAN_POINT('Ctrl Pts',(32.3633708408417,21.6528222481231,37.4259137156057));
#66982=CARTESIAN_POINT('Ctrl Pts',(32.3401647367117,21.7316367547278,37.4301829164756));
#66983=CARTESIAN_POINT('Ctrl Pts',(32.313116285293,21.808976699734,37.4344521173456));
#66984=CARTESIAN_POINT('Ctrl Pts',(32.2860678338742,21.8863166447401,37.4387213182155));
#66985=CARTESIAN_POINT('Ctrl Pts',(32.2551772777423,21.9621816037963,37.4429905190855));
#66986=CARTESIAN_POINT('Ctrl Pts',(32.2206494406737,22.0361787064187,37.4472597199555));
#66987=CARTESIAN_POINT('Ctrl Pts',(32.1864298465991,22.1095152090616,37.4514908080628));
#66988=CARTESIAN_POINT('Ctrl Pts',(32.1485092525824,22.1812923581581,37.4557218961701));
#66989=CARTESIAN_POINT('Ctrl Pts',(32.1070524450565,22.2511116032479,37.4599529842774));
#66990=CARTESIAN_POINT('Ctrl Pts',(32.0656551156771,22.3208306785576,37.4641780020361));
#66991=CARTESIAN_POINT('Ctrl Pts',(32.0207318843165,22.3885970323327,37.4684030197947));
#66992=CARTESIAN_POINT('Ctrl Pts',(31.9724947283962,22.4540339736228,37.4726280375533));
#66993=CARTESIAN_POINT('Ctrl Pts',(31.9241147065866,22.5196647220855,37.4768655687138));
#66994=CARTESIAN_POINT('Ctrl Pts',(31.8724013039645,22.5829518120537,37.4811030998743));
#66995=CARTESIAN_POINT('Ctrl Pts',(31.8176138401004,22.6435419612154,37.4853406310349));
#66996=CARTESIAN_POINT('Ctrl Pts',(31.7630865224159,22.703844411427,37.489558041214));
#66997=CARTESIAN_POINT('Ctrl Pts',(31.7055145802611,22.7614751231916,37.4937754513931));
#66998=CARTESIAN_POINT('Ctrl Pts',(31.645194657271,22.8161180549973,37.4979928615722));
#66999=CARTESIAN_POINT('Ctrl Pts',(31.5848946734435,22.8707429242086,37.5022088776575));
#67000=CARTESIAN_POINT('Ctrl Pts',(31.5218488569751,22.9223816628367,37.5064248937429));
#67001=CARTESIAN_POINT('Ctrl Pts',(31.4563898413395,22.970755915897,37.5106409098283));
#67002=CARTESIAN_POINT('Ctrl Pts',(31.3909324066066,23.0191290006693,37.5148568240925));
#67003=CARTESIAN_POINT('Ctrl Pts',(31.32306226317,23.0642374811803,37.5190727383567));
#67004=CARTESIAN_POINT('Ctrl Pts',(31.2531430119955,23.1058449234184,37.5232886526209));
#67005=CARTESIAN_POINT('Ctrl Pts',(31.1826029970165,23.1478217688422,37.5275419970197));
#67006=CARTESIAN_POINT('Ctrl Pts',(31.1099777121315,23.1862348383738,37.5317953414184));
#67007=CARTESIAN_POINT('Ctrl Pts',(31.0356664090088,23.2208884121565,37.5360486858172));
#67008=CARTESIAN_POINT('Ctrl Pts',(30.9619019186093,23.2552869908812,37.5402707323819));
#67009=CARTESIAN_POINT('Ctrl Pts',(30.8864765989373,23.2859810985366,37.5444927789466));
#67010=CARTESIAN_POINT('Ctrl Pts',(30.8097998461114,23.3128282381617,37.5487148255113));
#67011=CARTESIAN_POINT('Ctrl Pts',(30.7322704915026,23.3399739026755,37.5529838188271));
#67012=CARTESIAN_POINT('Ctrl Pts',(30.653462169298,23.3631863789658,37.5572528121428));
#67013=CARTESIAN_POINT('Ctrl Pts',(30.5738106252478,23.3823710072851,37.5615218054586));
#67014=CARTESIAN_POINT('Ctrl Pts',(30.4941590811977,23.4015556356044,37.5657907987744));
#67015=CARTESIAN_POINT('Ctrl Pts',(30.4136648031984,23.4167123898188,37.5700597920902));
#67016=CARTESIAN_POINT('Ctrl Pts',(30.3327688885244,23.4278004689081,37.574328785406));
#67017=CARTESIAN_POINT('Ctrl Pts',(30.2525914914025,23.4387900636737,37.5785598615211));
#67018=CARTESIAN_POINT('Ctrl Pts',(30.1717186653201,23.4458242593714,37.5827909376363));
#67019=CARTESIAN_POINT('Ctrl Pts',(30.0905746568081,23.4488255310544,37.5870220137514));
#67020=CARTESIAN_POINT('Ctrl Pts',(30.0095470655888,23.4518224968136,37.5912470195425));
#67021=CARTESIAN_POINT('Ctrl Pts',(29.9282495253672,23.4507980129853,37.5954720253336));
#67022=CARTESIAN_POINT('Ctrl Pts',(29.8471134892017,23.4457260608694,37.5996970311247));
#67023=CARTESIAN_POINT('Ctrl Pts',(29.7657368612176,23.4406390689483,37.6039345652802));
#67024=CARTESIAN_POINT('Ctrl Pts',(29.6845231655729,23.4314805080844,37.6081720994357));
#67025=CARTESIAN_POINT('Ctrl Pts',(29.6039098464817,23.4182768328473,37.6124096335912));
#67026=CARTESIAN_POINT('Ctrl Pts',(29.5236795834133,23.4051358984497,37.6166270319552));
#67027=CARTESIAN_POINT('Ctrl Pts',(29.4440444673046,23.3879882755164,37.6208444303193));
#67028=CARTESIAN_POINT('Ctrl Pts',(29.3654308702183,23.3669119691125,37.6250618286833));
#67029=CARTESIAN_POINT('Ctrl Pts',(29.2868432578898,23.3458426292225,37.6292778330382));
#67030=CARTESIAN_POINT('Ctrl Pts',(29.2092769428068,23.3208473049538,37.6334938373931));
#67031=CARTESIAN_POINT('Ctrl Pts',(29.1331461317234,23.2920546723527,37.637709841748));
#67032=CARTESIAN_POINT('Ctrl Pts',(29.0570171574561,23.2632627344345,37.6419257443829));
#67033=CARTESIAN_POINT('Ctrl Pts',(28.9823240528332,23.2306738358525,37.6461416470178));
#67034=CARTESIAN_POINT('Ctrl Pts',(28.9094625786465,23.1944653979108,37.6503575496527));
#67035=CARTESIAN_POINT('Ctrl Pts',(28.8359537734017,23.1579352694363,37.6546109080863));
#67036=CARTESIAN_POINT('Ctrl Pts',(28.7643097455512,23.1177211641151,37.65886426652));
#67037=CARTESIAN_POINT('Ctrl Pts',(28.6949113690655,23.074052534389,37.6631176249536));
#67038=CARTESIAN_POINT('Ctrl Pts',(28.6260240650023,23.0307054947852,37.6673396602597));
#67039=CARTESIAN_POINT('Ctrl Pts',(28.5593497956466,22.9839549628578,37.6715616955658));
#67040=CARTESIAN_POINT('Ctrl Pts',(28.4952301982313,22.9340677582972,37.6757837308719));
#67041=CARTESIAN_POINT('Ctrl Pts',(28.4303970493476,22.8836253866816,37.6800527508694));
#67042=CARTESIAN_POINT('Ctrl Pts',(28.3681761538577,22.8299764158856,37.6843217708668));
#67043=CARTESIAN_POINT('Ctrl Pts',(28.3088832363183,22.7734357449862,37.6885907908642));
#67044=CARTESIAN_POINT('Ctrl Pts',(28.2495903187789,22.7168950740868,37.6928598108616));
#67045=CARTESIAN_POINT('Ctrl Pts',(28.1932256655969,22.6574630989647,37.697128830859));
#67046=CARTESIAN_POINT('Ctrl Pts',(28.1400626378422,22.5954884076199,37.7013978508565));
#67047=CARTESIAN_POINT('Ctrl Pts',(28.0877693370062,22.5345275986595,37.70559703131));
#67048=CARTESIAN_POINT('Ctrl Pts',(28.0383698377252,22.4708688955375,37.7097962117636));
#67049=CARTESIAN_POINT('Ctrl Pts',(27.9921578849601,22.4048203767998,37.7139953922172));
#67050=CARTESIAN_POINT('Ctrl Pts',(27.9460081015478,22.3388607137244,37.7181889234758));
#67051=CARTESIAN_POINT('Ctrl Pts',(27.9030376245187,22.2705179968799,37.7223824547344));
#67052=CARTESIAN_POINT('Ctrl Pts',(27.8635012387214,22.2001346978798,37.726575985993));
#67053=CARTESIAN_POINT('Ctrl Pts',(27.8240054789372,22.1298237219504,37.7307652081461));
#67054=CARTESIAN_POINT('Ctrl Pts',(27.7879370364907,22.0574767349971,37.7349544302993));
#67055=CARTESIAN_POINT('Ctrl Pts',(27.7555076055583,21.9834653737135,37.7391436524524));
#67056=CARTESIAN_POINT('Ctrl Pts',(27.7216214270493,21.9061293820526,37.7435210567304));
#67057=CARTESIAN_POINT('Ctrl Pts',(27.6917091889156,21.8269764095386,37.7478984610083));
#67058=CARTESIAN_POINT('Ctrl Pts',(27.665958510845,21.7464586906875,37.7522758652863));
#67059=CARTESIAN_POINT('Ctrl Pts',(27.6413376838498,21.6694738120588,37.7564612041391));
#67060=CARTESIAN_POINT('Ctrl Pts',(27.6205210305988,21.5912419318454,37.7606465429919));
#67061=CARTESIAN_POINT('Ctrl Pts',(27.603622382931,21.5121763040309,37.7648318818448));
#67062=CARTESIAN_POINT('Ctrl Pts',(27.586725155894,21.4331173230834,37.7690168688457));
#67063=CARTESIAN_POINT('Ctrl Pts',(27.5737453711307,21.3532251972858,37.7732018558466));
#67064=CARTESIAN_POINT('Ctrl Pts',(27.5647458291997,21.2729237505235,37.7773868428476));
#67065=CARTESIAN_POINT('Ctrl Pts',(27.5557418328296,21.1925825575264,37.7815739012617));
#67066=CARTESIAN_POINT('Ctrl Pts',(27.550722051835,21.111832109761,37.7857609596758));
#67067=CARTESIAN_POINT('Ctrl Pts',(27.5496973641803,21.0311005288507,37.7899480180899));
#67068=CARTESIAN_POINT('Ctrl Pts',(27.5495566879162,21.0200171346639,37.790522846656));
#67069=CARTESIAN_POINT('Ctrl Pts',(27.5494912296765,21.0089340952719,37.791097675222));
#67070=CARTESIAN_POINT('Ctrl Pts',(27.5495009409688,20.9978525161318,37.791672503788));
#67071=CARTESIAN_POINT('',(27.5495000018184,21.000094404414,38.5916725038344));
#67072=CARTESIAN_POINT('Ctrl Pts',(27.5495009409694,20.9978525154208,37.7916725038249));
#67073=CARTESIAN_POINT('Ctrl Pts',(27.5495877392395,20.8988068312588,37.7968102452855));
#67074=CARTESIAN_POINT('Ctrl Pts',(27.5556832349185,20.800025431165,37.8019479867462));
#67075=CARTESIAN_POINT('Ctrl Pts',(27.5676691624476,20.7021460984115,37.8070857282068));
#67076=CARTESIAN_POINT('Ctrl Pts',(27.5798394239549,20.6027614598102,37.8123024840216));
#67077=CARTESIAN_POINT('Ctrl Pts',(27.5980826296213,20.5043067985095,37.8175192398364));
#67078=CARTESIAN_POINT('Ctrl Pts',(27.6222262848908,20.4074272958228,37.8227359956512));
#67079=CARTESIAN_POINT('Ctrl Pts',(27.6310673716759,20.3719513050752,37.8246463025364));
#67080=CARTESIAN_POINT('Ctrl Pts',(27.6406992042418,20.3366863206436,37.8265566094216));
#67081=CARTESIAN_POINT('Ctrl Pts',(27.6511117280305,20.3016633077059,37.8284669163068));
#67082=CARTESIAN_POINT('Ctrl Pts',(27.6741740636527,20.2240920583861,37.8326979883718));
#67083=CARTESIAN_POINT('Ctrl Pts',(27.7011264532798,20.1475189097962,37.8369290604367));
#67084=CARTESIAN_POINT('Ctrl Pts',(27.7318645173868,20.0723623107533,37.8411601325017));
#67085=CARTESIAN_POINT('Ctrl Pts',(27.7625584804569,19.9973135416613,37.8453851340911));
#67086=CARTESIAN_POINT('Ctrl Pts',(27.7970271562525,19.9236777123993,37.8496101356806));
#67087=CARTESIAN_POINT('Ctrl Pts',(27.8351162725447,19.8518585903298,37.85383513727));
#67088=CARTESIAN_POINT('Ctrl Pts',(27.873318381375,19.7798264146199,37.858072672457));
#67089=CARTESIAN_POINT('Ctrl Pts',(27.9151623051707,19.709622193279,37.862310207644));
#67090=CARTESIAN_POINT('Ctrl Pts',(27.9604434986149,19.6416335076064,37.8665477428309));
#67091=CARTESIAN_POINT('Ctrl Pts',(28.0055094667055,19.5739679779242,37.8707651366537));
#67092=CARTESIAN_POINT('Ctrl Pts',(28.0539798483688,19.5084973634363,37.8749825304765));
#67093=CARTESIAN_POINT('Ctrl Pts',(28.1056077059987,19.4455778930971,37.8791999242993));
#67094=CARTESIAN_POINT('Ctrl Pts',(28.1572184972102,19.3826792218004,37.8834159239947));
#67095=CARTESIAN_POINT('Ctrl Pts',(28.2119843969412,19.3223303791028,37.8876319236902));
#67096=CARTESIAN_POINT('Ctrl Pts',(28.269617326673,19.2648556100861,37.8918479233856));
#67097=CARTESIAN_POINT('Ctrl Pts',(28.3272488643532,19.2073822293007,37.8960638212488));
#67098=CARTESIAN_POINT('Ctrl Pts',(28.3877469643417,19.1527831117174,37.9002797191121));
#67099=CARTESIAN_POINT('Ctrl Pts',(28.4507867522404,19.1013455914869,37.9044956169753));
#67100=CARTESIAN_POINT('Ctrl Pts',(28.5143867625375,19.0494509559661,37.9087489807071));
#67101=CARTESIAN_POINT('Ctrl Pts',(28.5805734995497,19.0007747090515,37.913002344439));
#67102=CARTESIAN_POINT('Ctrl Pts',(28.6489808289029,18.9555691624982,37.9172557081708));
#67103=CARTESIAN_POINT('Ctrl Pts',(28.7168842192202,18.9106966334704,37.9214777384763));
#67104=CARTESIAN_POINT('Ctrl Pts',(28.7869751575657,18.8692440248076,37.9256997687818));
#67105=CARTESIAN_POINT('Ctrl Pts',(28.8588696574109,18.8314124893788,37.9299217990873));
#67106=CARTESIAN_POINT('Ctrl Pts',(28.9315644953121,18.7931598088333,37.9341908295323));
#67107=CARTESIAN_POINT('Ctrl Pts',(29.0061028556114,18.758609527363,37.9384598599774));
#67108=CARTESIAN_POINT('Ctrl Pts',(29.0820676379718,18.7279193613031,37.9427288904224));
#67109=CARTESIAN_POINT('Ctrl Pts',(29.1580324203322,18.6972291952432,37.9469979208675));
#67110=CARTESIAN_POINT('Ctrl Pts',(29.2354231459706,18.6703992421989,37.9512669513125));
#67111=CARTESIAN_POINT('Ctrl Pts',(29.3138095002204,18.6475347296905,37.9555359817575));
#67112=CARTESIAN_POINT('Ctrl Pts',(29.3914988350456,18.62487353075,37.9597670515502));
#67113=CARTESIAN_POINT('Ctrl Pts',(29.4704577320105,18.6060224369706,37.9639981213429));
#67114=CARTESIAN_POINT('Ctrl Pts',(29.5502779601612,18.5911205225493,37.9682291911355));
#67115=CARTESIAN_POINT('Ctrl Pts',(29.6299836670217,18.5762399885036,37.9724541904423));
#67116=CARTESIAN_POINT('Ctrl Pts',(29.7105477975081,18.5652974652656,37.976679189749));
#67117=CARTESIAN_POINT('Ctrl Pts',(29.7915474176048,18.5583821406918,37.9809041890557));
#67118=CARTESIAN_POINT('Ctrl Pts',(29.8727873803813,18.5514462969151,37.9851417248121));
#67119=CARTESIAN_POINT('Ctrl Pts',(29.9544649660325,18.5485617158995,37.9893792605684));
#67120=CARTESIAN_POINT('Ctrl Pts',(30.0361435948961,18.5497665640703,37.9936167963248));
#67121=CARTESIAN_POINT('Ctrl Pts',(30.1174339432304,18.5509656846831,37.9978341878568));
#67122=CARTESIAN_POINT('Ctrl Pts',(30.1987248564328,18.5562154411305,38.0020515793887));
#67123=CARTESIAN_POINT('Ctrl Pts',(30.2795831278049,18.56550138126,38.0062689709207));
#67124=CARTESIAN_POINT('Ctrl Pts',(30.3604146702023,18.5747842517759,38.0104849683275));
#67125=CARTESIAN_POINT('Ctrl Pts',(30.4408133932167,18.5881006033968,38.0147009657343));
#67126=CARTESIAN_POINT('Ctrl Pts',(30.5203506711986,18.6053840748498,38.0189169631411));
#67127=CARTESIAN_POINT('Ctrl Pts',(30.5998860281561,18.6226671288636,38.023132858721));
#67128=CARTESIAN_POINT('Ctrl Pts',(30.6785595273242,18.6439170123943,38.0273487543009));
#67129=CARTESIAN_POINT('Ctrl Pts',(30.7559536196955,18.6690164361649,38.0315646498808));
#67130=CARTESIAN_POINT('Ctrl Pts',(30.8340355904679,18.6943389435194,38.0358180163248));
#67131=CARTESIAN_POINT('Ctrl Pts',(30.9108148351232,18.7235796304054,38.0400713827687));
#67132=CARTESIAN_POINT('Ctrl Pts',(30.9858808732983,18.7565675509023,38.0443247492126));
#67133=CARTESIAN_POINT('Ctrl Pts',(31.0603938322985,18.7893124196505,38.0485467772715));
#67134=CARTESIAN_POINT('Ctrl Pts',(31.1332183541381,18.8257492212204,38.0527688053305));
#67135=CARTESIAN_POINT('Ctrl Pts',(31.2039772776005,18.8656642801514,38.0569908333894));
#67136=CARTESIAN_POINT('Ctrl Pts',(31.275524022823,18.9060237487828,38.0612598690258));
#67137=CARTESIAN_POINT('Ctrl Pts',(31.344958475327,18.9499391472324,38.0655289046623));
#67138=CARTESIAN_POINT('Ctrl Pts',(31.411922028399,18.9971454282146,38.0697979402987));
#67139=CARTESIAN_POINT('Ctrl Pts',(31.4788855814709,19.0443517091968,38.0740669759351));
#67140=CARTESIAN_POINT('Ctrl Pts',(31.5433778935879,19.0948485232448,38.0783360115715));
#67141=CARTESIAN_POINT('Ctrl Pts',(31.6050773073057,19.1483312694836,38.0826050472079));
#67142=CARTESIAN_POINT('Ctrl Pts',(31.6662279866382,19.2013383576875,38.0868361154391));
#67143=CARTESIAN_POINT('Ctrl Pts',(31.7248647884748,19.2574773912429,38.0910671836702));
#67144=CARTESIAN_POINT('Ctrl Pts',(31.780649581212,19.3164806746195,38.0952982519014));
#67145=CARTESIAN_POINT('Ctrl Pts',(31.8363543367703,19.3753993030908,38.0995232496114));
#67146=CARTESIAN_POINT('Ctrl Pts',(31.8892148933253,19.4371736846638,38.1037482473214));
#67147=CARTESIAN_POINT('Ctrl Pts',(31.9389270742472,19.5014967298163,38.1079732450314));
#67148=CARTESIAN_POINT('Ctrl Pts',(31.9887867850132,19.5660106651823,38.1122107811825));
#67149=CARTESIAN_POINT('Ctrl Pts',(32.0354790502061,19.6330881017077,38.1164483173336));
#67150=CARTESIAN_POINT('Ctrl Pts',(32.0787351748207,19.7023828288115,38.1206858534848));
#67151=CARTESIAN_POINT('Ctrl Pts',(32.1217856491692,19.7713481117223,38.1249032433457));
#67152=CARTESIAN_POINT('Ctrl Pts',(32.1614323284732,19.8425092556063,38.1291206332067));
#67153=CARTESIAN_POINT('Ctrl Pts',(32.1974525662052,19.9154943664148,38.1333380230677));
#67154=CARTESIAN_POINT('Ctrl Pts',(32.2334608966685,19.988455350416,38.1375540187793));
#67155=CARTESIAN_POINT('Ctrl Pts',(32.2658449605813,20.0632386873489,38.1417700144908));
#67156=CARTESIAN_POINT('Ctrl Pts',(32.2944282180476,20.1394481989869,38.1459860102023));
#67157=CARTESIAN_POINT('Ctrl Pts',(32.3230107850069,20.2156558695752,38.1502019040649));
#67158=CARTESIAN_POINT('Ctrl Pts',(32.347792565828,20.2932892106309,38.1544177979275));
#67159=CARTESIAN_POINT('Ctrl Pts',(32.3686458232528,20.3719337503202,38.1586336917901));
#67160=CARTESIAN_POINT('Ctrl Pts',(32.3896844426245,20.4512773512972,38.1628870601958));
#67161=CARTESIAN_POINT('Ctrl Pts',(32.4067242093454,20.5316497569512,38.1671404286015));
#67162=CARTESIAN_POINT('Ctrl Pts',(32.4196863094521,20.6126133535473,38.1713937970072));
#67163=CARTESIAN_POINT('Ctrl Pts',(32.4325528948016,20.6929803478788,38.1756158233119));
#67164=CARTESIAN_POINT('Ctrl Pts',(32.4414017193707,20.7739293757007,38.1798378496166));
#67165=CARTESIAN_POINT('Ctrl Pts',(32.4462079373079,20.855027666598,38.1840598759212));
#67166=CARTESIAN_POINT('Ctrl Pts',(32.4510676734933,20.9370290040333,38.1883289153775));
#67167=CARTESIAN_POINT('Ctrl Pts',(32.4517942096248,21.0191824609694,38.1925979548337));
#67168=CARTESIAN_POINT('Ctrl Pts',(32.4484159285209,21.1010430154209,38.1968669942899));
#67169=CARTESIAN_POINT('Ctrl Pts',(32.445037647417,21.1829035698723,38.2011360337461));
#67170=CARTESIAN_POINT('Ctrl Pts',(32.4375546576655,21.2644707454179,38.2054050732023));
#67171=CARTESIAN_POINT('Ctrl Pts',(32.426048608691,21.345309134354,38.2096741126585));
#67172=CARTESIAN_POINT('Ctrl Pts',(32.4146448971588,21.4254285280921,38.2139051822973));
#67173=CARTESIAN_POINT('Ctrl Pts',(32.3992466487324,21.5051327585229,38.2181362519361));
#67174=CARTESIAN_POINT('Ctrl Pts',(32.3798955692347,21.5839925766113,38.2223673215748));
#67175=CARTESIAN_POINT('Ctrl Pts',(32.3605722535719,21.6627392510907,38.2265923207141));
#67176=CARTESIAN_POINT('Ctrl Pts',(32.3373074803006,21.7406434716311,38.2308173198533));
#67177=CARTESIAN_POINT('Ctrl Pts',(32.3101944645759,21.8172831735957,38.2350423189926));
#67178=CARTESIAN_POINT('Ctrl Pts',(32.283000997572,21.8941502852344,38.2392798547891));
#67179=CARTESIAN_POINT('Ctrl Pts',(32.2519364864172,21.969744894976,38.2435173905856));
#67180=CARTESIAN_POINT('Ctrl Pts',(32.2171462534557,22.0436535540051,38.2477549263821));
#67181=CARTESIAN_POINT('Ctrl Pts',(32.1825214068497,22.1172108648909,38.2519723177145));
#67182=CARTESIAN_POINT('Ctrl Pts',(32.1442063752251,22.1890977918698,38.2561897090468));
#67183=CARTESIAN_POINT('Ctrl Pts',(32.1023930227776,22.2589256641185,38.2604071003791));
#67184=CARTESIAN_POINT('Ctrl Pts',(32.0605934925087,22.3287304534697,38.2646230975746));
#67185=CARTESIAN_POINT('Ctrl Pts',(32.0152981766068,22.3964771411798,38.2688390947701));
#67186=CARTESIAN_POINT('Ctrl Pts',(31.9667443365176,22.4618026422112,38.2730550919655));
#67187=CARTESIAN_POINT('Ctrl Pts',(31.9181916692574,22.5271265652905,38.2772709873226));
#67188=CARTESIAN_POINT('Ctrl Pts',(31.8663809125555,22.5900290454566,38.2814868826797));
#67189=CARTESIAN_POINT('Ctrl Pts',(31.811591151904,22.650178095947,38.2857027780368));
#67190=CARTESIAN_POINT('Ctrl Pts',(31.7563144141723,22.710861757442,38.2899561447095));
#67191=CARTESIAN_POINT('Ctrl Pts',(31.6980057637354,22.7687424318833,38.2942095113822));
#67192=CARTESIAN_POINT('Ctrl Pts',(31.6369902492213,22.8235167051482,38.2984628780549));
#67193=CARTESIAN_POINT('Ctrl Pts',(31.5764242978359,22.8778874008334,38.3026849058649));
#67194=CARTESIAN_POINT('Ctrl Pts',(31.5131916421712,22.9291970715396,38.3069069336749));
#67195=CARTESIAN_POINT('Ctrl Pts',(31.4476425112592,22.9771902815852,38.3111289614849));
#67196=CARTESIAN_POINT('Ctrl Pts',(31.3813635526542,23.0257178507182,38.3153979975889));
#67197=CARTESIAN_POINT('Ctrl Pts',(31.3127166233379,23.070854381438,38.3196670336929));
#67198=CARTESIAN_POINT('Ctrl Pts',(31.2420910962522,23.1123825313165,38.3239360697969));
#67199=CARTESIAN_POINT('Ctrl Pts',(31.1714655691666,23.1539106811949,38.3282051059009));
#67200=CARTESIAN_POINT('Ctrl Pts',(31.0988619035401,23.1918302832754,38.3324741420049));
#67201=CARTESIAN_POINT('Ctrl Pts',(31.0246902622514,23.2259739702987,38.3367431781089));
#67202=CARTESIAN_POINT('Ctrl Pts',(30.9511782693252,23.2598139991199,38.3409742473751));
#67203=CARTESIAN_POINT('Ctrl Pts',(30.8758501925449,23.2900720565571,38.3452053166413));
#67204=CARTESIAN_POINT('Ctrl Pts',(30.7990893713817,23.3165505447852,38.3494363859075));
#67205=CARTESIAN_POINT('Ctrl Pts',(30.7224386823683,23.3429910431536,38.3536613846712));
#67206=CARTESIAN_POINT('Ctrl Pts',(30.644359767411,23.3656625918616,38.3578863834349));
#67207=CARTESIAN_POINT('Ctrl Pts',(30.5652578456333,23.3844147747298,38.3621113821986));
#67208=CARTESIAN_POINT('Ctrl Pts',(30.4859211993408,23.4032226022263,38.3663489180886));
#67209=CARTESIAN_POINT('Ctrl Pts',(30.4055558968884,23.4180875738996,38.3705864539787));
#67210=CARTESIAN_POINT('Ctrl Pts',(30.324588158273,23.4289077334285,38.3748239898687));
#67211=CARTESIAN_POINT('Ctrl Pts',(30.2440053344,23.4396764547057,38.3790413808212));
#67212=CARTESIAN_POINT('Ctrl Pts',(30.1628262527814,23.4464386664054,38.3832587717737));
#67213=CARTESIAN_POINT('Ctrl Pts',(30.0814815351787,23.4491449547597,38.3874761627262));
#67214=CARTESIAN_POINT('Ctrl Pts',(30.0001637075973,23.4518503484996,38.3916921595411));
#67215=CARTESIAN_POINT('Ctrl Pts',(29.9186808171045,23.4505024659984,38.395908156356));
#67216=CARTESIAN_POINT('Ctrl Pts',(29.8374665881496,23.4451039119089,38.4001241531708));
#67217=CARTESIAN_POINT('Ctrl Pts',(29.7562543209474,23.439705488223,38.4043400481471));
#67218=CARTESIAN_POINT('Ctrl Pts',(29.6753111662452,23.4302566194287,38.4085559431233));
#67219=CARTESIAN_POINT('Ctrl Pts',(29.5950673819249,23.4168119134138,38.4127718380996));
#67220=CARTESIAN_POINT('Ctrl Pts',(29.514110366661,23.4032477067991,38.4170252052213));
#67221=CARTESIAN_POINT('Ctrl Pts',(29.4338656936714,23.3856163381214,38.4212785723429));
#67222=CARTESIAN_POINT('Ctrl Pts',(29.35476452036,23.3640265281535,38.4255319394645));
#67223=CARTESIAN_POINT('Ctrl Pts',(29.2762461808626,23.3425957963733,38.4297539668971));
#67224=CARTESIAN_POINT('Ctrl Pts',(29.1988549730422,23.3172649678906,38.4339759943296));
#67225=CARTESIAN_POINT('Ctrl Pts',(29.1229953809785,23.2881899283528,38.4381980217621));
#67226=CARTESIAN_POINT('Ctrl Pts',(29.0462911416199,23.2587911571308,38.4424670587283));
#67227=CARTESIAN_POINT('Ctrl Pts',(28.971153283341,23.2255644764019,38.4467360956945));
#67228=CARTESIAN_POINT('Ctrl Pts',(28.8979754928976,23.1887193140615,38.4510051326607));
#67229=CARTESIAN_POINT('Ctrl Pts',(28.8247977024543,23.1518741517211,38.4552741696269));
#67230=CARTESIAN_POINT('Ctrl Pts',(28.7535803690505,23.1114108032114,38.4595432065931));
#67231=CARTESIAN_POINT('Ctrl Pts',(28.6846864487342,23.0675832539118,38.4638122435594));
#67232=CARTESIAN_POINT('Ctrl Pts',(28.6164052553478,23.0241454969133,38.4680433126773));
#67233=CARTESIAN_POINT('Ctrl Pts',(28.5501500146718,22.97724014817,38.4722743817952));
#67234=CARTESIAN_POINT('Ctrl Pts',(28.4862945500099,22.9270822661916,38.4765054509131));
#67235=CARTESIAN_POINT('Ctrl Pts',(28.4225307016716,22.8769963479953,38.4807304495248));
#67236=CARTESIAN_POINT('Ctrl Pts',(28.3611601537357,22.823667449454,38.4849554481365));
#67237=CARTESIAN_POINT('Ctrl Pts',(28.3025289370975,22.7673545882501,38.4891804467482));
#67238=CARTESIAN_POINT('Ctrl Pts',(28.2437237374235,22.7108746235286,38.4934179826757));
#67239=CARTESIAN_POINT('Ctrl Pts',(28.1876745481238,22.6513932170041,38.4976555186033));
#67240=CARTESIAN_POINT('Ctrl Pts',(28.1346980572471,22.5892132998318,38.5018930545309));
#67241=CARTESIAN_POINT('Ctrl Pts',(28.0819734152257,22.5273289843633,38.5061104453232));
#67242=CARTESIAN_POINT('Ctrl Pts',(28.0322926309513,22.4627721102107,38.5103278361156));
#67243=CARTESIAN_POINT('Ctrl Pts',(27.9859306220108,22.3958777849963,38.5145452269079));
#67244=CARTESIAN_POINT('Ctrl Pts',(27.9395839389319,22.329005572999,38.5187612235599));
#67245=CARTESIAN_POINT('Ctrl Pts',(27.8965541171862,22.2597978262391,38.5229772202119));
#67246=CARTESIAN_POINT('Ctrl Pts',(27.857074040336,22.1886204530455,38.5271932168639));
#67247=CARTESIAN_POINT('Ctrl Pts',(27.8175949171616,22.1174447992037,38.5314091116748));
#67248=CARTESIAN_POINT('Ctrl Pts',(27.7816655929627,22.0443000206626,38.5356250064857));
#67249=CARTESIAN_POINT('Ctrl Pts',(27.7494733695953,21.9695772975061,38.5398409012966));
#67250=CARTESIAN_POINT('Ctrl Pts',(27.7169950093346,21.8941904099764,38.544094268606));
#67251=CARTESIAN_POINT('Ctrl Pts',(27.6883207216346,21.817197821933,38.5483476359155));
#67252=CARTESIAN_POINT('Ctrl Pts',(27.6635928201128,21.7390207979288,38.5526010032249));
#67253=CARTESIAN_POINT('Ctrl Pts',(27.6390471209577,21.6614198049636,38.5568230304876));
#67254=CARTESIAN_POINT('Ctrl Pts',(27.6183899040228,21.5826522427068,38.5610450577502));
#67255=CARTESIAN_POINT('Ctrl Pts',(27.6017093895468,21.5031425223654,38.5652670850129));
#67256=CARTESIAN_POINT('Ctrl Pts',(27.5848431462474,21.4227475027822,38.5695361223457));
#67257=CARTESIAN_POINT('Ctrl Pts',(27.5720427878845,21.341594177903,38.5738051596785));
#67258=CARTESIAN_POINT('Ctrl Pts',(27.5633456864671,21.2601269043015,38.5780741970114));
#67259=CARTESIAN_POINT('Ctrl Pts',(27.5546485850497,21.1786596307001,38.5823432343442));
#67260=CARTESIAN_POINT('Ctrl Pts',(27.550054703235,21.0968788955847,38.5866122716771));
#67261=CARTESIAN_POINT('Ctrl Pts',(27.5495473118384,21.0152273793423,38.5908813090099));
#67262=CARTESIAN_POINT('Ctrl Pts',(27.5495159663311,21.0101831310155,38.5911450406026));
#67263=CARTESIAN_POINT('Ctrl Pts',(27.5495001961528,21.0051387858016,38.5914087721953));
#67264=CARTESIAN_POINT('Ctrl Pts',(27.5495000018185,21.0000944053028,38.5916725037879));
#67265=CARTESIAN_POINT('',(27.5495008920499,21.0020909174755,39.3916725037448));
#67266=CARTESIAN_POINT('Ctrl Pts',(27.5495000018184,21.000094404414,38.5916725038344));
#67267=CARTESIAN_POINT('Ctrl Pts',(27.5494968875853,20.9192567836295,38.5958988770199));
#67268=CARTESIAN_POINT('Ctrl Pts',(27.5534981084526,20.8382656888067,38.6001252502055));
#67269=CARTESIAN_POINT('Ctrl Pts',(27.5615232630837,20.7575511321572,38.604351623391));
#67270=CARTESIAN_POINT('Ctrl Pts',(27.5695369025683,20.6769523913385,38.6085719322315));
#67271=CARTESIAN_POINT('Ctrl Pts',(27.5815629634692,20.5966298605576,38.612792241072));
#67272=CARTESIAN_POINT('Ctrl Pts',(27.5975690364578,20.5170137523555,38.6170125499125));
#67273=CARTESIAN_POINT('Ctrl Pts',(27.6135565785834,20.437489818867,38.6212279727348));
#67274=CARTESIAN_POINT('Ctrl Pts',(27.6335148842582,20.3586711372262,38.625443395557));
#67275=CARTESIAN_POINT('Ctrl Pts',(27.657359896073,20.280981506863,38.6296588183792));
#67276=CARTESIAN_POINT('Ctrl Pts',(27.6811897786626,20.2033411691538,38.6338715665925));
#67277=CARTESIAN_POINT('Ctrl Pts',(27.7089013361122,20.1268289052043,38.6380843148059));
#67278=CARTESIAN_POINT('Ctrl Pts',(27.7403599824137,20.0518558965418,38.6422970630192));
#67279=CARTESIAN_POINT('Ctrl Pts',(27.7718083666841,19.9769073446006,38.6465084370045));
#67280=CARTESIAN_POINT('Ctrl Pts',(27.8070012323353,19.9034974803584,38.6507198109898));
#67281=CARTESIAN_POINT('Ctrl Pts',(27.8457554312733,19.8320185840041,38.6549311849751));
#67282=CARTESIAN_POINT('Ctrl Pts',(27.8845089350744,19.7605409697722,38.6591424834206));
#67283=CARTESIAN_POINT('Ctrl Pts',(27.9268234218982,19.6909946637565,38.6633537818662));
#67284=CARTESIAN_POINT('Ctrl Pts',(27.9724699464796,19.6237470682786,38.6675650803118));
#67285=CARTESIAN_POINT('Ctrl Pts',(28.0181616309772,19.5564329420889,38.6717805451618));
#67286=CARTESIAN_POINT('Ctrl Pts',(28.0671916763067,19.4914224562388,38.6759960100119));
#67287=CARTESIAN_POINT('Ctrl Pts',(28.1192882731924,19.4290532629499,38.6802114748619));
#67288=CARTESIAN_POINT('Ctrl Pts',(28.1714094082835,19.366654692923,38.6844289252532));
#67289=CARTESIAN_POINT('Ctrl Pts',(28.2265996556414,19.3069002367344,38.6886463756445));
#67290=CARTESIAN_POINT('Ctrl Pts',(28.2845491494127,19.250091822632,38.6928638260358));
#67291=CARTESIAN_POINT('Ctrl Pts',(28.3426040636323,19.1931800639085,38.6970889487204));
#67292=CARTESIAN_POINT('Ctrl Pts',(28.4034279052085,19.1392253670635,38.701314071405));
#67293=CARTESIAN_POINT('Ctrl Pts',(28.4666765370618,19.0884902804319,38.7055391940896));
#67294=CARTESIAN_POINT('Ctrl Pts',(28.5286069026978,19.038812645144,38.7096762542132));
#67295=CARTESIAN_POINT('Ctrl Pts',(28.5928615630646,18.9922218662125,38.7138133143368));
#67296=CARTESIAN_POINT('Ctrl Pts',(28.6590926403957,18.9489227944909,38.7179503744604));
#67297=CARTESIAN_POINT('Ctrl Pts',(28.7268287296149,18.904639809774,38.7221814436945));
#67298=CARTESIAN_POINT('Ctrl Pts',(28.7968879321114,18.8636327712722,38.7264125129286));
#67299=CARTESIAN_POINT('Ctrl Pts',(28.8689201357594,18.8261535034162,38.7306435821627));
#67300=CARTESIAN_POINT('Ctrl Pts',(28.9408489915871,18.7887280087401,38.7348685808928));
#67301=CARTESIAN_POINT('Ctrl Pts',(29.0147448175114,18.7548204451191,38.7390935796229));
#67302=CARTESIAN_POINT('Ctrl Pts',(29.0902289209727,18.7246391860266,38.7433185783529));
#67303=CARTESIAN_POINT('Ctrl Pts',(29.1659370143001,18.6943683677307,38.7475561142512));
#67304=CARTESIAN_POINT('Ctrl Pts',(29.2432424276188,18.667846257808,38.7517936501494));
#67305=CARTESIAN_POINT('Ctrl Pts',(29.3217385691692,18.6452363852294,38.7560311860477));
#67306=CARTESIAN_POINT('Ctrl Pts',(29.3998615449285,18.6227339985835,38.7602485769629));
#67307=CARTESIAN_POINT('Ctrl Pts',(29.4791635047628,18.6041068717068,38.7644659678782));
#67308=CARTESIAN_POINT('Ctrl Pts',(29.5592257759526,18.589467209637,38.7686833587934));
#67309=CARTESIAN_POINT('Ctrl Pts',(29.6392615810333,18.5748323869863,38.7728993555698));
#67310=CARTESIAN_POINT('Ctrl Pts',(29.7200567413363,18.5641824950953,38.7771153523461));
#67311=CARTESIAN_POINT('Ctrl Pts',(29.8011818652027,18.5575787424615,38.7813313491225));
#67312=CARTESIAN_POINT('Ctrl Pts',(29.8823050294451,18.5509751493452,38.785547244059));
#67313=CARTESIAN_POINT('Ctrl Pts',(29.9637576778849,18.5484175377863,38.7897631389955));
#67314=CARTESIAN_POINT('Ctrl Pts',(30.0451061999861,18.5499151686681,38.793979033932));
#67315=CARTESIAN_POINT('Ctrl Pts',(30.1271777738817,18.5514261109742,38.7982324010969));
#67316=CARTESIAN_POINT('Ctrl Pts',(30.2091428798303,18.5570647529042,38.8024857682618));
#67317=CARTESIAN_POINT('Ctrl Pts',(30.2905590595226,18.5667869631022,38.8067391354267));
#67318=CARTESIAN_POINT('Ctrl Pts',(30.3713753463214,18.5764375378486,38.8109611628168));
#67319=CARTESIAN_POINT('Ctrl Pts',(30.4516503165892,18.590111563357,38.815183190207));
#67320=CARTESIAN_POINT('Ctrl Pts',(30.5309609591426,18.6077143335575,38.8194052175971));
#67321=CARTESIAN_POINT('Ctrl Pts',(30.6111546766192,18.6255130997106,38.8236742546494));
#67322=CARTESIAN_POINT('Ctrl Pts',(30.6903619879445,18.6473285118998,38.8279432917017));
#67323=CARTESIAN_POINT('Ctrl Pts',(30.7681626877384,18.6730113160639,38.832212328754));
#67324=CARTESIAN_POINT('Ctrl Pts',(30.8459633875323,18.698694120228,38.8364813658063));
#67325=CARTESIAN_POINT('Ctrl Pts',(30.9223570473736,18.7282440813745,38.8407504028586));
#67326=CARTESIAN_POINT('Ctrl Pts',(30.9969473057037,18.7614633530697,38.8450194399109));
#67327=CARTESIAN_POINT('Ctrl Pts',(31.070874175486,18.7943871802268,38.8492505091326));
#67328=CARTESIAN_POINT('Ctrl Pts',(31.1433070747894,18.8310388393118,38.8534815783543));
#67329=CARTESIAN_POINT('Ctrl Pts',(31.2138446176822,18.8712605856696,38.857712647576));
#67330=CARTESIAN_POINT('Ctrl Pts',(31.2842809572046,18.9114246240873,38.8619376462933));
#67331=CARTESIAN_POINT('Ctrl Pts',(31.3528269406415,18.9551483484349,38.8661626450106));
#67332=CARTESIAN_POINT('Ctrl Pts',(31.4191022075216,19.0022264456132,38.8703876437279));
#67333=CARTESIAN_POINT('Ctrl Pts',(31.4855741384192,19.0494442414779,38.8746251796293));
#67334=CARTESIAN_POINT('Ctrl Pts',(31.5497614257093,19.1000361519305,38.8788627155307));
#67335=CARTESIAN_POINT('Ctrl Pts',(31.6113062747142,19.153749112643,38.8831002514321));
#67336=CARTESIAN_POINT('Ctrl Pts',(31.6725585430787,19.2072067250574,38.8873176423338));
#67337=CARTESIAN_POINT('Ctrl Pts',(31.7311930835111,19.2637554767435,38.8915350332354));
#67338=CARTESIAN_POINT('Ctrl Pts',(31.7868886856299,19.3231043338454,38.895752424137));
#67339=CARTESIAN_POINT('Ctrl Pts',(31.8425658765024,19.3824335720478,38.8999684208995));
#67340=CARTESIAN_POINT('Ctrl Pts',(31.8953057404331,19.4445607387253,38.9041844176619));
#67341=CARTESIAN_POINT('Ctrl Pts',(31.9448241143915,19.509158152559,38.9084004144243));
#67342=CARTESIAN_POINT('Ctrl Pts',(31.9943412922019,19.5737540060009,38.9126163093467));
#67343=CARTESIAN_POINT('Ctrl Pts',(32.0406368527598,19.6408196182743,38.916832204269));
#67344=CARTESIAN_POINT('Ctrl Pts',(32.0834680025975,19.7099956077004,38.9210480991913));
#67345=CARTESIAN_POINT('Ctrl Pts',(32.12667984976,19.7797864560367,38.9253014663722));
#67346=CARTESIAN_POINT('Ctrl Pts',(32.1663651249108,19.8517249844587,38.929554833553));
#67347=CARTESIAN_POINT('Ctrl Pts',(32.2023211093903,19.925415437886,38.9338082007338));
#67348=CARTESIAN_POINT('Ctrl Pts',(32.238012161756,19.9985629227956,38.9380302281092));
#67349=CARTESIAN_POINT('Ctrl Pts',(32.2700285698777,20.0734361449724,38.9422522554846));
#67350=CARTESIAN_POINT('Ctrl Pts',(32.2982206575318,20.1496282816944,38.94647428286));
#67351=CARTESIAN_POINT('Ctrl Pts',(32.3267266469434,20.22666877154,38.9507433199436));
#67352=CARTESIAN_POINT('Ctrl Pts',(32.3513224783992,20.3050572627901,38.9550123570271));
#67353=CARTESIAN_POINT('Ctrl Pts',(32.3719058378373,20.3843597264366,38.9592813941107));
#67354=CARTESIAN_POINT('Ctrl Pts',(32.3924891972755,20.4636621900832,38.9635504311943));
#67355=CARTESIAN_POINT('Ctrl Pts',(32.4090600499826,20.5438781387238,38.9678194682778));
#67356=CARTESIAN_POINT('Ctrl Pts',(32.4215698413416,20.6245672450295,38.9720885053614));
#67357=CARTESIAN_POINT('Ctrl Pts',(32.4339683734725,20.7045387208463,38.9763195746038));
#67358=CARTESIAN_POINT('Ctrl Pts',(32.4424243708411,20.7852751140938,38.9805506438462));
#67359=CARTESIAN_POINT('Ctrl Pts',(32.4468528546562,20.8663536096225,38.9847817130886));
#67360=CARTESIAN_POINT('Ctrl Pts',(32.4512749847276,20.9473157782114,38.989006711827));
#67361=CARTESIAN_POINT('Ctrl Pts',(32.4516810525102,21.0286186139134,38.9932317105654));
#67362=CARTESIAN_POINT('Ctrl Pts',(32.4480374506469,21.1098311896978,38.9974567093037));
#67363=CARTESIAN_POINT('Ctrl Pts',(32.4443830368485,21.1912847536914,39.0016942451999));
#67364=CARTESIAN_POINT('Ctrl Pts',(32.4366548144621,21.2726470533978,39.0059317810961));
#67365=CARTESIAN_POINT('Ctrl Pts',(32.4248715360129,21.3534802453242,39.0101693169922));
#67366=CARTESIAN_POINT('Ctrl Pts',(32.4131442745107,21.433929161461,39.0143867079156));
#67367=CARTESIAN_POINT('Ctrl Pts',(32.3974004863793,21.5138535247576,39.018604098839));
#67368=CARTESIAN_POINT('Ctrl Pts',(32.3777106614346,21.5928256577614,39.0228214897623));
#67369=CARTESIAN_POINT('Ctrl Pts',(32.358027345337,21.6717716850206,39.0270374865467));
#67370=CARTESIAN_POINT('Ctrl Pts',(32.3344006952404,21.7497656562931,39.0312534833311));
#67371=CARTESIAN_POINT('Ctrl Pts',(32.3069520781732,21.8263911658604,39.0354694801155));
#67372=CARTESIAN_POINT('Ctrl Pts',(32.2795041241438,21.9030148244929,39.0396853750599));
#67373=CARTESIAN_POINT('Ctrl Pts',(32.2482345445415,21.9782696497905,39.0439012700044));
#67374=CARTESIAN_POINT('Ctrl Pts',(32.2133137687003,22.051756821362,39.0481171649488));
#67375=CARTESIAN_POINT('Ctrl Pts',(32.1780826059329,22.1258971702114,39.0523705321041));
#67376=CARTESIAN_POINT('Ctrl Pts',(32.1391352075502,22.1982378434502,39.0566238992593));
#67377=CARTESIAN_POINT('Ctrl Pts',(32.0966942906118,22.2683939852096,39.0608772664146));
#67378=CARTESIAN_POINT('Ctrl Pts',(32.0545660878117,22.338033200875,39.0650992938124));
#67379=CARTESIAN_POINT('Ctrl Pts',(32.0089959918147,22.4055196158146,39.0693213212101));
#67380=CARTESIAN_POINT('Ctrl Pts',(31.960244769042,22.4705069518515,39.0735433486079));
#67381=CARTESIAN_POINT('Ctrl Pts',(31.9109507318739,22.5362178812571,39.0778123856419));
#67382=CARTESIAN_POINT('Ctrl Pts',(31.8584046011056,22.5993733597426,39.0820814226759));
#67383=CARTESIAN_POINT('Ctrl Pts',(31.8029156765867,22.6596521663041,39.0863504597099));
#67384=CARTESIAN_POINT('Ctrl Pts',(31.7474267520679,22.7199309728656,39.0906194967439));
#67385=CARTESIAN_POINT('Ctrl Pts',(31.6889954245913,22.7773328141653,39.0948885337779));
#67386=CARTESIAN_POINT('Ctrl Pts',(31.627965423889,22.8315782343711,39.0991575708119));
#67387=CARTESIAN_POINT('Ctrl Pts',(31.5674782094927,22.8853412087157,39.1033886400462));
#67388=CARTESIAN_POINT('Ctrl Pts',(31.5042113702353,22.9362054998204,39.1076197092805));
#67389=CARTESIAN_POINT('Ctrl Pts',(31.4384741774593,22.9838705327674,39.1118507785148));
#67390=CARTESIAN_POINT('Ctrl Pts',(31.3728313007722,23.031467178561,39.116075777245));
#67391=CARTESIAN_POINT('Ctrl Pts',(31.3047254830865,23.0758734118581,39.1203007759751));
#67392=CARTESIAN_POINT('Ctrl Pts',(31.2345006554552,23.1168274331368,39.1245257747053));
#67393=CARTESIAN_POINT('Ctrl Pts',(31.164067444219,23.1579029804751,39.1287633106035));
#67394=CARTESIAN_POINT('Ctrl Pts',(31.0915029841239,23.1955054853551,39.1330008465017));
#67395=CARTESIAN_POINT('Ctrl Pts',(31.017185397046,23.2294134022286,39.1372383823999));
#67396=CARTESIAN_POINT('Ctrl Pts',(30.943221111174,23.2631601229654,39.1414557733149));
#67397=CARTESIAN_POINT('Ctrl Pts',(30.8675207528168,23.2932471040874,39.1456731642299));
#67398=CARTESIAN_POINT('Ctrl Pts',(30.7904819413076,23.3195017892786,39.1498905551449));
#67399=CARTESIAN_POINT('Ctrl Pts',(30.7134685964475,23.3457477954826,39.1541065519209));
#67400=CARTESIAN_POINT('Ctrl Pts',(30.6351181168376,23.3681638716389,39.1583225486969));
#67401=CARTESIAN_POINT('Ctrl Pts',(30.5558462239094,23.3866263271333,39.1625385454729));
#67402=CARTESIAN_POINT('Ctrl Pts',(30.4765762458415,23.4050883366559,39.1667544404089));
#67403=CARTESIAN_POINT('Ctrl Pts',(30.396385351801,23.4195968110048,39.1709703353449));
#67404=CARTESIAN_POINT('Ctrl Pts',(30.3157010757981,23.4300788219191,39.175186230281));
#67405=CARTESIAN_POINT('Ctrl Pts',(30.2342996520202,23.4406540003152,39.1794395974461));
#67406=CARTESIAN_POINT('Ctrl Pts',(30.152396506657,23.447130701546,39.1836929646112));
#67407=CARTESIAN_POINT('Ctrl Pts',(30.0704357773143,23.4494875078828,39.1879463317763));
#67408=CARTESIAN_POINT('Ctrl Pts',(29.9890789532496,23.451826948735,39.1921683591657));
#67409=CARTESIAN_POINT('Ctrl Pts',(29.9076658592812,23.4501070776601,39.196390386555));
#67410=CARTESIAN_POINT('Ctrl Pts',(29.8266288350047,23.4443593617036,39.2006124139443));
#67411=CARTESIAN_POINT('Ctrl Pts',(29.7446895135839,23.4385476484849,39.2048814509973));
#67412=CARTESIAN_POINT('Ctrl Pts',(29.6631351732003,23.4286178978568,39.2091504880503));
#67413=CARTESIAN_POINT('Ctrl Pts',(29.5824034001455,23.4146559443925,39.2134195251033));
#67414=CARTESIAN_POINT('Ctrl Pts',(29.5016716270906,23.4006939909282,39.2176885621563));
#67415=CARTESIAN_POINT('Ctrl Pts',(29.4217628796863,23.3827000040603,39.2219575992094));
#67416=CARTESIAN_POINT('Ctrl Pts',(29.3430983057943,23.3608113889402,39.2262266362624));
#67417=CARTESIAN_POINT('Ctrl Pts',(29.2651333562676,23.3391174460557,39.2304577054959));
#67418=CARTESIAN_POINT('Ctrl Pts',(29.188097907312,23.3135164956762,39.2346887747295));
#67419=CARTESIAN_POINT('Ctrl Pts',(29.1124121790456,23.2841055383001,39.238919843963));
#67420=CARTESIAN_POINT('Ctrl Pts',(29.0368350404775,23.2547367781397,39.2431448426924));
#67421=CARTESIAN_POINT('Ctrl Pts',(28.9626042062942,23.2215690345955,39.2473698414217));
#67422=CARTESIAN_POINT('Ctrl Pts',(28.8901260953187,23.1847494514721,39.251594840151));
#67423=CARTESIAN_POINT('Ctrl Pts',(28.8174329143776,23.1478206107208,39.2558323760495));
#67424=CARTESIAN_POINT('Ctrl Pts',(28.7465033289733,23.1072183551549,39.2600699119479));
#67425=CARTESIAN_POINT('Ctrl Pts',(28.6777284599249,23.0631403792053,39.2643074478463));
#67426=CARTESIAN_POINT('Ctrl Pts',(28.6092805423615,23.0192719472345,39.2685248387604));
#67427=CARTESIAN_POINT('Ctrl Pts',(28.5429672982889,22.9719610146033,39.2727422296745));
#67428=CARTESIAN_POINT('Ctrl Pts',(28.4791492459235,22.9214482126315,39.2769596205887));
#67429=CARTESIAN_POINT('Ctrl Pts',(28.4153522898335,22.8709521086307,39.2811756173637));
#67430=CARTESIAN_POINT('Ctrl Pts',(28.3540492517466,22.8172565255332,39.2853916141388));
#67431=CARTESIAN_POINT('Ctrl Pts',(28.2955693948253,22.7606437919533,39.2896076109139));
#67432=CARTESIAN_POINT('Ctrl Pts',(28.2370909505208,22.7040324258887,39.2938235058489));
#67433=CARTESIAN_POINT('Ctrl Pts',(28.1814358850927,22.6445043736385,39.298039400784));
#67434=CARTESIAN_POINT('Ctrl Pts',(28.1288972038969,22.582379403435,39.3022552957191));
#67435=CARTESIAN_POINT('Ctrl Pts',(28.0758915419931,22.5197022465014,39.3065086628852));
#67436=CARTESIAN_POINT('Ctrl Pts',(28.0260582638189,22.4543821326794,39.3107620300514));
#67437=CARTESIAN_POINT('Ctrl Pts',(27.979656084827,22.3867807016337,39.3150153972175));
#67438=CARTESIAN_POINT('Ctrl Pts',(27.9335958076563,22.3196773733256,39.3192374246059));
#67439=CARTESIAN_POINT('Ctrl Pts',(27.8909164286964,22.2503266672343,39.3234594519942));
#67440=CARTESIAN_POINT('Ctrl Pts',(27.8518258253334,22.1791089709164,39.3276814793825));
#67441=CARTESIAN_POINT('Ctrl Pts',(27.8122999722509,22.1070983095459,39.3319505164376));
#67442=CARTESIAN_POINT('Ctrl Pts',(27.7764435212813,22.0331792638651,39.3362195534926));
#67443=CARTESIAN_POINT('Ctrl Pts',(27.7444215036457,21.9577660971156,39.3404885905477));
#67444=CARTESIAN_POINT('Ctrl Pts',(27.7123994860101,21.8823529303662,39.3447576276027));
#67445=CARTESIAN_POINT('Ctrl Pts',(27.6842120077232,21.8054461195461,39.3490266646578));
#67446=CARTESIAN_POINT('Ctrl Pts',(27.6599718513331,21.7274740637621,39.3532957017129));
#67447=CARTESIAN_POINT('Ctrl Pts',(27.6307739903376,21.6335548163087,39.3584378612152));
#67448=CARTESIAN_POINT('Ctrl Pts',(27.6072124747056,21.5378055642196,39.3635800207174));
#67449=CARTESIAN_POINT('Ctrl Pts',(27.5894793038261,21.4408403603544,39.3687221802197));
#67450=CARTESIAN_POINT('Ctrl Pts',(27.5719783728498,21.3451450472329,39.3737969961751));
#67451=CARTESIAN_POINT('Ctrl Pts',(27.560154166145,21.2482654276719,39.3788718121305));
#67452=CARTESIAN_POINT('Ctrl Pts',(27.5541451768665,21.1508125795628,39.3839466280858));
#67453=CARTESIAN_POINT('Ctrl Pts',(27.5510958246397,21.1013586621714,39.3865219199722));
#67454=CARTESIAN_POINT('Ctrl Pts',(27.5495432706177,21.0517574604063,39.3890972118585));
#67455=CARTESIAN_POINT('Ctrl Pts',(27.5495008920499,21.0020909174755,39.3916725037448));
#67456=CARTESIAN_POINT('',(27.5495003167105,20.9987541275197,40.1916725038142));
#67457=CARTESIAN_POINT('Ctrl Pts',(27.5495008920492,21.0020909166425,39.391672503788));
#67458=CARTESIAN_POINT('Ctrl Pts',(27.5494318810471,20.9212118439509,39.3958662166454));
#67459=CARTESIAN_POINT('Ctrl Pts',(27.553371295196,20.8402633153025,39.4000599295028));
#67460=CARTESIAN_POINT('Ctrl Pts',(27.5613130467361,20.7596748161747,39.4042536423602));
#67461=CARTESIAN_POINT('Ctrl Pts',(27.5692519940786,20.6791147724934,39.408445874436));
#67462=CARTESIAN_POINT('Ctrl Pts',(27.581190427325,20.5989149738489,39.4126381065117));
#67463=CARTESIAN_POINT('Ctrl Pts',(27.5970702728484,20.5195013253181,39.4168303385874));
#67464=CARTESIAN_POINT('Ctrl Pts',(27.6129495126589,20.4400907059015,39.4210224107568));
#67465=CARTESIAN_POINT('Ctrl Pts',(27.6327697726531,20.3614666382289,39.4252144829261));
#67466=CARTESIAN_POINT('Ctrl Pts',(27.6564218627886,20.2840448583991,39.4294065550955));
#67467=CARTESIAN_POINT('Ctrl Pts',(27.6803811398932,20.205617545369,39.4336530727678));
#67468=CARTESIAN_POINT('Ctrl Pts',(27.7082723719833,20.1284244542174,39.4378995904401));
#67469=CARTESIAN_POINT('Ctrl Pts',(27.7399305388862,20.0528800071055,39.4421461081125));
#67470=CARTESIAN_POINT('Ctrl Pts',(27.7712287202026,19.978194577263,39.4463443385558));
#67471=CARTESIAN_POINT('Ctrl Pts',(27.8062083394607,19.9051208898304,39.4505425689992));
#67472=CARTESIAN_POINT('Ctrl Pts',(27.8446630165833,19.8340357046993,39.4547407994425));
#67473=CARTESIAN_POINT('Ctrl Pts',(27.8837811410171,19.7617241076342,39.4590114607293));
#67474=CARTESIAN_POINT('Ctrl Pts',(27.9264950968783,19.6914707088051,39.4632821220161));
#67475=CARTESIAN_POINT('Ctrl Pts',(27.9725421441624,19.6236407108598,39.467552783303));
#67476=CARTESIAN_POINT('Ctrl Pts',(28.0185891914466,19.5558107129145,39.4718234445898));
#67477=CARTESIAN_POINT('Ctrl Pts',(28.0679689693166,19.4904044755504,39.4760941058766));
#67478=CARTESIAN_POINT('Ctrl Pts',(28.1203778365118,19.4277497742014,39.4803647671634));
#67479=CARTESIAN_POINT('Ctrl Pts',(28.1723008364246,19.365675926267,39.4845958363983));
#67480=CARTESIAN_POINT('Ctrl Pts',(28.2273995277617,19.3060604645673,39.4888269056331));
#67481=CARTESIAN_POINT('Ctrl Pts',(28.2854122053,19.2492461782804,39.493057974868));
#67482=CARTESIAN_POINT('Ctrl Pts',(28.3433416494564,19.1925134059899,39.4972829735987));
#67483=CARTESIAN_POINT('Ctrl Pts',(28.4041764470199,19.1385741497362,39.5015079723293));
#67484=CARTESIAN_POINT('Ctrl Pts',(28.4676149074809,19.0877379420631,39.50573297106));
#67485=CARTESIAN_POINT('Ctrl Pts',(28.5312416138204,19.0367508841564,39.5099705069581));
#67486=CARTESIAN_POINT('Ctrl Pts',(28.597487152285,18.988885678891,39.5142080428562));
#67487=CARTESIAN_POINT('Ctrl Pts',(28.6660100934245,18.9444170707182,39.5184455787543));
#67488=CARTESIAN_POINT('Ctrl Pts',(28.7342072807563,18.9001598635476,39.5226629696698));
#67489=CARTESIAN_POINT('Ctrl Pts',(28.8046598767883,18.8592672920668,39.5268803605853));
#67490=CARTESIAN_POINT('Ctrl Pts',(28.8769999621023,18.8219685115036,39.5310977515008));
#67491=CARTESIAN_POINT('Ctrl Pts',(28.9493161340208,18.784682060764,39.5353137482773));
#67492=CARTESIAN_POINT('Ctrl Pts',(29.0235181432202,18.7509872546709,39.5395297450538));
#67493=CARTESIAN_POINT('Ctrl Pts',(29.0992129786693,18.7210675762098,39.5437457418303));
#67494=CARTESIAN_POINT('Ctrl Pts',(29.1749059856636,18.6911486204768,39.5479616367668));
#67495=CARTESIAN_POINT('Ctrl Pts',(29.2520913143972,18.6650047809581,39.5521775317033));
#67496=CARTESIAN_POINT('Ctrl Pts',(29.3303568044323,18.642771067412,39.5563934266398));
#67497=CARTESIAN_POINT('Ctrl Pts',(29.4093179432751,18.6203397334803,39.5606467938043));
#67498=CARTESIAN_POINT('Ctrl Pts',(29.4893780829221,18.6018885298034,39.5649001609688));
#67499=CARTESIAN_POINT('Ctrl Pts',(29.5701010645751,18.5875039574498,39.5691535281333));
#67500=CARTESIAN_POINT('Ctrl Pts',(29.6502292609765,18.5732253738903,39.5733755555231));
#67501=CARTESIAN_POINT('Ctrl Pts',(29.7310100900831,18.562953690652,39.5775975829129));
#67502=CARTESIAN_POINT('Ctrl Pts',(29.8120112854347,18.5567213639873,39.5818196103027));
#67503=CARTESIAN_POINT('Ctrl Pts',(29.8939143789668,18.5504196442223,39.5860886473545));
#67504=CARTESIAN_POINT('Ctrl Pts',(29.9760422882747,18.548247803433,39.5903576844064));
#67505=CARTESIAN_POINT('Ctrl Pts',(30.0579495617972,18.5501852930706,39.5946267214583));
#67506=CARTESIAN_POINT('Ctrl Pts',(30.1398568353197,18.5521227827082,39.5988957585101));
#67507=CARTESIAN_POINT('Ctrl Pts',(30.2215429948011,18.5581695025844,39.603164795562));
#67508=CARTESIAN_POINT('Ctrl Pts',(30.3025712642528,18.5682514768076,39.6074338326139));
#67509=CARTESIAN_POINT('Ctrl Pts',(30.3828788872287,18.5782437843103,39.6116649018487));
#67510=CARTESIAN_POINT('Ctrl Pts',(30.4628416922434,18.5922373140605,39.6158959710836));
#67511=CARTESIAN_POINT('Ctrl Pts',(30.5420297629938,18.6101979190676,39.6201270403184));
#67512=CARTESIAN_POINT('Ctrl Pts',(30.6211042190791,18.6281327551918,39.6243520390491));
#67513=CARTESIAN_POINT('Ctrl Pts',(30.6994056988939,18.6500232604064,39.6285770377798));
#67514=CARTESIAN_POINT('Ctrl Pts',(30.7765105631452,18.6757836599568,39.6328020365105));
#67515=CARTESIAN_POINT('Ctrl Pts',(30.8538442266582,18.7016205003446,39.6370395724086));
#67516=CARTESIAN_POINT('Ctrl Pts',(30.9299736934121,18.7313501746332,39.6412771083066));
#67517=CARTESIAN_POINT('Ctrl Pts',(31.004483021658,18.7648346573014,39.6455146442047));
#67518=CARTESIAN_POINT('Ctrl Pts',(31.0786381371836,18.798159956818,39.6497320351202));
#67519=CARTESIAN_POINT('Ctrl Pts',(31.151188053749,18.8352042586239,39.6539494260358));
#67520=CARTESIAN_POINT('Ctrl Pts',(31.2217407850415,18.8757825666457,39.6581668169513));
#67521=CARTESIAN_POINT('Ctrl Pts',(31.2922701937822,18.9163474607335,39.6623828137277));
#67522=CARTESIAN_POINT('Ctrl Pts',(31.3608033255887,18.9604438094675,39.6665988105042));
#67523=CARTESIAN_POINT('Ctrl Pts',(31.4269729772403,19.0078407763871,39.6708148072807));
#67524=CARTESIAN_POINT('Ctrl Pts',(31.4931410305236,19.0552365984041,39.6750307022172));
#67525=CARTESIAN_POINT('Ctrl Pts',(31.5569453398099,19.1059326084342,39.6792465971537));
#67526=CARTESIAN_POINT('Ctrl Pts',(31.6180490594758,19.159655605293,39.6834624920902));
#67527=CARTESIAN_POINT('Ctrl Pts',(31.6796958886238,19.2138561093994,39.6877158592547));
#67528=CARTESIAN_POINT('Ctrl Pts',(31.7385935081576,19.2711373741441,39.6919692264192));
#67529=CARTESIAN_POINT('Ctrl Pts',(31.7944328317891,19.3311797393975,39.6962225935837));
#67530=CARTESIAN_POINT('Ctrl Pts',(31.8498607186091,19.3907796988747,39.7004446209735));
#67531=CARTESIAN_POINT('Ctrl Pts',(31.9022749734291,19.4530998057375,39.7046666483633));
#67532=CARTESIAN_POINT('Ctrl Pts',(31.9514140381495,19.5177943794085,39.708888675753));
#67533=CARTESIAN_POINT('Ctrl Pts',(32.001100235945,19.58320928712,39.7131577128049));
#67534=CARTESIAN_POINT('Ctrl Pts',(32.0474375813126,19.6510514628234,39.7174267498568));
#67535=CARTESIAN_POINT('Ctrl Pts',(32.0902019145975,19.7209354174973,39.7216957869087));
#67536=CARTESIAN_POINT('Ctrl Pts',(32.1329662478825,19.7908193721712,39.7259648239606));
#67537=CARTESIAN_POINT('Ctrl Pts',(32.1721573940739,19.8627446495949,39.7302338610125));
#67538=CARTESIAN_POINT('Ctrl Pts',(32.207600795234,19.9363040947327,39.7345028980644));
#67539=CARTESIAN_POINT('Ctrl Pts',(32.2427289710765,20.0092093193755,39.7387339672995));
#67540=CARTESIAN_POINT('Ctrl Pts',(32.2743076826463,20.0839933687258,39.7429650365346));
#67541=CARTESIAN_POINT('Ctrl Pts',(32.3021326181401,20.16027643924,39.7471961057698));
#67542=CARTESIAN_POINT('Ctrl Pts',(32.3299176319551,20.236450063023,39.7514211045007));
#67543=CARTESIAN_POINT('Ctrl Pts',(32.3539594081034,20.3141180033863,39.7556461032317));
#67544=CARTESIAN_POINT('Ctrl Pts',(32.3741004241681,20.3928777503957,39.7598711019627));
#67545=CARTESIAN_POINT('Ctrl Pts',(32.394301206235,20.4718712073225,39.7641086378607));
#67546=CARTESIAN_POINT('Ctrl Pts',(32.4105778411914,20.5519625326692,39.7683461737587));
#67547=CARTESIAN_POINT('Ctrl Pts',(32.4228208894798,20.6327273662515,39.7725837096567));
#67548=CARTESIAN_POINT('Ctrl Pts',(32.4350057350778,20.7131082488363,39.7768011005725));
#67549=CARTESIAN_POINT('Ctrl Pts',(32.4431951820262,20.7941557882775,39.7810184914883));
#67550=CARTESIAN_POINT('Ctrl Pts',(32.4473322477455,20.8754402988734,39.7852358824041));
#67551=CARTESIAN_POINT('Ctrl Pts',(32.4514679458789,20.9566979393232,39.7894518791809));
#67552=CARTESIAN_POINT('Ctrl Pts',(32.4515538993977,21.0381919313699,39.7936678759576));
#67553=CARTESIAN_POINT('Ctrl Pts',(32.4475850815018,21.1194885718798,39.7978838727344));
#67554=CARTESIAN_POINT('Ctrl Pts',(32.4436163594751,21.2007832486199,39.8020997676712));
#67555=CARTESIAN_POINT('Ctrl Pts',(32.4355930845468,21.2818801189463,39.806315662608));
#67556=CARTESIAN_POINT('Ctrl Pts',(32.4235622860938,21.3623480307987,39.8105315575448));
#67557=CARTESIAN_POINT('Ctrl Pts',(32.4114245540427,21.4435311672794,39.814784924709));
#67558=CARTESIAN_POINT('Ctrl Pts',(32.3952077562772,21.524073630282,39.8190382918731));
#67559=CARTESIAN_POINT('Ctrl Pts',(32.3750130108635,21.6035424162633,39.8232916590373));
#67560=CARTESIAN_POINT('Ctrl Pts',(32.354967064915,21.6824256582027,39.8275136864274));
#67561=CARTESIAN_POINT('Ctrl Pts',(32.3310017950156,21.7602505621038,39.8317357138175));
#67562=CARTESIAN_POINT('Ctrl Pts',(32.3032659460962,21.8366099638145,39.8359577412075));
#67563=CARTESIAN_POINT('Ctrl Pts',(32.2752212756702,21.9138195801895,39.8402267782588));
#67564=CARTESIAN_POINT('Ctrl Pts',(32.2433217288294,21.9895304069517,39.84449581531));
#67565=CARTESIAN_POINT('Ctrl Pts',(32.2077697744543,22.0633451335318,39.8487648523612));
#67566=CARTESIAN_POINT('Ctrl Pts',(32.1722178200793,22.137159860112,39.8530338894124));
#67567=CARTESIAN_POINT('Ctrl Pts',(32.133013746719,22.209078092168,39.8573029264636));
#67568=CARTESIAN_POINT('Ctrl Pts',(32.0904051145294,22.2787324611306,39.8615719635149));
#67569=CARTESIAN_POINT('Ctrl Pts',(32.0481754335407,22.3477673404405,39.8658030327499));
#67570=CARTESIAN_POINT('Ctrl Pts',(32.0024430523482,22.4148375899673,39.8700341019848));
#67571=CARTESIAN_POINT('Ctrl Pts',(31.9534164190798,22.4795656604793,39.8742651712198));
#67572=CARTESIAN_POINT('Ctrl Pts',(31.9044601265138,22.544200862735,39.8784901699507));
#67573=CARTESIAN_POINT('Ctrl Pts',(31.8522192472137,22.6065001925079,39.8827151686815));
#67574=CARTESIAN_POINT('Ctrl Pts',(31.7969466706598,22.666113115249,39.8869401674123));
#67575=CARTESIAN_POINT('Ctrl Pts',(31.741510079492,22.7259029320507,39.8911777033103));
#67576=CARTESIAN_POINT('Ctrl Pts',(31.6830240213945,22.7829899730464,39.8954152392084));
#67577=CARTESIAN_POINT('Ctrl Pts',(31.6217858087531,22.8370522694052,39.8996527751064));
#67578=CARTESIAN_POINT('Ctrl Pts',(31.5608387187701,22.8908575569659,39.9038701660221));
#67579=CARTESIAN_POINT('Ctrl Pts',(31.4971659294199,22.9416664792799,39.9080875569377));
#67580=CARTESIAN_POINT('Ctrl Pts',(31.4310976595226,22.9891982653595,39.9123049478534));
#67581=CARTESIAN_POINT('Ctrl Pts',(31.3650512297526,23.0367143389,39.91652094463));
#67582=CARTESIAN_POINT('Ctrl Pts',(31.2966112691117,23.0809551561929,39.9207369414066));
#67583=CARTESIAN_POINT('Ctrl Pts',(31.2261395319125,23.1216814318558,39.9249529381832));
#67584=CARTESIAN_POINT('Ctrl Pts',(31.1556694970008,23.1624067237507,39.9291688331199));
#67585=CARTESIAN_POINT('Ctrl Pts',(31.0831681862348,23.1996174111144,39.9333847280565));
#67586=CARTESIAN_POINT('Ctrl Pts',(31.0090234237429,23.2331193385796,39.9376006229931));
#67587=CARTESIAN_POINT('Ctrl Pts',(30.9342196387978,23.2669190419319,39.9418539901575));
#67588=CARTESIAN_POINT('Ctrl Pts',(30.8577434724237,23.2969435128454,39.9461073573218));
#67589=CARTESIAN_POINT('Ctrl Pts',(30.7800136200119,23.3230430479429,39.9503607244862));
#67590=CARTESIAN_POINT('Ctrl Pts',(30.7028564987912,23.3489502757432,39.9545827518761));
#67591=CARTESIAN_POINT('Ctrl Pts',(30.6244645740498,23.370990147871,39.958804779266));
#67592=CARTESIAN_POINT('Ctrl Pts',(30.5452606391552,23.389066990561,39.9630268066559));
#67593=CARTESIAN_POINT('Ctrl Pts',(30.4651748174707,23.4073451077052,39.9672958437075));
#67594=CARTESIAN_POINT('Ctrl Pts',(30.3842592719849,23.4215713116105,39.9715648807591));
#67595=CARTESIAN_POINT('Ctrl Pts',(30.3029576328519,23.4317004179579,39.9758339178106));
#67596=CARTESIAN_POINT('Ctrl Pts',(30.2216559937188,23.4418295243054,39.9801029548622));
#67597=CARTESIAN_POINT('Ctrl Pts',(30.1399687487282,23.4478615618603,39.9843719919138));
#67598=CARTESIAN_POINT('Ctrl Pts',(30.0583388039753,23.4498054685935,39.9886410289654));
#67599=CARTESIAN_POINT('Ctrl Pts',(29.9774348568495,23.4517320866751,39.9928720982004));
#67600=CARTESIAN_POINT('Ctrl Pts',(29.8962835467492,23.4496502773267,39.9971031674354));
#67601=CARTESIAN_POINT('Ctrl Pts',(29.8153151373108,23.4435305914789,40.0013342366704));
#67602=CARTESIAN_POINT('Ctrl Pts',(29.7344628968688,23.437419685818,40.0055592354012));
#67603=CARTESIAN_POINT('Ctrl Pts',(29.6537934956345,23.4272824443422,40.009784234132));
#67604=CARTESIAN_POINT('Ctrl Pts',(29.5737385810179,23.4131414075199,40.0140092328629));
#67605=CARTESIAN_POINT('Ctrl Pts',(29.4934461132292,23.3989584088998,40.0182467687609));
#67606=CARTESIAN_POINT('Ctrl Pts',(29.4137722572628,23.3807478098741,40.0224843046589));
#67607=CARTESIAN_POINT('Ctrl Pts',(29.3351487308337,23.3585849655859,40.026721840557));
#67608=CARTESIAN_POINT('Ctrl Pts',(29.2568989757643,23.3365274820825,40.0309392314726));
#67609=CARTESIAN_POINT('Ctrl Pts',(29.1796900388715,23.3105553671463,40.0351566223883));
#67610=CARTESIAN_POINT('Ctrl Pts',(29.1039368505293,23.2807939587259,40.039374013304));
#67611=CARTESIAN_POINT('Ctrl Pts',(29.0282087038492,23.2510423885071,40.0435900100806));
#67612=CARTESIAN_POINT('Ctrl Pts',(28.9539357824988,23.2175041822141,40.0478060068572));
#67613=CARTESIAN_POINT('Ctrl Pts',(28.8815152446484,23.1803536644421,40.0520220036338));
#67614=CARTESIAN_POINT('Ctrl Pts',(28.8090964561599,23.1432040440634,40.0562378985705));
#67615=CARTESIAN_POINT('Ctrl Pts',(28.7385303754074,23.1024424988996,40.0604537935071));
#67616=CARTESIAN_POINT('Ctrl Pts',(28.6701903633218,23.0582897221231,40.0646696884438));
#67617=CARTESIAN_POINT('Ctrl Pts',(28.6012429232688,23.0137445012918,40.0689230556081));
#67618=CARTESIAN_POINT('Ctrl Pts',(28.534561735099,22.9657477095122,40.0731764227725));
#67619=CARTESIAN_POINT('Ctrl Pts',(28.4704995346241,22.9145700761306,40.0774297899368));
#67620=CARTESIAN_POINT('Ctrl Pts',(28.4069093589788,22.8637695311647,40.0816518173267));
#67621=CARTESIAN_POINT('Ctrl Pts',(28.3459000154409,22.8098352208492,40.0858738447167));
#67622=CARTESIAN_POINT('Ctrl Pts',(28.2877810550468,22.7530706016996,40.0900958721066));
#67623=CARTESIAN_POINT('Ctrl Pts',(28.2290149760035,22.6956739436522,40.0943649091581));
#67624=CARTESIAN_POINT('Ctrl Pts',(28.1732043764096,22.635383916685,40.0986339462097));
#67625=CARTESIAN_POINT('Ctrl Pts',(28.1206276698347,22.572548852853,40.1029029832612));
#67626=CARTESIAN_POINT('Ctrl Pts',(28.0680509632599,22.5097137890209,40.1071720203128));
#67627=CARTESIAN_POINT('Ctrl Pts',(28.0187083899052,22.4443341138468,40.1114410573643));
#67628=CARTESIAN_POINT('Ctrl Pts',(27.9728324872057,22.3767868844056,40.1157100944159));
#67629=CARTESIAN_POINT('Ctrl Pts',(27.9266694884468,22.3088169375408,40.1200058475349));
#67630=CARTESIAN_POINT('Ctrl Pts',(27.8838466951709,22.2384023151295,40.124301600654));
#67631=CARTESIAN_POINT('Ctrl Pts',(27.8446277155084,22.1658990373294,40.1285973537731));
#67632=CARTESIAN_POINT('Ctrl Pts',(27.8054697114269,22.0935084837643,40.132886428084));
#67633=CARTESIAN_POINT('Ctrl Pts',(27.7699045982222,22.0190361163048,40.1371755023949));
#67634=CARTESIAN_POINT('Ctrl Pts',(27.7381530541333,21.9428672459438,40.1414645767059));
#67635=CARTESIAN_POINT('Ctrl Pts',(27.7064501225189,21.8668149921874,40.1457470843278));
#67636=CARTESIAN_POINT('Ctrl Pts',(27.6785493147091,21.7890718124622,40.1500295919497));
#67637=CARTESIAN_POINT('Ctrl Pts',(27.6546249595839,21.7100465969167,40.1543120995716));
#67638=CARTESIAN_POINT('Ctrl Pts',(27.6307223085427,21.6310930727464,40.1585907221189));
#67639=CARTESIAN_POINT('Ctrl Pts',(27.6107890710512,21.5508602491011,40.1628693446662));
#67640=CARTESIAN_POINT('Ctrl Pts',(27.5949508390342,21.4697752476854,40.1671479672134));
#67641=CARTESIAN_POINT('Ctrl Pts',(27.5791219983052,21.3887383256638,40.1714240527492));
#67642=CARTESIAN_POINT('Ctrl Pts',(27.5673834247026,21.3068506668956,40.175700138285));
#67643=CARTESIAN_POINT('Ctrl Pts',(27.5598100877106,21.2245516465335,40.1799762238208));
#67644=CARTESIAN_POINT('Ctrl Pts',(27.5529050286324,21.149514764077,40.1838749838099));
#67645=CARTESIAN_POINT('Ctrl Pts',(27.5494619912402,21.0741363136556,40.1877737437989));
#67646=CARTESIAN_POINT('Ctrl Pts',(27.5495003167103,20.9987541280282,40.1916725037879));
#67647=CARTESIAN_POINT('',(27.5495004369098,20.998536683703,40.9916725037587));
#67648=CARTESIAN_POINT('Ctrl Pts',(27.5495003167105,20.9987541275197,40.1916725038142));
#67649=CARTESIAN_POINT('Ctrl Pts',(27.5495460863282,20.9087301200364,40.1963285375377));
#67650=CARTESIAN_POINT('Ctrl Pts',(27.5545568244828,20.8188767932227,40.2009845712612));
#67651=CARTESIAN_POINT('Ctrl Pts',(27.5644515219164,20.7297152225801,40.2056406049846));
#67652=CARTESIAN_POINT('Ctrl Pts',(27.5743801343139,20.6402480426492,40.2103125976817));
#67653=CARTESIAN_POINT('Ctrl Pts',(27.5892261144754,20.5514776431576,40.2149845903788));
#67654=CARTESIAN_POINT('Ctrl Pts',(27.60885757913,20.4639140245109,40.2196565830759));
#67655=CARTESIAN_POINT('Ctrl Pts',(27.6285833211493,20.3759298938268,40.2243510123647));
#67656=CARTESIAN_POINT('Ctrl Pts',(27.6531404882094,20.2891644297647,40.2290454416536));
#67657=CARTESIAN_POINT('Ctrl Pts',(27.6823468164612,20.2041143481427,40.2337398709425));
#67658=CARTESIAN_POINT('Ctrl Pts',(27.7010927543397,20.1495253723252,40.2367529672504));
#67659=CARTESIAN_POINT('Ctrl Pts',(27.7217530099953,20.0956426438008,40.2397660635584));
#67660=CARTESIAN_POINT('Ctrl Pts',(27.7442693557824,20.0425922964913,40.2427791598663));
#67661=CARTESIAN_POINT('Ctrl Pts',(27.7758874018746,19.9680976008471,40.2470102291013));
#67662=CARTESIAN_POINT('Ctrl Pts',(27.8112589881166,19.8950310561913,40.2512412983363));
#67663=CARTESIAN_POINT('Ctrl Pts',(27.8502334563358,19.8237967617192,40.2554723675714));
#67664=CARTESIAN_POINT('Ctrl Pts',(27.8891520061431,19.752664670274,40.2596973663022));
#67665=CARTESIAN_POINT('Ctrl Pts',(27.9316629502183,19.6833600124647,40.263922365033));
#67666=CARTESIAN_POINT('Ctrl Pts',(27.9775676993811,19.6162667022098,40.2681473637638));
#67667=CARTESIAN_POINT('Ctrl Pts',(28.0236086652751,19.548974300759,40.2723848996619));
#67668=CARTESIAN_POINT('Ctrl Pts',(28.0730634199664,19.4839068243992,40.2766224355599));
#67669=CARTESIAN_POINT('Ctrl Pts',(28.1256852334135,19.4214264648881,40.280859971458));
#67670=CARTESIAN_POINT('Ctrl Pts',(28.178056886029,19.3592431331241,40.2850773623736));
#67671=CARTESIAN_POINT('Ctrl Pts',(28.2335652563088,19.299622737962,40.2892947532893));
#67672=CARTESIAN_POINT('Ctrl Pts',(28.2919250068862,19.2428915605748,40.293512144205));
#67673=CARTESIAN_POINT('Ctrl Pts',(28.3502654655344,19.1861791367608,40.2977281409816));
#67674=CARTESIAN_POINT('Ctrl Pts',(28.411455099526,19.132354357901,40.3019441377583));
#67675=CARTESIAN_POINT('Ctrl Pts',(28.4751712778851,19.0817071083347,40.3061601345349));
#67676=CARTESIAN_POINT('Ctrl Pts',(28.5388859171412,19.0310610821835,40.3103760294716));
#67677=CARTESIAN_POINT('Ctrl Pts',(28.6051266147554,18.9835927211783,40.3145919244082));
#67678=CARTESIAN_POINT('Ctrl Pts',(28.6735383164339,18.9395511042418,40.3188078193449));
#67679=CARTESIAN_POINT('Ctrl Pts',(28.7425580832798,18.895118031275,40.3230611865092));
#67680=CARTESIAN_POINT('Ctrl Pts',(28.8137872449956,18.8541731976804,40.3273145536736));
#67681=CARTESIAN_POINT('Ctrl Pts',(28.8868336744412,18.8169262537326,40.3315679208379));
#67682=CARTESIAN_POINT('Ctrl Pts',(28.9593418812197,18.7799537537195,40.3357899482278));
#67683=CARTESIAN_POINT('Ctrl Pts',(29.0336402106091,18.7466249661912,40.3400119756178));
#67684=CARTESIAN_POINT('Ctrl Pts',(29.1093245362922,18.7170967019278,40.3442340030077));
#67685=CARTESIAN_POINT('Ctrl Pts',(29.1858515600938,18.6872396587196,40.3485030400592));
#67686=CARTESIAN_POINT('Ctrl Pts',(29.263795172758,18.6612684511329,40.3527720771108));
#67687=CARTESIAN_POINT('Ctrl Pts',(29.3427232126071,18.6392930137871,40.3570411141623));
#67688=CARTESIAN_POINT('Ctrl Pts',(29.4216512524562,18.6173175764413,40.3613101512138));
#67689=CARTESIAN_POINT('Ctrl Pts',(29.5015632327741,18.59933795262,40.3655791882654));
#67690=CARTESIAN_POINT('Ctrl Pts',(29.5820197486823,18.5854104366356,40.3698482253169));
#67691=CARTESIAN_POINT('Ctrl Pts',(29.6617607031666,18.571606788719,40.3740792945519));
#67692=CARTESIAN_POINT('Ctrl Pts',(29.7423358224686,18.5617316071648,40.3783103637869));
#67693=CARTESIAN_POINT('Ctrl Pts',(29.8233238520227,18.5558772967103,40.382541433022));
#67694=CARTESIAN_POINT('Ctrl Pts',(29.9041956844304,18.5500313856968,40.3867664317528));
#67695=CARTESIAN_POINT('Ctrl Pts',(29.9854787906683,18.5481949215412,40.3909914304837));
#67696=CARTESIAN_POINT('Ctrl Pts',(30.0667429017055,18.5504090882207,40.3952164292145));
#67697=CARTESIAN_POINT('Ctrl Pts',(30.1482481540567,18.552629825169,40.3994539651126));
#67698=CARTESIAN_POINT('Ctrl Pts',(30.2297338316988,18.558925345847,40.4036915010106));
#67699=CARTESIAN_POINT('Ctrl Pts',(30.3107618289751,18.5692846041439,40.4079290369086));
#67700=CARTESIAN_POINT('Ctrl Pts',(30.3914046241873,18.5795946151705,40.4121464278243));
#67701=CARTESIAN_POINT('Ctrl Pts',(30.4715936153757,18.5939297601873,40.41636381874));
#67702=CARTESIAN_POINT('Ctrl Pts',(30.5508999510761,18.6122270849379,40.4205812096557));
#67703=CARTESIAN_POINT('Ctrl Pts',(30.6301800705538,18.6305183611585,40.4247972064324));
#67704=CARTESIAN_POINT('Ctrl Pts',(30.708577661269,18.6527691116501,40.429013203209));
#67705=CARTESIAN_POINT('Ctrl Pts',(30.7856742466026,18.6788653145013,40.4332291999857));
#67706=CARTESIAN_POINT('Ctrl Pts',(30.8627689696215,18.7049608869828,40.4374450949223));
#67707=CARTESIAN_POINT('Ctrl Pts',(30.9385623096799,18.7349015770176,40.441660989859));
#67708=CARTESIAN_POINT('Ctrl Pts',(31.0126525095517,18.7685239985833,40.4458768847957));
#67709=CARTESIAN_POINT('Ctrl Pts',(31.0874012469051,18.8024452670257,40.45013025196));
#67710=CARTESIAN_POINT('Ctrl Pts',(31.1604159714467,18.8401138597372,40.4543836191243));
#67711=CARTESIAN_POINT('Ctrl Pts',(31.2313079683454,18.8813138653663,40.4586369862886));
#67712=CARTESIAN_POINT('Ctrl Pts',(31.3016776169255,18.9222103000056,40.4628590136786));
#67713=CARTESIAN_POINT('Ctrl Pts',(31.3699553554139,18.9665859718893,40.4670810410685));
#67714=CARTESIAN_POINT('Ctrl Pts',(31.4357903712559,19.014186247452,40.4713030684585));
#67715=CARTESIAN_POINT('Ctrl Pts',(31.5023584192471,19.0623165226182,40.4755721055099));
#67716=CARTESIAN_POINT('Ctrl Pts',(31.566428629876,19.1137433491633,40.4798411425614));
#67717=CARTESIAN_POINT('Ctrl Pts',(31.6276743899694,19.1681631267393,40.4841101796129));
#67718=CARTESIAN_POINT('Ctrl Pts',(31.6889201500628,19.2225829043152,40.4883792166644));
#67719=CARTESIAN_POINT('Ctrl Pts',(31.7473411594526,19.2799952473507,40.4926482537159));
#67720=CARTESIAN_POINT('Ctrl Pts',(31.8026519579067,19.3400613961188,40.4969172907674));
#67721=CARTESIAN_POINT('Ctrl Pts',(31.8574708350635,19.3995933306167,40.5011483600024));
#67722=CARTESIAN_POINT('Ctrl Pts',(31.9094403829716,19.461955459761,40.5053794292374));
#67723=CARTESIAN_POINT('Ctrl Pts',(31.9582546318543,19.5268438484597,40.5096104984724));
#67724=CARTESIAN_POINT('Ctrl Pts',(32.0069988447519,19.5916391388863,40.5138354972032));
#67725=CARTESIAN_POINT('Ctrl Pts',(32.0525964724986,19.6589531218623,40.518060495934));
#67726=CARTESIAN_POINT('Ctrl Pts',(32.094779704901,19.7284465257274,40.5222854946648));
#67727=CARTESIAN_POINT('Ctrl Pts',(32.1370881108886,19.7981461427727,40.5265230305629));
#67728=CARTESIAN_POINT('Ctrl Pts',(32.1759615096516,19.8700377842204,40.5307605664609));
#67729=CARTESIAN_POINT('Ctrl Pts',(32.2111717371794,19.9437472846429,40.534998102359));
#67730=CARTESIAN_POINT('Ctrl Pts',(32.2462145774731,20.0171063746802,40.5392154932746));
#67731=CARTESIAN_POINT('Ctrl Pts',(32.2776287894671,20.0922656587053,40.5434328841903));
#67732=CARTESIAN_POINT('Ctrl Pts',(32.3052348477571,20.1688306149247,40.547650275106));
#67733=CARTESIAN_POINT('Ctrl Pts',(32.3328317803376,20.2453702611367,40.5518662718826));
#67734=CARTESIAN_POINT('Ctrl Pts',(32.3566229015349,20.3233142197191,40.5560822686592));
#67735=CARTESIAN_POINT('Ctrl Pts',(32.3764772255902,20.4022490098284,40.5602982654358));
#67736=CARTESIAN_POINT('Ctrl Pts',(32.3963310700522,20.4811818932199,40.5645141603725));
#67737=CARTESIAN_POINT('Ctrl Pts',(32.4122481940969,20.5611051093655,40.5687300553092));
#67738=CARTESIAN_POINT('Ctrl Pts',(32.4241481586286,20.6415924735481,40.5729459502458));
#67739=CARTESIAN_POINT('Ctrl Pts',(32.4361538938655,20.7227952352634,40.5771993174102));
#67740=CARTESIAN_POINT('Ctrl Pts',(32.4440706137376,20.8045717503721,40.5814526845745));
#67741=CARTESIAN_POINT('Ctrl Pts',(32.4478690895806,20.8864783268449,40.5857060517388));
#67742=CARTESIAN_POINT('Ctrl Pts',(32.4516395773916,20.9677813970766,40.5899280791288));
#67743=CARTESIAN_POINT('Ctrl Pts',(32.4513523716402,21.0492121488906,40.5941501065187));
#67744=CARTESIAN_POINT('Ctrl Pts',(32.4470313278271,21.1303377559753,40.5983721339086));
#67745=CARTESIAN_POINT('Ctrl Pts',(32.4426621718658,21.2123666464792,40.6026411709602));
#67746=CARTESIAN_POINT('Ctrl Pts',(32.4341688424918,21.2940830691546,40.6069102080117));
#67747=CARTESIAN_POINT('Ctrl Pts',(32.4216294620063,21.3750479952526,40.6111792450632));
#67748=CARTESIAN_POINT('Ctrl Pts',(32.4090900815209,21.4560129213506,40.6154482821148));
#67749=CARTESIAN_POINT('Ctrl Pts',(32.3925048112666,21.5362258896395,40.6197173191663));
#67750=CARTESIAN_POINT('Ctrl Pts',(32.3720036253616,21.6152633999123,40.6239863562179));
#67751=CARTESIAN_POINT('Ctrl Pts',(32.3516847722065,21.6935979690641,40.6282174254529));
#67752=CARTESIAN_POINT('Ctrl Pts',(32.3274431624911,21.7710719222324,40.6324484946878));
#67753=CARTESIAN_POINT('Ctrl Pts',(32.2993683882583,21.8472633976979,40.6366795639228));
#67754=CARTESIAN_POINT('Ctrl Pts',(32.271333894159,21.9233455578475,40.6409045626537));
#67755=CARTESIAN_POINT('Ctrl Pts',(32.2394773175561,21.998148462118,40.6451295613845));
#67756=CARTESIAN_POINT('Ctrl Pts',(32.2039386288593,22.0712631657168,40.6493545601153));
#67757=CARTESIAN_POINT('Ctrl Pts',(32.1682944834485,22.1445948282604,40.6535920960133));
#67758=CARTESIAN_POINT('Ctrl Pts',(32.1289464627612,22.2162277990869,40.6578296319114));
#67759=CARTESIAN_POINT('Ctrl Pts',(32.0860853491656,22.2857675396418,40.6620671678094));
#67760=CARTESIAN_POINT('Ctrl Pts',(32.0434279946412,22.3549766925905,40.6662845587251));
#67761=CARTESIAN_POINT('Ctrl Pts',(31.997291114425,22.4221120705536,40.6705019496407));
#67762=CARTESIAN_POINT('Ctrl Pts',(31.9479089595562,22.4868089774012,40.6747193405564));
#67763=CARTESIAN_POINT('Ctrl Pts',(31.898543128901,22.5514844974516,40.678935337333));
#67764=CARTESIAN_POINT('Ctrl Pts',(31.8459344358771,22.613722777839,40.6831513341096));
#67765=CARTESIAN_POINT('Ctrl Pts',(31.7903593722719,22.6731896390183,40.6873673308862));
#67766=CARTESIAN_POINT('Ctrl Pts',(31.734785651116,22.7326550637395,40.6915832258228));
#67767=CARTESIAN_POINT('Ctrl Pts',(31.6762460201253,22.7893488634034,40.6957991207595));
#67768=CARTESIAN_POINT('Ctrl Pts',(31.6150550428373,22.8429724519389,40.7000150156961));
#67769=CARTESIAN_POINT('Ctrl Pts',(31.553320180498,22.8970726641451,40.7042683828605));
#67770=CARTESIAN_POINT('Ctrl Pts',(31.48888695479,22.9480474844173,40.7085217500248));
#67771=CARTESIAN_POINT('Ctrl Pts',(31.4221123975052,22.9956318745856,40.7127751171892));
#67772=CARTESIAN_POINT('Ctrl Pts',(31.3558298503109,23.0428656521693,40.7169971445791));
#67773=CARTESIAN_POINT('Ctrl Pts',(31.2872407889696,23.0867585957071,40.721219171969));
#67774=CARTESIAN_POINT('Ctrl Pts',(31.2167218847191,23.1270961673713,40.7254411993589));
#67775=CARTESIAN_POINT('Ctrl Pts',(31.1454177961193,23.167882872928,40.7297102364105));
#67776=CARTESIAN_POINT('Ctrl Pts',(31.0721410583789,23.2050343208802,40.7339792734621));
#67777=CARTESIAN_POINT('Ctrl Pts',(30.9973029670206,23.2383782169178,40.7382483105136));
#67778=CARTESIAN_POINT('Ctrl Pts',(30.9224648756623,23.2717221129554,40.7425173475652));
#67779=CARTESIAN_POINT('Ctrl Pts',(30.846065905745,23.3012583426877,40.7467863846168));
#67780=CARTESIAN_POINT('Ctrl Pts',(30.7685324057423,23.3268666036806,40.7510554216683));
#67781=CARTESIAN_POINT('Ctrl Pts',(30.691688470543,23.3522471107934,40.7552864909035));
#67782=CARTESIAN_POINT('Ctrl Pts',(30.6134417082201,23.3738645400482,40.7595175601386));
#67783=CARTESIAN_POINT('Ctrl Pts',(30.5341952037729,23.3915655404496,40.7637486293738));
#67784=CARTESIAN_POINT('Ctrl Pts',(30.4550623978283,23.4092411444344,40.7679736281047));
#67785=CARTESIAN_POINT('Ctrl Pts',(30.3749331484721,23.4230113789361,40.7721986268357));
#67786=CARTESIAN_POINT('Ctrl Pts',(30.294226989835,23.4327722311085,40.7764236255667));
#67787=CARTESIAN_POINT('Ctrl Pts',(30.2132813455421,23.442562047416,40.7806611614647));
#67788=CARTESIAN_POINT('Ctrl Pts',(30.1317558131787,23.448318505887,40.7848986973627));
#67789=CARTESIAN_POINT('Ctrl Pts',(30.050085359408,23.4499881033942,40.7891362332607));
#67790=CARTESIAN_POINT('Ctrl Pts',(29.9688031618969,23.4516497637386,40.7933536241765));
#67791=CARTESIAN_POINT('Ctrl Pts',(29.8873778859494,23.4492633170818,40.7975710150923));
#67792=CARTESIAN_POINT('Ctrl Pts',(29.8062429784239,23.4428279650008,40.8017884060081));
#67793=CARTESIAN_POINT('Ctrl Pts',(29.7251348915903,23.4363947402483,40.8060044027848));
#67794=CARTESIAN_POINT('Ctrl Pts',(29.6443174457049,23.4259153047548,40.8102203995616));
#67795=CARTESIAN_POINT('Ctrl Pts',(29.5642213357481,23.4114408982562,40.8144363963384));
#67796=CARTESIAN_POINT('Ctrl Pts',(29.4841271605615,23.3969668413957,40.8186522912752));
#67797=CARTESIAN_POINT('Ctrl Pts',(29.4047547440148,23.3784980891681,40.822868186212));
#67798=CARTESIAN_POINT('Ctrl Pts',(29.3265255031183,23.3561371674947,40.8270840811488));
#67799=CARTESIAN_POINT('Ctrl Pts',(29.2476009356196,23.3335774947723,40.8313374483129));
#67800=CARTESIAN_POINT('Ctrl Pts',(29.1698404344567,23.3070562328267,40.8355908154771));
#67801=CARTESIAN_POINT('Ctrl Pts',(29.0936602405861,23.2767297798609,40.8398441826413));
#67802=CARTESIAN_POINT('Ctrl Pts',(29.0180413596646,23.2466267790798,40.8440662100313));
#67803=CARTESIAN_POINT('Ctrl Pts',(28.943979976671,23.2127747277735,40.8482882374214));
#67804=CARTESIAN_POINT('Ctrl Pts',(28.8718605369971,23.1753738993597,40.8525102648114));
#67805=CARTESIAN_POINT('Ctrl Pts',(28.7989380920113,23.1375566358762,40.8567793018627));
#67806=CARTESIAN_POINT('Ctrl Pts',(28.7280015249602,23.0961113245285,40.8610483389139));
#67807=CARTESIAN_POINT('Ctrl Pts',(28.6594185461734,23.0512902319409,40.8653173759651));
#67808=CARTESIAN_POINT('Ctrl Pts',(28.5908355673866,23.0064691393533,40.8695864130163));
#67809=CARTESIAN_POINT('Ctrl Pts',(28.5246065304716,22.9582726027613,40.8738554500675));
#67810=CARTESIAN_POINT('Ctrl Pts',(28.4610636109115,22.9069937179601,40.8781244871188));
#67811=CARTESIAN_POINT('Ctrl Pts',(28.3988991871278,22.8568272737991,40.8823009119704));
#67812=CARTESIAN_POINT('Ctrl Pts',(28.3390590737905,22.8035117847631,40.8864773368221));
#67813=CARTESIAN_POINT('Ctrl Pts',(28.2818859516553,22.7472934404045,40.8906537616738));
#67814=CARTESIAN_POINT('Ctrl Pts',(28.2242653283127,22.690635068004,40.8948628759274));
#67815=CARTESIAN_POINT('Ctrl Pts',(28.1693540614958,22.6310284373932,40.8990719901809));
#67816=CARTESIAN_POINT('Ctrl Pts',(28.1174713076324,22.568768935316,40.9032811044344));
#67817=CARTESIAN_POINT('Ctrl Pts',(28.0661251752047,22.5071533810039,40.9074466839723));
#67818=CARTESIAN_POINT('Ctrl Pts',(28.0177455279077,22.4429399392236,40.9116122635103));
#67819=CARTESIAN_POINT('Ctrl Pts',(27.9726054180359,22.3764524906521,40.9157778430482));
#67820=CARTESIAN_POINT('Ctrl Pts',(27.9274926432361,22.3100053042598,40.9199409000753));
#67821=CARTESIAN_POINT('Ctrl Pts',(27.8856157817235,22.2412872376611,40.9241039571024));
#67822=CARTESIAN_POINT('Ctrl Pts',(27.8472064165828,22.1706536794449,40.9282670141295));
#67823=CARTESIAN_POINT('Ctrl Pts',(27.8088078168249,22.1000399184133,40.9324289043343));
#67824=CARTESIAN_POINT('Ctrl Pts',(27.7738750118051,22.0275121516492,40.9365907945391));
#67825=CARTESIAN_POINT('Ctrl Pts',(27.7425943696033,21.9534516609945,40.9407526847439));
#67826=CARTESIAN_POINT('Ctrl Pts',(27.7107017166422,21.8779421650148,40.9449960029952));
#67827=CARTESIAN_POINT('Ctrl Pts',(27.6826058921223,21.8008397889873,40.9492393212464));
#67828=CARTESIAN_POINT('Ctrl Pts',(27.6584528198875,21.7225697567066,40.9534826394976));
#67829=CARTESIAN_POINT('Ctrl Pts',(27.6347410320592,21.645729743117,40.9576484309581));
#67830=CARTESIAN_POINT('Ctrl Pts',(27.6148291982902,21.5677648703724,40.9618142224187));
#67831=CARTESIAN_POINT('Ctrl Pts',(27.5988043145566,21.4890905133083,40.9659800138792));
#67832=CARTESIAN_POINT('Ctrl Pts',(27.5823320880484,21.4082199215771,40.9702620955257));
#67833=CARTESIAN_POINT('Ctrl Pts',(27.5699671547341,21.3266001775221,40.9745441771723));
#67834=CARTESIAN_POINT('Ctrl Pts',(27.5617470040674,21.2446887366138,40.9788262588189));
#67835=CARTESIAN_POINT('Ctrl Pts',(27.5535268534007,21.1627772957055,40.9831083404655));
#67836=CARTESIAN_POINT('Ctrl Pts',(27.5494514478907,21.0805747024057,40.9873904221121));
#67837=CARTESIAN_POINT('Ctrl Pts',(27.5495004369098,20.998536683703,40.9916725037586));
#67838=CARTESIAN_POINT('',(27.5495009231109,21.0021270086603,41.7916725038169));
#67839=CARTESIAN_POINT('Ctrl Pts',(27.5495004369101,20.9985366831405,40.991672503788));
#67840=CARTESIAN_POINT('Ctrl Pts',(27.5495519993063,20.912189267378,40.9961795200484));
#67841=CARTESIAN_POINT('Ctrl Pts',(27.5541671351712,20.8259795206028,41.0006865363089));
#67842=CARTESIAN_POINT('Ctrl Pts',(27.5633043849036,20.7402602660931,41.0051935525694));
#67843=CARTESIAN_POINT('Ctrl Pts',(27.5718821964757,20.6597892671807,41.0094246218043));
#67844=CARTESIAN_POINT('Ctrl Pts',(27.5844666777454,20.5795926345089,41.0136556910392));
#67845=CARTESIAN_POINT('Ctrl Pts',(27.6010312510458,20.5001008186231,41.0178867602741));
#67846=CARTESIAN_POINT('Ctrl Pts',(27.6175720584124,20.4207230531991,41.0221117590048));
#67847=CARTESIAN_POINT('Ctrl Pts',(27.6380815224783,20.3420485475221,41.0263367577355));
#67848=CARTESIAN_POINT('Ctrl Pts',(27.6624813353646,20.2645023844489,41.0305617564662));
#67849=CARTESIAN_POINT('Ctrl Pts',(27.6869535517137,20.1867261126142,41.0347992923643));
#67850=CARTESIAN_POINT('Ctrl Pts',(27.7153391862825,20.1100853598019,41.0390368282624));
#67851=CARTESIAN_POINT('Ctrl Pts',(27.7475075530817,20.0349984318273,41.0432743641604));
#67852=CARTESIAN_POINT('Ctrl Pts',(27.7795229934625,19.9602684624459,41.047491755076));
#67853=CARTESIAN_POINT('Ctrl Pts',(27.8152851026761,19.8870780106468,41.0517091459915));
#67854=CARTESIAN_POINT('Ctrl Pts',(27.8546158099747,19.815822256927,41.055926536907));
#67855=CARTESIAN_POINT('Ctrl Pts',(27.8939335157574,19.7445900581565,41.0601425336835));
#67856=CARTESIAN_POINT('Ctrl Pts',(27.9368172524685,19.67529169416,41.06435853046));
#67857=CARTESIAN_POINT('Ctrl Pts',(27.9830426800296,19.6082983727042,41.0685745272364));
#67858=CARTESIAN_POINT('Ctrl Pts',(28.0292669909874,19.5413066695127,41.072790422173));
#67859=CARTESIAN_POINT('Ctrl Pts',(28.0788325673311,19.4766202802318,41.0770063171095));
#67860=CARTESIAN_POINT('Ctrl Pts',(28.1314721766981,19.4145808051034,41.081222212046));
#67861=CARTESIAN_POINT('Ctrl Pts',(28.1845796638163,19.3519899031984,41.0854755792104));
#67862=CARTESIAN_POINT('Ctrl Pts',(28.240815804874,19.2920935818062,41.0897289463749));
#67863=CARTESIAN_POINT('Ctrl Pts',(28.2998664273511,19.2352065035387,41.0939823135394));
#67864=CARTESIAN_POINT('Ctrl Pts',(28.3584819514384,19.1787385821762,41.0982043409291));
#67865=CARTESIAN_POINT('Ctrl Pts',(28.4198702243352,19.1252359674877,41.1024263683189));
#67866=CARTESIAN_POINT('Ctrl Pts',(28.4836902208801,19.0749662590631,41.1066483957087));
#67867=CARTESIAN_POINT('Ctrl Pts',(28.5482208135895,19.0241368285462,41.1109174327605));
#67868=CARTESIAN_POINT('Ctrl Pts',(28.6152372189881,18.9766130262241,41.1151864698123));
#67869=CARTESIAN_POINT('Ctrl Pts',(28.6843579516364,18.9326257594287,41.1194555068642));
#67870=CARTESIAN_POINT('Ctrl Pts',(28.7534786842848,18.8886384926333,41.123724543916));
#67871=CARTESIAN_POINT('Ctrl Pts',(28.8247032911121,18.8481879443753,41.1279935809678));
#67872=CARTESIAN_POINT('Ctrl Pts',(28.8976277513153,18.8114558091439,41.1322626180197));
#67873=CARTESIAN_POINT('Ctrl Pts',(28.9699036384469,18.7750503609214,41.1364936872557));
#67874=CARTESIAN_POINT('Ctrl Pts',(29.0441205094844,18.742160771114,41.1407247564917));
#67875=CARTESIAN_POINT('Ctrl Pts',(29.1199022143788,18.712998002243,41.1449558257277));
#67876=CARTESIAN_POINT('Ctrl Pts',(29.1955751918736,18.6838770745001,41.1491808244596));
#67877=CARTESIAN_POINT('Ctrl Pts',(29.2728081139551,18.658472513689,41.1534058231914));
#67878=CARTESIAN_POINT('Ctrl Pts',(29.3512013044756,18.636948899688,41.1576308219233));
#67879=CARTESIAN_POINT('Ctrl Pts',(29.4298271171814,18.6153614170003,41.161868357821));
#67880=CARTESIAN_POINT('Ctrl Pts',(29.5096196706376,18.5976781578755,41.1661058937188));
#67881=CARTESIAN_POINT('Ctrl Pts',(29.5901565958493,18.5840160112132,41.1703434296166));
#67882=CARTESIAN_POINT('Ctrl Pts',(29.6703106535468,18.5704188135431,41.1745608205333));
#67883=CARTESIAN_POINT('Ctrl Pts',(29.7512015607937,18.560804666775,41.17877821145));
#67884=CARTESIAN_POINT('Ctrl Pts',(29.8324007009626,18.5552381046486,41.1829956023667));
#67885=CARTESIAN_POINT('Ctrl Pts',(29.9135729992062,18.5496733826555,41.1872115991444));
#67886=CARTESIAN_POINT('Ctrl Pts',(29.9950528645208,18.5481536199984,41.191427595922));
#67887=CARTESIAN_POINT('Ctrl Pts',(30.0764067493481,18.5506914733635,41.1956435926997));
#67888=CARTESIAN_POINT('Ctrl Pts',(30.1577586690228,18.5532292654253,41.1998594876374));
#67889=CARTESIAN_POINT('Ctrl Pts',(30.238984149559,18.5598244630332,41.2040753825751));
#67890=CARTESIAN_POINT('Ctrl Pts',(30.3196512781898,18.57043762987,41.2082912775127));
#67891=CARTESIAN_POINT('Ctrl Pts',(30.4010354021145,18.5811451299354,41.2125446446759));
#67892=CARTESIAN_POINT('Ctrl Pts',(30.4818507196718,18.5959423364578,41.216798011839));
#67893=CARTESIAN_POINT('Ctrl Pts',(30.561662515251,18.614735765379,41.2210513790021));
#67894=CARTESIAN_POINT('Ctrl Pts',(30.6408862394515,18.6333907200613,41.2252734063931));
#67895=CARTESIAN_POINT('Ctrl Pts',(30.719120746844,18.6559830126456,41.229495433784));
#67896=CARTESIAN_POINT('Ctrl Pts',(30.7959563192517,18.682371084957,41.233717461175));
#67897=CARTESIAN_POINT('Ctrl Pts',(30.8736474081375,18.709052972099,41.2379864982242));
#67898=CARTESIAN_POINT('Ctrl Pts',(30.9499077629167,18.7396155089754,41.2422555352734));
#67899=CARTESIAN_POINT('Ctrl Pts',(31.0243365722403,18.773863248412,41.2465245723226));
#67900=CARTESIAN_POINT('Ctrl Pts',(31.0987653815639,18.8081109878485,41.2507936093719));
#67901=CARTESIAN_POINT('Ctrl Pts',(31.171362246074,18.846043648279,41.2550626464211));
#67902=CARTESIAN_POINT('Ctrl Pts',(31.2417554984415,18.8874201714277,41.2593316834703));
#67903=CARTESIAN_POINT('Ctrl Pts',(31.3115226897067,18.9284287014689,41.2635627527037));
#67904=CARTESIAN_POINT('Ctrl Pts',(31.3793871825405,18.9729739556384,41.2677938219371));
#67905=CARTESIAN_POINT('Ctrl Pts',(31.444967818672,19.0208541607546,41.2720248911705));
#67906=CARTESIAN_POINT('Ctrl Pts',(31.5104543633331,19.0686656700002,41.2762498898998));
#67907=CARTESIAN_POINT('Ctrl Pts',(31.5736631867936,19.1198023553884,41.280474888629));
#67908=CARTESIAN_POINT('Ctrl Pts',(31.6342393593733,19.1740175339628,41.2846998873582));
#67909=CARTESIAN_POINT('Ctrl Pts',(31.6949952843682,19.2283935894773,41.2889374232567));
#67910=CARTESIAN_POINT('Ctrl Pts',(31.7531025048827,19.2858661931019,41.2931749591551));
#67911=CARTESIAN_POINT('Ctrl Pts',(31.8082338709465,19.3461437432589,41.2974124950535));
#67912=CARTESIAN_POINT('Ctrl Pts',(31.8631031458958,19.4061347376594,41.3016298859676));
#67913=CARTESIAN_POINT('Ctrl Pts',(31.9150244759364,19.468903728195,41.3058472768817));
#67914=CARTESIAN_POINT('Ctrl Pts',(31.963711323602,19.5341254871043,41.3100646677958));
#67915=CARTESIAN_POINT('Ctrl Pts',(32.0123820769012,19.5993256857168,41.3142806645709));
#67916=CARTESIAN_POINT('Ctrl Pts',(32.057820193218,19.6669766702517,41.3184966613459));
#67917=CARTESIAN_POINT('Ctrl Pts',(32.0997800594278,19.7367209524301,41.322712658121));
#67918=CARTESIAN_POINT('Ctrl Pts',(32.1417389120718,19.8064635498931,41.3269285530561));
#67919=CARTESIAN_POINT('Ctrl Pts',(32.1802194429077,19.8782989454798,41.3311444479912));
#67920=CARTESIAN_POINT('Ctrl Pts',(32.2150207031626,19.9518427911037,41.3353603429263));
#67921=CARTESIAN_POINT('Ctrl Pts',(32.2501312882196,20.0260403180981,41.3396137100925));
#67922=CARTESIAN_POINT('Ctrl Pts',(32.2814966494339,20.1019763898893,41.3438670772587));
#67923=CARTESIAN_POINT('Ctrl Pts',(32.3089597399857,20.1792350098078,41.3481204444249));
#67924=CARTESIAN_POINT('Ctrl Pts',(32.3362204762329,20.2559243706229,41.3523424718133));
#67925=CARTESIAN_POINT('Ctrl Pts',(32.3596361808314,20.333916386892,41.3565644992017));
#67926=CARTESIAN_POINT('Ctrl Pts',(32.3791037561101,20.4127900139962,41.3607865265902));
#67927=CARTESIAN_POINT('Ctrl Pts',(32.3987880908128,20.4925418502114,41.3650555636453));
#67928=CARTESIAN_POINT('Ctrl Pts',(32.414435737801,20.5731945720105,41.3693246007004));
#67929=CARTESIAN_POINT('Ctrl Pts',(32.4259937144277,20.65430541289,41.3735936377554));
#67930=CARTESIAN_POINT('Ctrl Pts',(32.4375516910545,20.7354162537694,41.3778626748105));
#67931=CARTESIAN_POINT('Ctrl Pts',(32.4450200174982,20.8169847255092,41.3821317118656));
#67932=CARTESIAN_POINT('Ctrl Pts',(32.4483998377637,20.8985678333135,41.3864007489207));
#67933=CARTESIAN_POINT('Ctrl Pts',(32.4517495986954,20.9794253599701,41.3906318181552));
#67934=CARTESIAN_POINT('Ctrl Pts',(32.4510959048197,21.0606007364284,41.3948628873896));
#67935=CARTESIAN_POINT('Ctrl Pts',(32.4464017414766,21.1416642837855,41.3990939566241));
#67936=CARTESIAN_POINT('Ctrl Pts',(32.4417143130594,21.222611525647,41.4033189553543));
#67937=CARTESIAN_POINT('Ctrl Pts',(32.4329979551542,21.3034467968029,41.4075439540846));
#67938=CARTESIAN_POINT('Ctrl Pts',(32.4202676102448,21.3837381200763,41.4117689528148));
#67939=CARTESIAN_POINT('Ctrl Pts',(32.4074994895911,21.4642676980495,41.416006488713));
#67940=CARTESIAN_POINT('Ctrl Pts',(32.3906935079778,21.5442496224051,41.4202440246112));
#67941=CARTESIAN_POINT('Ctrl Pts',(32.3699174131512,21.6232509164394,41.4244815605094));
#67942=CARTESIAN_POINT('Ctrl Pts',(32.3492400865923,21.7018766432162,41.4286989514244));
#67943=CARTESIAN_POINT('Ctrl Pts',(32.3246304221739,21.7795305877749,41.4329163423395));
#67944=CARTESIAN_POINT('Ctrl Pts',(32.2962064380711,21.8557956787463,41.4371337332545));
#67945=CARTESIAN_POINT('Ctrl Pts',(32.2677918500587,21.9320355588364,41.4413497300305));
#67946=CARTESIAN_POINT('Ctrl Pts',(32.2355656085661,22.0068870617242,41.4455657268065));
#67947=CARTESIAN_POINT('Ctrl Pts',(32.1996950235204,22.079950023612,41.4497817235825));
#67948=CARTESIAN_POINT('Ctrl Pts',(32.1638253049505,22.1530112206193,41.4539976185185));
#67949=CARTESIAN_POINT('Ctrl Pts',(32.1243116237569,22.2242835456374,41.4582135134545));
#67950=CARTESIAN_POINT('Ctrl Pts',(32.0813680699598,22.2933898126056,41.4624294083905));
#67951=CARTESIAN_POINT('Ctrl Pts',(32.0380428200558,22.3631103182832,41.4666827755556));
#67952=CARTESIAN_POINT('Ctrl Pts',(31.9912266605584,22.4306256505362,41.4709361427207));
#67953=CARTESIAN_POINT('Ctrl Pts',(31.9411840727999,22.4955783648837,41.4751895098857));
#67954=CARTESIAN_POINT('Ctrl Pts',(31.8915102101996,22.560052492872,41.479411537275));
#67955=CARTESIAN_POINT('Ctrl Pts',(31.8386576596229,22.6220013243684,41.4836335646642));
#67956=CARTESIAN_POINT('Ctrl Pts',(31.7829243843073,22.6811100171739,41.4878555920535));
#67957=CARTESIAN_POINT('Ctrl Pts',(31.7265705534414,22.7408768487159,41.4921246291065));
#67958=CARTESIAN_POINT('Ctrl Pts',(31.6672718021908,22.7977395648272,41.4963936661594));
#67959=CARTESIAN_POINT('Ctrl Pts',(31.6053715102256,22.8514136664063,41.5006627032124));
#67960=CARTESIAN_POINT('Ctrl Pts',(31.5434712182605,22.9050877679853,41.5049317402654));
#67961=CARTESIAN_POINT('Ctrl Pts',(31.4789698068114,22.9555730073813,41.5092007773183));
#67962=CARTESIAN_POINT('Ctrl Pts',(31.4122401832769,23.0026302491319,41.5134698143713));
#67963=CARTESIAN_POINT('Ctrl Pts',(31.3461040372992,23.0492689748563,41.5177008836141));
#67964=CARTESIAN_POINT('Ctrl Pts',(31.277530958774,23.0927155165667,41.5219319528568));
#67965=CARTESIAN_POINT('Ctrl Pts',(31.2068619831371,23.1327058877535,41.5261630220996));
#67966=CARTESIAN_POINT('Ctrl Pts',(31.1362943994381,23.1726388829673,41.5303880208382));
#67967=CARTESIAN_POINT('Ctrl Pts',(31.0636372921346,23.2091253289662,41.5346130195768));
#67968=CARTESIAN_POINT('Ctrl Pts',(30.9892617881354,23.2419436577522,41.5388380183154));
#67969=CARTESIAN_POINT('Ctrl Pts',(30.9146655840924,23.2748593708409,41.5430755542115));
#67970=CARTESIAN_POINT('Ctrl Pts',(30.8383411582727,23.3040848949014,41.5473130901076));
#67971=CARTESIAN_POINT('Ctrl Pts',(30.7606890972723,23.329442497099,41.5515506260037));
#67972=CARTESIAN_POINT('Ctrl Pts',(30.683406189167,23.3546795508895,41.5557680169272));
#67973=CARTESIAN_POINT('Ctrl Pts',(30.6048086837415,23.3760852242856,41.5599854078507));
#67974=CARTESIAN_POINT('Ctrl Pts',(30.5253110468039,23.3935326515646,41.5642027987741));
#67975=CARTESIAN_POINT('Ctrl Pts',(30.4458396893275,23.4109743112635,41.5684187955585));
#67976=CARTESIAN_POINT('Ctrl Pts',(30.3654692450358,23.4244602236845,41.5726347923429));
#67977=CARTESIAN_POINT('Ctrl Pts',(30.2846266862501,23.4339141109485,41.5768507891273));
#67978=CARTESIAN_POINT('Ctrl Pts',(30.2037860802659,23.4433677698481,41.5810666840717));
#67979=CARTESIAN_POINT('Ctrl Pts',(30.1224738444053,23.4487895443275,41.5852825790161));
#67980=CARTESIAN_POINT('Ctrl Pts',(30.0411229949267,23.450154923528,41.5894984739605));
#67981=CARTESIAN_POINT('Ctrl Pts',(29.9590490733099,23.4515324386515,41.5937518411156));
#67982=CARTESIAN_POINT('Ctrl Pts',(29.876936328975,23.4487810638216,41.5980052082707));
#67983=CARTESIAN_POINT('Ctrl Pts',(29.7952284989678,23.4419293360712,41.6022585754258));
#67984=CARTESIAN_POINT('Ctrl Pts',(29.7141227104706,23.4351280933785,41.6064806028234));
#67985=CARTESIAN_POINT('Ctrl Pts',(29.6334163464032,23.4242868457514,41.6107026302209));
#67986=CARTESIAN_POINT('Ctrl Pts',(29.5535354881006,23.4094853578336,41.6149246576184));
#67987=CARTESIAN_POINT('Ctrl Pts',(29.4727652063653,23.3945190645985,41.6191936946523));
#67988=CARTESIAN_POINT('Ctrl Pts',(29.3928394025217,23.3755039074134,41.6234627316862));
#67989=CARTESIAN_POINT('Ctrl Pts',(29.3141832729915,23.3525742638555,41.6277317687201));
#67990=CARTESIAN_POINT('Ctrl Pts',(29.2355271434614,23.3296446202977,41.632000805754));
#67991=CARTESIAN_POINT('Ctrl Pts',(29.1581411246682,23.3028007101411,41.6362698427879));
#67992=CARTESIAN_POINT('Ctrl Pts',(29.0824282935996,23.2722263121471,41.6405388798218));
#67993=CARTESIAN_POINT('Ctrl Pts',(29.0073888346806,23.2419238356729,41.6447699490422));
#67994=CARTESIAN_POINT('Ctrl Pts',(28.9337112650968,23.207843272893,41.6490010182627));
#67995=CARTESIAN_POINT('Ctrl Pts',(28.8618022722028,23.1701281488514,41.6532320874831));
#67996=CARTESIAN_POINT('Ctrl Pts',(28.7899964503554,23.1324671363842,41.6574570861995));
#67997=CARTESIAN_POINT('Ctrl Pts',(28.7199545739187,23.0911821334844,41.6616820849158));
#67998=CARTESIAN_POINT('Ctrl Pts',(28.652063991403,23.0464649439283,41.6659070836321));
#67999=CARTESIAN_POINT('Ctrl Pts',(28.5839719515911,23.0016150613865,41.6701446195337));
#68000=CARTESIAN_POINT('Ctrl Pts',(28.5180444295562,22.9533127726564,41.6743821554354));
#68001=CARTESIAN_POINT('Ctrl Pts',(28.4546479020158,22.9017983971115,41.6786196913371));
#68002=CARTESIAN_POINT('Ctrl Pts',(28.3915527578972,22.8505289179257,41.6828370822384));
#68003=CARTESIAN_POINT('Ctrl Pts',(28.3309649655752,22.7960781137796,41.6870544731397));
#68004=CARTESIAN_POINT('Ctrl Pts',(28.2732157760017,22.7387255372113,41.691271864041));
#68005=CARTESIAN_POINT('Ctrl Pts',(28.2154856765237,22.6813919196304,41.6954878608034));
#68006=CARTESIAN_POINT('Ctrl Pts',(28.1605926460114,22.6211587619126,41.6997038575658));
#68007=CARTESIAN_POINT('Ctrl Pts',(28.1088322003689,22.5583435448059,41.7039198543281));
#68008=CARTESIAN_POINT('Ctrl Pts',(28.0570730050299,22.4955298450372,41.7081357492506));
#68009=CARTESIAN_POINT('Ctrl Pts',(28.008446538943,22.4301345694235,41.7123516441731));
#68010=CARTESIAN_POINT('Ctrl Pts',(27.9632080893745,22.3625083349508,41.7165675390956));
#68011=CARTESIAN_POINT('Ctrl Pts',(27.9175675456066,22.2942810162927,41.720820906277));
#68012=CARTESIAN_POINT('Ctrl Pts',(27.8753758287363,22.223783271918,41.7250742734584));
#68013=CARTESIAN_POINT('Ctrl Pts',(27.8368494557566,22.1514034796453,41.7293276406398));
#68014=CARTESIAN_POINT('Ctrl Pts',(27.7986069541128,22.0795569986277,41.733549668016));
#68015=CARTESIAN_POINT('Ctrl Pts',(27.7639761051277,22.0058565638607,41.7377716953922));
#68016=CARTESIAN_POINT('Ctrl Pts',(27.7331208055899,21.9307034801432,41.7419937227684));
#68017=CARTESIAN_POINT('Ctrl Pts',(27.7019219510522,21.8547136125324,41.7462627598523));
#68018=CARTESIAN_POINT('Ctrl Pts',(27.6745834069441,21.777239007102,41.7505317969363));
#68019=CARTESIAN_POINT('Ctrl Pts',(27.6512226944134,21.6987098244344,41.7548008340203));
#68020=CARTESIAN_POINT('Ctrl Pts',(27.6278619818826,21.6201806417669,41.7590698711043));
#68021=CARTESIAN_POINT('Ctrl Pts',(27.6084791527692,21.5405973677416,41.7633389081883));
#68022=CARTESIAN_POINT('Ctrl Pts',(27.5931382236528,21.4603983487793,41.7676079452723));
#68023=CARTESIAN_POINT('Ctrl Pts',(27.5707299436689,21.3432527666765,41.773843667862));
#68024=CARTESIAN_POINT('Ctrl Pts',(27.5568689197519,21.2244236305085,41.7800793904518));
#68025=CARTESIAN_POINT('Ctrl Pts',(27.5517475311304,21.1049290173105,41.7863151130416));
#68026=CARTESIAN_POINT('Ctrl Pts',(27.5502808590853,21.0707079453196,41.7881009099571));
#68027=CARTESIAN_POINT('Ctrl Pts',(27.5495306999149,21.036432469201,41.7898867068725));
#68028=CARTESIAN_POINT('Ctrl Pts',(27.5495009231114,21.0021270092151,41.791672503788));
#68029=CARTESIAN_POINT('',(27.5495000081341,21.0001996626194,42.5916725037481));
#68030=CARTESIAN_POINT('Ctrl Pts',(27.5495009231109,21.0021270086603,41.7916725038169));
#68031=CARTESIAN_POINT('Ctrl Pts',(27.5494293597252,20.9196797606114,41.7959643582713));
#68032=CARTESIAN_POINT('Ctrl Pts',(27.5535234877986,20.837092575959,41.8002562127257));
#68033=CARTESIAN_POINT('Ctrl Pts',(27.5617955596507,20.7548279031765,41.8045480671801));
#68034=CARTESIAN_POINT('Ctrl Pts',(27.5698087291806,20.6751379801294,41.8087055936083));
#68035=CARTESIAN_POINT('Ctrl Pts',(27.5817421408007,20.5957511991929,41.8128631200365));
#68036=CARTESIAN_POINT('Ctrl Pts',(27.5975541099105,20.5170880047132,41.8170206464647));
#68037=CARTESIAN_POINT('Ctrl Pts',(27.6133577590071,20.4384662015873,41.8211759852669));
#68038=CARTESIAN_POINT('Ctrl Pts',(27.6330358229658,20.3605676992317,41.8253313240692));
#68039=CARTESIAN_POINT('Ctrl Pts',(27.6564951166518,20.2838051161009,41.8294866628714));
#68040=CARTESIAN_POINT('Ctrl Pts',(27.6799497481538,20.2070577883864,41.8336411758621));
#68041=CARTESIAN_POINT('Ctrl Pts',(27.7071839769369,20.1314463904358,41.8377956888529));
#68042=CARTESIAN_POINT('Ctrl Pts',(27.7380545492334,20.0573690925095,41.8419502018436));
#68043=CARTESIAN_POINT('Ctrl Pts',(27.768929095014,19.9832822597759,41.8461052495795));
#68044=CARTESIAN_POINT('Ctrl Pts',(27.8034407258317,19.9107303607031,41.8502602973155));
#68045=CARTESIAN_POINT('Ctrl Pts',(27.8413984224977,19.8400907450992,41.8544153450514));
#68046=CARTESIAN_POINT('Ctrl Pts',(27.8793960608656,19.7693767976281,41.8585747650147));
#68047=CARTESIAN_POINT('Ctrl Pts',(27.9208467696119,19.7005795699702,41.862734184978));
#68048=CARTESIAN_POINT('Ctrl Pts',(27.9655144623797,19.6340502032601,41.8668936049412));
#68049=CARTESIAN_POINT('Ctrl Pts',(28.0102106244738,19.5674784335036,41.8710556759455));
#68050=CARTESIAN_POINT('Ctrl Pts',(28.0581275598252,19.5031777817647,41.8752177469497));
#68051=CARTESIAN_POINT('Ctrl Pts',(28.1089884823503,19.4414668145605,41.879379817954));
#68052=CARTESIAN_POINT('Ctrl Pts',(28.1599291773465,19.3796590572058,41.8835484169304));
#68053=CARTESIAN_POINT('Ctrl Pts',(28.2138227429899,19.3204494349801,41.8877170159069));
#68054=CARTESIAN_POINT('Ctrl Pts',(28.2703557697157,19.2641195068081,41.8918856148834));
#68055=CARTESIAN_POINT('Ctrl Pts',(28.282974402217,19.2515462075599,41.8928160801632));
#68056=CARTESIAN_POINT('Ctrl Pts',(28.2957244110023,19.2391162178597,41.8937465454429));
#68057=CARTESIAN_POINT('Ctrl Pts',(28.3086021002813,19.2268323838883,41.8946770107227));
#68058=CARTESIAN_POINT('Ctrl Pts',(28.3671603257765,19.1709745739927,41.8989080800154));
#68059=CARTESIAN_POINT('Ctrl Pts',(28.4285984395889,19.1179158573553,41.9031391493081));
#68060=CARTESIAN_POINT('Ctrl Pts',(28.4926179369572,19.0679675038921,41.9073702186008));
#68061=CARTESIAN_POINT('Ctrl Pts',(28.5565455826954,19.0180908135609,41.9115952173895));
#68062=CARTESIAN_POINT('Ctrl Pts',(28.6230468928422,18.9713159070137,41.9158202161782));
#68063=CARTESIAN_POINT('Ctrl Pts',(28.6917873601505,18.9279165222082,41.920045214967));
#68064=CARTESIAN_POINT('Ctrl Pts',(28.7607318052119,18.8843883557789,41.9242827508506));
#68065=CARTESIAN_POINT('Ctrl Pts',(28.8319283715699,18.8442560979162,41.9285202867341));
#68066=CARTESIAN_POINT('Ctrl Pts',(28.9050069660881,18.8077544604483,41.9327578226177));
#68067=CARTESIAN_POINT('Ctrl Pts',(28.9777381507575,18.7714263488731,41.9369752135915));
#68068=CARTESIAN_POINT('Ctrl Pts',(29.0523330936432,18.738694631029,41.9411926045652));
#68069=CARTESIAN_POINT('Ctrl Pts',(29.1284004926172,18.709745745833,41.9454099955389));
#68070=CARTESIAN_POINT('Ctrl Pts',(29.20444274606,18.6808064302437,41.9496259923735));
#68071=CARTESIAN_POINT('Ctrl Pts',(29.2819560547665,18.655647629269,41.9538419892081));
#68072=CARTESIAN_POINT('Ctrl Pts',(29.3605293064773,18.6344075832626,41.9580579860427));
#68073=CARTESIAN_POINT('Ctrl Pts',(29.4391006602005,18.6131680503232,41.9622738810372));
#68074=CARTESIAN_POINT('Ctrl Pts',(29.5187314568824,18.5958472044146,41.9664897760316));
#68075=CARTESIAN_POINT('Ctrl Pts',(29.5989969930278,18.5825329705663,41.9707056710261));
#68076=CARTESIAN_POINT('Ctrl Pts',(29.6799759526077,18.5691003959344,41.9749590381217));
#68077=CARTESIAN_POINT('Ctrl Pts',(29.7616005197291,18.5597461088512,41.9792124052173));
#68078=CARTESIAN_POINT('Ctrl Pts',(29.8434275853269,18.5545071398666,41.9834657723129));
#68079=CARTESIAN_POINT('Ctrl Pts',(29.9246517329442,18.5493067726402,41.9876877997597));
#68080=CARTESIAN_POINT('Ctrl Pts',(30.0060749342987,18.5481612245314,41.9919098272065));
#68081=CARTESIAN_POINT('Ctrl Pts',(30.0872640103474,18.5510542589722,41.9961318546533));
#68082=CARTESIAN_POINT('Ctrl Pts',(30.169357072868,18.5539795054312,42.0004008915733));
#68083=CARTESIAN_POINT('Ctrl Pts',(30.2512102775175,18.5610337842884,42.0046699284933));
#68084=CARTESIAN_POINT('Ctrl Pts',(30.3323832890513,18.5721467097126,42.0089389654133));
#68085=CARTESIAN_POINT('Ctrl Pts',(30.4135563005851,18.5832596351368,42.0132080023333));
#68086=CARTESIAN_POINT('Ctrl Pts',(30.4940486550042,18.5984310539254,42.0174770392533));
#68087=CARTESIAN_POINT('Ctrl Pts',(30.5734346309067,18.6175384632534,42.0217460761733));
#68088=CARTESIAN_POINT('Ctrl Pts',(30.6521145665756,18.6364759357684,42.0259771452811));
#68089=CARTESIAN_POINT('Ctrl Pts',(30.7300030373767,18.6593506992851,42.0302082143889));
#68090=CARTESIAN_POINT('Ctrl Pts',(30.8066766706075,18.6860805979685,42.0344392834967));
#68091=CARTESIAN_POINT('Ctrl Pts',(30.8832402967475,18.7127721460709,42.0386642821004));
#68092=CARTESIAN_POINT('Ctrl Pts',(30.9585921116628,18.7433076923567,42.0428892807042));
#68093=CARTESIAN_POINT('Ctrl Pts',(31.0323207712093,18.7775544831583,42.0471142793079));
#68094=CARTESIAN_POINT('Ctrl Pts',(31.1062682143186,18.8119028984157,42.0513518152377));
#68095=CARTESIAN_POINT('Ctrl Pts',(31.1785823954215,18.8499845028644,42.0555893511676));
#68096=CARTESIAN_POINT('Ctrl Pts',(31.2488654803406,18.8916154852557,42.0598268870974));
#68097=CARTESIAN_POINT('Ctrl Pts',(31.3188144412274,18.9330485549953,42.0640442778871));
#68098=CARTESIAN_POINT('Ctrl Pts',(31.3867511677669,18.9779970980926,42.0682616686769));
#68099=CARTESIAN_POINT('Ctrl Pts',(31.4523068988343,19.0262333163217,42.0724790594666));
#68100=CARTESIAN_POINT('Ctrl Pts',(31.5178409592142,19.0744535891561,42.076695056118));
#68101=CARTESIAN_POINT('Ctrl Pts',(31.5809952129406,19.1259591035466,42.0809110527694));
#68102=CARTESIAN_POINT('Ctrl Pts',(31.6414306675575,19.1804792901421,42.0851270494208));
#68103=CARTESIAN_POINT('Ctrl Pts',(31.7018646623319,19.2349981597808,42.0893429442331));
#68104=CARTESIAN_POINT('Ctrl Pts',(31.7595796440716,19.2925312445725,42.0935588390454));
#68105=CARTESIAN_POINT('Ctrl Pts',(31.8142715384427,19.3527692830702,42.0977747338578));
#68106=CARTESIAN_POINT('Ctrl Pts',(31.8694495554961,19.4135427405216,42.1020281011716));
#68107=CARTESIAN_POINT('Ctrl Pts',(31.92155013975,19.4770691326891,42.1062814684854));
#68108=CARTESIAN_POINT('Ctrl Pts',(31.970302012333,19.5429961461284,42.1105348357993));
#68109=CARTESIAN_POINT('Ctrl Pts',(32.0186946669692,19.6084373901982,42.1147568630682));
#68110=CARTESIAN_POINT('Ctrl Pts',(32.0637875861554,19.6762435705913,42.1189788903372));
#68111=CARTESIAN_POINT('Ctrl Pts',(32.1053596380592,19.7460418490112,42.1232009176062));
#68112=CARTESIAN_POINT('Ctrl Pts',(32.1473945730361,19.8166172947859,42.1274699549425));
#68113=CARTESIAN_POINT('Ctrl Pts',(32.1858295198242,19.889229044105,42.1317389922787));
#68114=CARTESIAN_POINT('Ctrl Pts',(32.2204849743354,19.9634688963902,42.136008029615));
#68115=CARTESIAN_POINT('Ctrl Pts',(32.2551404288467,20.0377087486754,42.1402770669512));
#68116=CARTESIAN_POINT('Ctrl Pts',(32.2860162683499,20.113576230954,42.1445461042875));
#68117=CARTESIAN_POINT('Ctrl Pts',(32.3129847077609,20.1906471772681,42.1488151416238));
#68118=CARTESIAN_POINT('Ctrl Pts',(32.3397132946812,20.2670326683299,42.1530462109033));
#68119=CARTESIAN_POINT('Ctrl Pts',(32.3627040678191,20.3448869777792,42.1572772801828));
#68120=CARTESIAN_POINT('Ctrl Pts',(32.3817966079494,20.423809781096,42.1615083494623));
#68121=CARTESIAN_POINT('Ctrl Pts',(32.4008617551541,20.5026193503185,42.1657333482365));
#68122=CARTESIAN_POINT('Ctrl Pts',(32.4160396689735,20.5824939206251,42.1699583470106));
#68123=CARTESIAN_POINT('Ctrl Pts',(32.427218971285,20.6630158528444,42.1741833457848));
#68124=CARTESIAN_POINT('Ctrl Pts',(32.4384314466653,20.7437767230157,42.1784208816719));
#68125=CARTESIAN_POINT('Ctrl Pts',(32.445621391254,20.8251883552419,42.1826584175589));
#68126=CARTESIAN_POINT('Ctrl Pts',(32.4487276573074,20.9068167915449,42.186895953446));
#68127=CARTESIAN_POINT('Ctrl Pts',(32.4518191564025,20.9880571723197,42.1911133444019));
#68128=CARTESIAN_POINT('Ctrl Pts',(32.450865692402,21.0695118326457,42.1953307353578));
#68129=CARTESIAN_POINT('Ctrl Pts',(32.4458588408457,21.1507474068,42.1995481263138));
#68130=CARTESIAN_POINT('Ctrl Pts',(32.4408536444012,21.2319561269616,42.2037641231294));
#68131=CARTESIAN_POINT('Ctrl Pts',(32.4317977498745,21.312945441057,42.2079801199451));
#68132=CARTESIAN_POINT('Ctrl Pts',(32.4187348113261,21.393283819244,42.2121961167607));
#68133=CARTESIAN_POINT('Ctrl Pts',(32.4056721883249,21.4736202567844,42.2164120117352));
#68134=CARTESIAN_POINT('Ctrl Pts',(32.3886027894625,21.5533053309216,42.2206279067096));
#68135=CARTESIAN_POINT('Ctrl Pts',(32.367621710285,21.6319158860063,42.224843801684));
#68136=CARTESIAN_POINT('Ctrl Pts',(32.3464541449708,21.7112251553278,42.2290971687998));
#68137=CARTESIAN_POINT('Ctrl Pts',(32.321305122915,21.7894402395756,42.2333505359157));
#68138=CARTESIAN_POINT('Ctrl Pts',(32.2923236946659,21.8661422105367,42.2376039030316));
#68139=CARTESIAN_POINT('Ctrl Pts',(32.2635558075951,21.9422790254564,42.2418259304557));
#68140=CARTESIAN_POINT('Ctrl Pts',(32.2310120473007,22.0169245451166,42.2460479578799));
#68141=CARTESIAN_POINT('Ctrl Pts',(32.194885892181,22.0896908599713,42.2502699853041));
#68142=CARTESIAN_POINT('Ctrl Pts',(32.1583574957506,22.1632673805554,42.2545390222658));
#68143=CARTESIAN_POINT('Ctrl Pts',(32.118166673225,22.2349221633375,42.2588080592275));
#68144=CARTESIAN_POINT('Ctrl Pts',(32.0745591825804,22.304283116494,42.2630770961892));
#68145=CARTESIAN_POINT('Ctrl Pts',(32.0309516919358,22.3736440696506,42.2673461331509));
#68146=CARTESIAN_POINT('Ctrl Pts',(31.9839278641339,22.4407108336954,42.2716151701126));
#68147=CARTESIAN_POINT('Ctrl Pts',(31.933774905206,22.5051461277881,42.2758842070743));
#68148=CARTESIAN_POINT('Ctrl Pts',(31.8840679890306,22.5690083570698,42.2801152767248));
#68149=CARTESIAN_POINT('Ctrl Pts',(31.8311008536773,22.6305254517548,42.2843463463754));
#68150=CARTESIAN_POINT('Ctrl Pts',(31.7751229820897,22.6893456272939,42.2885774160259));
#68151=CARTESIAN_POINT('Ctrl Pts',(31.7192254244211,22.7480814109353,42.2928024151744));
#68152=CARTESIAN_POINT('Ctrl Pts',(31.6603260274446,22.804127626336,42.2970274143229));
#68153=CARTESIAN_POINT('Ctrl Pts',(31.5987154046977,22.8571643181965,42.3012524134714));
#68154=CARTESIAN_POINT('Ctrl Pts',(31.5369219675871,22.9103583833904,42.3054899492653));
#68155=CARTESIAN_POINT('Ctrl Pts',(31.4724014839592,22.9605246670681,42.3097274850591));
#68156=CARTESIAN_POINT('Ctrl Pts',(31.4054855055089,23.0073765824589,42.313965020853));
#68157=CARTESIAN_POINT('Ctrl Pts',(31.3388876331981,23.0540057725413,42.3181824121884));
#68158=CARTESIAN_POINT('Ctrl Pts',(31.2699173703278,23.0973517613215,42.3223998035238));
#68159=CARTESIAN_POINT('Ctrl Pts',(31.1989343462416,23.1371725909252,42.3266171948591));
#68160=CARTESIAN_POINT('Ctrl Pts',(31.1279747869491,23.1769802569936,42.3308331920553));
#68161=CARTESIAN_POINT('Ctrl Pts',(31.0550041929314,23.2132648507062,42.3350491892514));
#68162=CARTESIAN_POINT('Ctrl Pts',(30.9804088764946,23.2458291753583,42.3392651864476));
#68163=CARTESIAN_POINT('Ctrl Pts',(30.9058153619657,23.2783927133938,42.3434810818031));
#68164=CARTESIAN_POINT('Ctrl Pts',(30.8295976296179,23.3072359760307,42.3476969771585));
#68165=CARTESIAN_POINT('Ctrl Pts',(30.7521628347386,23.332209536049,42.351912872514));
#68166=CARTESIAN_POINT('Ctrl Pts',(30.6740397914275,23.3574050636408,42.3561662391815));
#68167=CARTESIAN_POINT('Ctrl Pts',(30.5946783953211,23.3786615921939,42.3604196058491));
#68168=CARTESIAN_POINT('Ctrl Pts',(30.5145114916103,23.3958773288716,42.3646729725167));
#68169=CARTESIAN_POINT('Ctrl Pts',(30.434935258764,23.4129662197614,42.3688950003193));
#68170=CARTESIAN_POINT('Ctrl Pts',(30.3545658224632,23.4260736518788,42.373117028122));
#68171=CARTESIAN_POINT('Ctrl Pts',(30.273834039708,23.4351519806158,42.3773390559246));
#68172=CARTESIAN_POINT('Ctrl Pts',(30.1922033846978,23.4443313879807,42.3816080920246));
#68173=CARTESIAN_POINT('Ctrl Pts',(30.1102027518452,23.4493913847828,42.3858771281247));
#68174=CARTESIAN_POINT('Ctrl Pts',(30.0282780395337,23.4503368344944,42.3901461642247));
#68175=CARTESIAN_POINT('Ctrl Pts',(29.9463533272223,23.451282284206,42.3944152003247));
#68176=CARTESIAN_POINT('Ctrl Pts',(29.8645050169356,23.4481132701266,42.3986842364247));
#68177=CARTESIAN_POINT('Ctrl Pts',(29.7831722166065,23.4408883551586,42.4029532725248));
#68178=CARTESIAN_POINT('Ctrl Pts',(29.7025627738389,23.4337276971305,42.4071843406767));
#68179=CARTESIAN_POINT('Ctrl Pts',(29.6221571600935,23.4225561642766,42.4114154088286));
#68180=CARTESIAN_POINT('Ctrl Pts',(29.5423862267232,23.4073927565953,42.4156464769805));
#68181=CARTESIAN_POINT('Ctrl Pts',(29.462729744305,23.3922511045381,42.4198714746283));
#68182=CARTESIAN_POINT('Ctrl Pts',(29.3837065866612,23.3731290386071,42.4240964722761));
#68183=CARTESIAN_POINT('Ctrl Pts',(29.3057431484531,23.3500973754464,42.4283214699239));
#68184=CARTESIAN_POINT('Ctrl Pts',(29.2275483382329,23.3269973612436,42.4325590060927));
#68185=CARTESIAN_POINT('Ctrl Pts',(29.150420017547,23.2999645552081,42.4367965422615));
#68186=CARTESIAN_POINT('Ctrl Pts',(29.0747787270261,23.2691222633513,42.4410340784303));
#68187=CARTESIAN_POINT('Ctrl Pts',(28.999497054501,23.2384266036197,42.4452514682709));
#68188=CARTESIAN_POINT('Ctrl Pts',(28.9256887406675,23.2039577700228,42.4494688581115));
#68189=CARTESIAN_POINT('Ctrl Pts',(28.8537520377168,23.1658868527607,42.4536862479521));
#68190=CARTESIAN_POINT('Ctrl Pts',(28.7818391147307,23.1278285205216,42.4579022436591));
#68191=CARTESIAN_POINT('Ctrl Pts',(28.7117969846284,23.0861706865561,42.462118239366));
#68192=CARTESIAN_POINT('Ctrl Pts',(28.6440007446553,23.0411311250149,42.4663342350729));
#68193=CARTESIAN_POINT('Ctrl Pts',(28.5762061422333,22.9960926513598,42.4705501289466));
#68194=CARTESIAN_POINT('Ctrl Pts',(28.5106577087616,22.9476728707419,42.4747660228203));
#68195=CARTESIAN_POINT('Ctrl Pts',(28.4477016931987,22.8961329638772,42.478981916694));
#68196=CARTESIAN_POINT('Ctrl Pts',(28.3841860692927,22.8441349250671,42.4832352851341));
#68197=CARTESIAN_POINT('Ctrl Pts',(28.3233095641587,22.7889613054111,42.4874886535742));
#68198=CARTESIAN_POINT('Ctrl Pts',(28.2653923196798,22.7309206929765,42.4917420220143));
#68199=CARTESIAN_POINT('Ctrl Pts',(28.2079018539464,22.6733077683572,42.4959640483686));
#68200=CARTESIAN_POINT('Ctrl Pts',(28.1533274502599,22.6128703532463,42.5001860747229));
#68201=CARTESIAN_POINT('Ctrl Pts',(28.1019426666762,22.5499447117287,42.5044081010772));
#68202=CARTESIAN_POINT('Ctrl Pts',(28.0499857029963,22.4863183802966,42.5086771405602));
#68203=CARTESIAN_POINT('Ctrl Pts',(28.0012901237273,22.4201484581849,42.5129461800432));
#68204=CARTESIAN_POINT('Ctrl Pts',(27.9560935127577,22.3518123099783,42.5172152195262));
#68205=CARTESIAN_POINT('Ctrl Pts',(27.9108969017881,22.2834761617717,42.5214842590092));
#68206=CARTESIAN_POINT('Ctrl Pts',(27.8691994500721,22.2129742372533,42.5257532984923));
#68207=CARTESIAN_POINT('Ctrl Pts',(27.8311899325944,22.1407072987932,42.5300223379753));
#68208=CARTESIAN_POINT('Ctrl Pts',(27.7913112811431,22.0648866033058,42.5345013092665));
#68209=CARTESIAN_POINT('Ctrl Pts',(27.7553561644625,21.9868657022069,42.5389802805577));
#68210=CARTESIAN_POINT('Ctrl Pts',(27.7235581914406,21.907062810528,42.5434592518489));
#68211=CARTESIAN_POINT('Ctrl Pts',(27.6918561073449,21.827500569836,42.5479247165009));
#68212=CARTESIAN_POINT('Ctrl Pts',(27.6642863325223,21.7461673995204,42.552390181153));
#68213=CARTESIAN_POINT('Ctrl Pts',(27.6410356048089,21.6635037544889,42.556855645805));
#68214=CARTESIAN_POINT('Ctrl Pts',(27.6178276006091,21.5809920049766,42.5613129051078));
#68215=CARTESIAN_POINT('Ctrl Pts',(27.5989229557308,21.4971550122848,42.5657701644107));
#68216=CARTESIAN_POINT('Ctrl Pts',(27.5844599283427,21.4124517089524,42.5702274237136));
#68217=CARTESIAN_POINT('Ctrl Pts',(27.5700323064602,21.327955759392,42.5746737716412));
#68218=CARTESIAN_POINT('Ctrl Pts',(27.560024706694,21.2425981005171,42.5791201195687));
#68219=CARTESIAN_POINT('Ctrl Pts',(27.5545249146432,21.1568497908799,42.5835664674963));
#68220=CARTESIAN_POINT('Ctrl Pts',(27.5511827325148,21.1047411901609,42.5862684795803));
#68221=CARTESIAN_POINT('Ctrl Pts',(27.5495042685491,21.0524886039351,42.5889704916642));
#68222=CARTESIAN_POINT('Ctrl Pts',(27.5495000081341,21.0001996626194,42.5916725037481));
#68223=CARTESIAN_POINT('',(27.5495010068324,20.9977786299922,43.3916725037471));
#68224=CARTESIAN_POINT('Ctrl Pts',(27.549500008134,21.0001996618478,42.591672503788));
#68225=CARTESIAN_POINT('Ctrl Pts',(27.549493086791,20.9152522810414,42.5960621288915));
#68226=CARTESIAN_POINT('Ctrl Pts',(27.5539075740442,20.8303783217193,42.600451753995));
#68227=CARTESIAN_POINT('Ctrl Pts',(27.5626947630161,20.746044429534,42.6048413790985));
#68228=CARTESIAN_POINT('Ctrl Pts',(27.5715034330423,20.6615043757502,42.6092417350257));
#68229=CARTESIAN_POINT('Ctrl Pts',(27.5847061246101,20.5775074337583,42.6136420909529));
#68230=CARTESIAN_POINT('Ctrl Pts',(27.602202470725,20.4945128502102,42.6180424468801));
#68231=CARTESIAN_POINT('Ctrl Pts',(27.6197201796934,20.4114169311539,42.6224481755953));
#68232=CARTESIAN_POINT('Ctrl Pts',(27.641541890222,20.3293262038286,42.6268539043105));
#68233=CARTESIAN_POINT('Ctrl Pts',(27.6675172453543,20.2486848535533,42.6312596330258));
#68234=CARTESIAN_POINT('Ctrl Pts',(27.6935620327325,20.1678279485709,42.6356771382745));
#68235=CARTESIAN_POINT('Ctrl Pts',(27.7237825197494,20.088428549067,42.6400946435232));
#68236=CARTESIAN_POINT('Ctrl Pts',(27.7579797073247,20.0109119062327,42.6445121487719));
#68237=CARTESIAN_POINT('Ctrl Pts',(27.7904395918625,19.9373333035882,42.6487052336565));
#68238=CARTESIAN_POINT('Ctrl Pts',(27.8264818567594,19.8654510897126,42.6528983185412));
#68239=CARTESIAN_POINT('Ctrl Pts',(27.8658994649333,19.7956058966318,42.6570914034258));
#68240=CARTESIAN_POINT('Ctrl Pts',(27.9056741766947,19.7251279414386,42.6613224755381));
#68241=CARTESIAN_POINT('Ctrl Pts',(27.9490185459123,19.6564901683137,42.6655535476503));
#68242=CARTESIAN_POINT('Ctrl Pts',(27.9957375362144,19.5900772268453,42.6697846197626));
#68243=CARTESIAN_POINT('Ctrl Pts',(28.0423894969425,19.5237595706378,42.6740096213892));
#68244=CARTESIAN_POINT('Ctrl Pts',(28.09240619754,19.4596607835253,42.6782346230158));
#68245=CARTESIAN_POINT('Ctrl Pts',(28.1455472373667,19.3981400806681,42.6824596246424));
#68246=CARTESIAN_POINT('Ctrl Pts',(28.1988459211258,19.3364368754447,42.6866971598188));
#68247=CARTESIAN_POINT('Ctrl Pts',(28.2552872733254,19.2773274835091,42.6909346949952));
#68248=CARTESIAN_POINT('Ctrl Pts',(28.3145854936707,19.2211441340416,42.6951722301716));
#68249=CARTESIAN_POINT('Ctrl Pts',(28.3736018648619,19.1652278284993,42.6993896240065));
#68250=CARTESIAN_POINT('Ctrl Pts',(28.435447671836,19.1122101393852,42.7036070178415));
#68251=CARTESIAN_POINT('Ctrl Pts',(28.4998027780823,19.0623832821349,42.7078244116764));
#68252=CARTESIAN_POINT('Ctrl Pts',(28.5641366105701,19.0125728960644,42.7120404113746));
#68253=CARTESIAN_POINT('Ctrl Pts',(28.6309777277201,18.9659515316314,42.7162564110728));
#68254=CARTESIAN_POINT('Ctrl Pts',(28.6999730174825,18.9227710538492,42.720472410771));
#68255=CARTESIAN_POINT('Ctrl Pts',(28.768966640596,18.8795916191339,42.7246883086276));
#68256=CARTESIAN_POINT('Ctrl Pts',(28.8401139381397,18.8398531515447,42.7289042064842));
#68257=CARTESIAN_POINT('Ctrl Pts',(28.9130341565902,18.8037633312276,42.7331201043407));
#68258=CARTESIAN_POINT('Ctrl Pts',(28.9866024026739,18.7673527877786,42.737373468052));
#68259=CARTESIAN_POINT('Ctrl Pts',(29.0619748147519,18.7346562940568,42.7416268317633));
#68260=CARTESIAN_POINT('Ctrl Pts',(29.1387382250637,18.7058381911832,42.7458801954746));
#68261=CARTESIAN_POINT('Ctrl Pts',(29.2149361390944,18.6772323838542,42.7501022257505));
#68262=CARTESIAN_POINT('Ctrl Pts',(29.2925041588335,18.6524480987598,42.7543242560263));
#68263=CARTESIAN_POINT('Ctrl Pts',(29.3710231183096,18.6315958258146,42.7585462863022));
#68264=CARTESIAN_POINT('Ctrl Pts',(29.4504161603667,18.6105114228375,42.7628153167312));
#68265=CARTESIAN_POINT('Ctrl Pts',(29.5307809677201,18.5934472196906,42.7670843471602));
#68266=CARTESIAN_POINT('Ctrl Pts',(29.6116757770617,18.5804639808675,42.7713533775892));
#68267=CARTESIAN_POINT('Ctrl Pts',(29.6925705864033,18.5674807420445,42.7756224080182));
#68268=CARTESIAN_POINT('Ctrl Pts',(29.7739949092396,18.5585784559607,42.7798914384472));
#68269=CARTESIAN_POINT('Ctrl Pts',(29.8555058016396,18.5537637733366,42.7841604688763));
#68270=CARTESIAN_POINT('Ctrl Pts',(29.9362917085614,18.5489919141301,42.788391529103));
#68271=CARTESIAN_POINT('Ctrl Pts',(30.0174658560517,18.5482172809471,42.7926225893298));
#68272=CARTESIAN_POINT('Ctrl Pts',(30.0985992845727,18.5514844433654,42.7968536495566));
#68273=CARTESIAN_POINT('Ctrl Pts',(30.1796163069832,18.5547469182254,42.8010786392737));
#68274=CARTESIAN_POINT('Ctrl Pts',(30.260592265792,18.562039652997,42.8053036289908));
#68275=CARTESIAN_POINT('Ctrl Pts',(30.3410949892738,18.5733553086015,42.8095286187079));
#68276=CARTESIAN_POINT('Ctrl Pts',(30.4218368099261,18.584704572277,42.8137661568587));
#68277=CARTESIAN_POINT('Ctrl Pts',(30.5021021076208,18.6001007137476,42.8180036950095));
#68278=CARTESIAN_POINT('Ctrl Pts',(30.5814567786513,18.6194836138853,42.8222412331603));
#68279=CARTESIAN_POINT('Ctrl Pts',(30.6604339926941,18.6387743176721,42.826458615114));
#68280=CARTESIAN_POINT('Ctrl Pts',(30.7385087669624,18.6620138338785,42.8306759970678));
#68281=CARTESIAN_POINT('Ctrl Pts',(30.8152620195595,18.6890915012784,42.8348933790215));
#68282=CARTESIAN_POINT('Ctrl Pts',(30.8919899005624,18.7161602178708,42.8391093668753));
#68283=CARTESIAN_POINT('Ctrl Pts',(30.9673966892661,18.747064411558,42.8433253547292));
#68284=CARTESIAN_POINT('Ctrl Pts',(31.0410793414582,18.7816438395089,42.847541342583));
#68285=CARTESIAN_POINT('Ctrl Pts',(31.114760214688,18.8162224325889,42.8517572286478));
#68286=CARTESIAN_POINT('Ctrl Pts',(31.1867166137223,18.8544758849736,42.8559731147126));
#68287=CARTESIAN_POINT('Ctrl Pts',(31.2565676454783,18.8961967767072,42.8601890007775));
#68288=CARTESIAN_POINT('Ctrl Pts',(31.3270398600767,18.9382886909077,42.8644423785732));
#68289=CARTESIAN_POINT('Ctrl Pts',(31.395368652384,18.9839097925061,42.868695756369));
#68290=CARTESIAN_POINT('Ctrl Pts',(31.4611919764053,19.0328019270829,42.8729491341648));
#68291=CARTESIAN_POINT('Ctrl Pts',(31.5265300019485,19.0813335924969,42.8771711528975));
#68292=CARTESIAN_POINT('Ctrl Pts',(31.5893990575742,19.1330878717429,42.8813931716302));
#68293=CARTESIAN_POINT('Ctrl Pts',(31.6494791089642,19.187772387615,42.8856151903628));
#68294=CARTESIAN_POINT('Ctrl Pts',(31.7102285276313,19.2430661577178,42.8898842476902));
#68295=CARTESIAN_POINT('Ctrl Pts',(31.7681260661066,19.3013555162733,42.8941533050175));
#68296=CARTESIAN_POINT('Ctrl Pts',(31.8228812237863,19.3623021359337,42.8984223623448));
#68297=CARTESIAN_POINT('Ctrl Pts',(31.8776363814661,19.4232487555941,42.9026914196721));
#68298=CARTESIAN_POINT('Ctrl Pts',(31.9292489033193,19.4868522195339,42.9069604769995));
#68299=CARTESIAN_POINT('Ctrl Pts',(31.9774731271901,19.5527438784925,42.9112295343268));
#68300=CARTESIAN_POINT('Ctrl Pts',(32.0252683195604,19.6180493258951,42.9154606115702));
#68301=CARTESIAN_POINT('Ctrl Pts',(32.069914686428,19.6858474989918,42.9196916888135));
#68302=CARTESIAN_POINT('Ctrl Pts',(32.1111422814506,19.7558020585647,42.9239227660569));
#68303=CARTESIAN_POINT('Ctrl Pts',(32.1523107249026,19.8256562503607,42.9281477727336));
#68304=CARTESIAN_POINT('Ctrl Pts',(32.1900699043101,19.8976602867672,42.9323727794103));
#68305=CARTESIAN_POINT('Ctrl Pts',(32.2241917558679,19.9714469954693,42.936597786087));
#68306=CARTESIAN_POINT('Ctrl Pts',(32.25841477938,20.0454524831993,42.9408353199908));
#68307=CARTESIAN_POINT('Ctrl Pts',(32.2889785966458,20.1212508467144,42.9450728538945));
#68308=CARTESIAN_POINT('Ctrl Pts',(32.3156984551624,20.198444690144,42.9493103877983));
#68309=CARTESIAN_POINT('Ctrl Pts',(32.3422913504427,20.2752717359655,42.9535277864525));
#68310=CARTESIAN_POINT('Ctrl Pts',(32.3650765757841,20.3534805893461,42.9577451851068));
#68311=CARTESIAN_POINT('Ctrl Pts',(32.3839199923844,20.4326590796445,42.961962583761));
#68312=CARTESIAN_POINT('Ctrl Pts',(32.4027571795232,20.5118113942566,42.9661785881817));
#68313=CARTESIAN_POINT('Ctrl Pts',(32.4176550381721,20.5919322572445,42.9703945926024));
#68314=CARTESIAN_POINT('Ctrl Pts',(32.4285297894867,20.6725961032983,42.9746105970231));
#68315=CARTESIAN_POINT('Ctrl Pts',(32.439404277847,20.7532579988783,42.9788264994997));
#68316=CARTESIAN_POINT('Ctrl Pts',(32.4462557912599,20.8344623904805,42.9830424019763));
#68317=CARTESIAN_POINT('Ctrl Pts',(32.4490522035399,20.9157767589296,42.9872583044529));
#68318=CARTESIAN_POINT('Ctrl Pts',(32.4518734600683,20.9978135510283,42.9915116623966));
#68319=CARTESIAN_POINT('Ctrl Pts',(32.450567168116,21.0799618036545,42.9957650203403));
#68320=CARTESIAN_POINT('Ctrl Pts',(32.4451540521899,21.1617773502671,43.000018378284));
#68321=CARTESIAN_POINT('Ctrl Pts',(32.4397808005059,21.2429903761122,43.0042404128839));
#68322=CARTESIAN_POINT('Ctrl Pts',(32.4303611284438,21.3238751206313,43.0084624474838));
#68323=CARTESIAN_POINT('Ctrl Pts',(32.4169672910001,21.4040041636366,43.0126844820837));
#68324=CARTESIAN_POINT('Ctrl Pts',(32.4034243999077,21.4850249246634,43.0169535016993));
#68325=CARTESIAN_POINT('Ctrl Pts',(32.3858184464448,21.5652725831967,43.0212225213149));
#68326=CARTESIAN_POINT('Ctrl Pts',(32.3642763033408,21.6443196500661,43.0254915409305));
#68327=CARTESIAN_POINT('Ctrl Pts',(32.3427341602367,21.7233667169355,43.0297605605461));
#68328=CARTESIAN_POINT('Ctrl Pts',(32.3172560395432,21.8012127519313,43.0340295801617));
#68329=CARTESIAN_POINT('Ctrl Pts',(32.2880185956719,21.8774515119707,43.0382985997773));
#68330=CARTESIAN_POINT('Ctrl Pts',(32.259040935268,21.9530128677363,43.0425296878718));
#68331=CARTESIAN_POINT('Ctrl Pts',(32.2262617796299,22.0272789944634,43.0467607759663));
#68332=CARTESIAN_POINT('Ctrl Pts',(32.1898174801253,22.0998407401701,43.0509918640608));
#68333=CARTESIAN_POINT('Ctrl Pts',(32.1534254672907,22.1722983814735,43.0552168818094));
#68334=CARTESIAN_POINT('Ctrl Pts',(32.1133789610299,22.2430560862626,43.0594418995579));
#68335=CARTESIAN_POINT('Ctrl Pts',(32.0698629240861,22.3117231893558,43.0636669173065));
#68336=CARTESIAN_POINT('Ctrl Pts',(32.0262180038441,22.38059366673,43.0679044484699));
#68337=CARTESIAN_POINT('Ctrl Pts',(31.9790831429959,22.4473606998694,43.0721419796333));
#68338=CARTESIAN_POINT('Ctrl Pts',(31.9286921753868,22.5116536450529,43.0763795107966));
#68339=CARTESIAN_POINT('Ctrl Pts',(31.8785404782383,22.5756413092836,43.0805969209725));
#68340=CARTESIAN_POINT('Ctrl Pts',(31.8251638105296,22.6371779554607,43.0848143311483));
#68341=CARTESIAN_POINT('Ctrl Pts',(31.7688358566356,22.6959274637437,43.0890317413241));
#68342=CARTESIAN_POINT('Ctrl Pts',(31.7125265222976,22.7546575520108,43.0932477574087));
#68343=CARTESIAN_POINT('Ctrl Pts',(31.6532681606354,22.8106019966062,43.0974637734933));
#68344=CARTESIAN_POINT('Ctrl Pts',(31.5913730069765,22.8634597400176,43.1016797895779));
#68345=CARTESIAN_POINT('Ctrl Pts',(31.5294793481123,22.9163162068917,43.1058957038439));
#68346=CARTESIAN_POINT('Ctrl Pts',(31.464949378151,22.9660858196879,43.1101116181099));
#68347=CARTESIAN_POINT('Ctrl Pts',(31.3981291712374,23.0125071603686,43.1143275323759));
#68348=CARTESIAN_POINT('Ctrl Pts',(31.3307157146918,23.0593406434918,43.1185808767802));
#68349=CARTESIAN_POINT('Ctrl Pts',(31.2609715366747,23.1027658152123,43.1228342211846));
#68350=CARTESIAN_POINT('Ctrl Pts',(31.1892811368985,23.1425593638024,43.1270875655889));
#68351=CARTESIAN_POINT('Ctrl Pts',(31.1181182641333,23.1820600953373,43.1313096121616));
#68352=CARTESIAN_POINT('Ctrl Pts',(31.0450381656912,23.2179823208382,43.1355316587343));
#68353=CARTESIAN_POINT('Ctrl Pts',(30.9704392033924,23.2501551063247,43.139753705307));
#68354=CARTESIAN_POINT('Ctrl Pts',(30.8950107432233,23.2826856348176,43.1440226986272));
#68355=CARTESIAN_POINT('Ctrl Pts',(30.8180298896953,23.3113826528595,43.1482916919473));
#68356=CARTESIAN_POINT('Ctrl Pts',(30.7399246530609,23.3361210922794,43.1525606852674));
#68357=CARTESIAN_POINT('Ctrl Pts',(30.6618194164265,23.3608595316993,43.1568296785875));
#68358=CARTESIAN_POINT('Ctrl Pts',(30.5825902815366,23.3816393321179,43.1610986719076));
#68359=CARTESIAN_POINT('Ctrl Pts',(30.5026743844033,23.3983887744202,43.1653676652278));
#68360=CARTESIAN_POINT('Ctrl Pts',(30.4234698009203,23.4149891336567,43.1695986611865));
#68361=CARTESIAN_POINT('Ctrl Pts',(30.3432933544925,23.4276929462028,43.1738296571453));
#68362=CARTESIAN_POINT('Ctrl Pts',(30.262562773737,23.4363930388686,43.1780606531041));
#68363=CARTESIAN_POINT('Ctrl Pts',(30.181948024525,23.4450806487163,43.1822855784662));
#68364=CARTESIAN_POINT('Ctrl Pts',(30.1007811784374,23.4497758982526,43.1865105038283));
#68365=CARTESIAN_POINT('Ctrl Pts',(30.0194907761083,23.4504224859495,43.1907354291904));
#68366=CARTESIAN_POINT('Ctrl Pts',(29.9379573859028,23.4510710063834,43.1949729834191));
#68367=CARTESIAN_POINT('Ctrl Pts',(29.8563001633159,23.4476465305232,43.1992105376478));
#68368=CARTESIAN_POINT('Ctrl Pts',(29.7749573475945,23.44014467903,43.2034480918764));
#68369=CARTESIAN_POINT('Ctrl Pts',(29.6940029832178,23.4326786525113,43.2076654097311));
#68370=CARTESIAN_POINT('Ctrl Pts',(29.6133604966496,23.421174142012,43.2118827275858));
#68371=CARTESIAN_POINT('Ctrl Pts',(29.5334606770915,23.4056789707233,43.2161000454405));
#68372=CARTESIAN_POINT('Ctrl Pts',(29.4535872651673,23.3901889207328,43.2203159694324));
#68373=CARTESIAN_POINT('Ctrl Pts',(29.374456488926,23.3707109176446,43.2245318934243));
#68374=CARTESIAN_POINT('Ctrl Pts',(29.2964905660705,23.3473441857496,43.2287478174162));
#68375=CARTESIAN_POINT('Ctrl Pts',(29.2185265196641,23.3239780162346,43.2329636399411));
#68376=CARTESIAN_POINT('Ctrl Pts',(29.1417277159923,23.2967234385438,43.237179462466));
#68377=CARTESIAN_POINT('Ctrl Pts',(29.0665014004674,23.2657295987541,43.241395284991));
#68378=CARTESIAN_POINT('Ctrl Pts',(28.9906035996739,23.2344591016978,43.2456487387982));
#68379=CARTESIAN_POINT('Ctrl Pts',(28.9163069520686,23.199382420127,43.2499021926055));
#68380=CARTESIAN_POINT('Ctrl Pts',(28.8440075601775,23.1607016751679,43.2541556464128));
#68381=CARTESIAN_POINT('Ctrl Pts',(28.772243551341,23.1223073643661,43.2583776030382));
#68382=CARTESIAN_POINT('Ctrl Pts',(28.7024476878714,23.0803624840626,43.2625995596637));
#68383=CARTESIAN_POINT('Ctrl Pts',(28.6349795107216,23.0351091650941,43.2668215162891));
#68384=CARTESIAN_POINT('Ctrl Pts',(28.5667563314609,22.9893494392122,43.2710907186873));
#68385=CARTESIAN_POINT('Ctrl Pts',(28.5009136506876,22.9402070591589,43.2753599210855));
#68386=CARTESIAN_POINT('Ctrl Pts',(28.4377886014137,22.8879739924392,43.2796291234837));
#68387=CARTESIAN_POINT('Ctrl Pts',(28.3746635521398,22.8357409257196,43.2838983258819));
#68388=CARTESIAN_POINT('Ctrl Pts',(28.3142564479958,22.7804175472364,43.2881675282801));
#68389=CARTESIAN_POINT('Ctrl Pts',(28.2568645214409,22.7223324166341,43.2924367306782));
#68390=CARTESIAN_POINT('Ctrl Pts',(28.2007779866314,22.6655684448528,43.2966088291473));
#68391=CARTESIAN_POINT('Ctrl Pts',(28.1473479519389,22.605941111798,43.3007809276163));
#68392=CARTESIAN_POINT('Ctrl Pts',(28.0968868343006,22.5437326609688,43.3049530260853));
#68393=CARTESIAN_POINT('Ctrl Pts',(28.0464909074219,22.4816045772886,43.3091197346169));
#68394=CARTESIAN_POINT('Ctrl Pts',(27.9990565902623,22.4169023559389,43.3132864431485));
#68395=CARTESIAN_POINT('Ctrl Pts',(27.9548600169935,22.349945443308,43.31745315168));
#68396=CARTESIAN_POINT('Ctrl Pts',(27.910706113351,22.2830531742962,43.3216158374587));
#68397=CARTESIAN_POINT('Ctrl Pts',(27.8697840150892,22.2139109292311,43.3257785232373));
#68398=CARTESIAN_POINT('Ctrl Pts',(27.8323290073754,22.1428703853605,43.3299412090159));
#68399=CARTESIAN_POINT('Ctrl Pts',(27.7948979409024,22.0718752506051,43.3341012340058));
#68400=CARTESIAN_POINT('Ctrl Pts',(27.7609297891928,21.9989846476863,43.3382612589956));
#68401=CARTESIAN_POINT('Ctrl Pts',(27.7306151223929,21.9245769450339,43.3424212839855));
#68402=CARTESIAN_POINT('Ctrl Pts',(27.7002985254673,21.8501645048654,43.3465815738429));
#68403=CARTESIAN_POINT('Ctrl Pts',(27.673636076591,21.7742352081396,43.3507418637004));
#68404=CARTESIAN_POINT('Ctrl Pts',(27.6507706882892,21.6971885620109,43.3549021535578));
#68405=CARTESIAN_POINT('Ctrl Pts',(27.6279060413098,21.6201444138239,43.3590623085338));
#68406=CARTESIAN_POINT('Ctrl Pts',(27.6088383386126,21.5419834500785,43.3632224635098));
#68407=CARTESIAN_POINT('Ctrl Pts',(27.5936603281247,21.4631194592749,43.3673826184857));
#68408=CARTESIAN_POINT('Ctrl Pts',(27.5784668653675,21.3841751794489,43.3715470087886));
#68409=CARTESIAN_POINT('Ctrl Pts',(27.567171087686,21.304526915724,43.3757113990914));
#68410=CARTESIAN_POINT('Ctrl Pts',(27.559814264702,21.2245970330348,43.3798757893942));
#68411=CARTESIAN_POINT('Ctrl Pts',(27.5528675623857,21.1491229999606,43.3838080275118));
#68412=CARTESIAN_POINT('Ctrl Pts',(27.5494324578582,21.0733982663518,43.3877402656295));
#68413=CARTESIAN_POINT('Ctrl Pts',(27.5495010068324,20.9977786299922,43.3916725037471));
#68414=CARTESIAN_POINT('',(27.549500297338,21.0012071676208,44.1916725038378));
#68415=CARTESIAN_POINT('Ctrl Pts',(27.5495010068331,20.9977786292072,43.3916725037879));
#68416=CARTESIAN_POINT('Ctrl Pts',(27.5496021452566,20.8862080595143,43.3974741985338));
#68417=CARTESIAN_POINT('Ctrl Pts',(27.5573265235963,20.7749710520682,43.4032758932798));
#68418=CARTESIAN_POINT('Ctrl Pts',(27.5725171141633,20.6649222642881,43.4090775880257));
#68419=CARTESIAN_POINT('Ctrl Pts',(27.5816185145056,20.5989868373306,43.4125536573934));
#68420=CARTESIAN_POINT('Ctrl Pts',(27.5933992287848,20.5334773180416,43.416029726761));
#68421=CARTESIAN_POINT('Ctrl Pts',(27.6078177664,20.4685732305873,43.4195057961287));
#68422=CARTESIAN_POINT('Ctrl Pts',(27.6253684716024,20.3895698991994,43.4237369789548));
#68423=CARTESIAN_POINT('Ctrl Pts',(27.646870004191,20.311288753792,43.4279681617809));
#68424=CARTESIAN_POINT('Ctrl Pts',(27.6722476464476,20.2341545648558,43.432199344607));
#68425=CARTESIAN_POINT('Ctrl Pts',(27.6975888871691,20.1571310167292,43.4364244582503));
#68426=CARTESIAN_POINT('Ctrl Pts',(27.726795051179,20.0812515955261,43.4406495718936));
#68427=CARTESIAN_POINT('Ctrl Pts',(27.7597406196658,20.0069299325705,43.4448746855369));
#68428=CARTESIAN_POINT('Ctrl Pts',(27.7927828286825,19.9323902589617,43.449112192872));
#68429=CARTESIAN_POINT('Ctrl Pts',(27.8295863064312,19.8594179568088,43.4533497002071));
#68430=CARTESIAN_POINT('Ctrl Pts',(27.8699742662314,19.788414004916,43.4575872075422));
#68431=CARTESIAN_POINT('Ctrl Pts',(27.9101716126747,19.7177451603595,43.4618047157116));
#68432=CARTESIAN_POINT('Ctrl Pts',(27.9539194565869,19.6490265384259,43.4660222238811));
#68433=CARTESIAN_POINT('Ctrl Pts',(28.0009965032448,19.5826308631974,43.4702397320505));
#68434=CARTESIAN_POINT('Ctrl Pts',(28.048057994974,19.5162571260484,43.474455846695));
#68435=CARTESIAN_POINT('Ctrl Pts',(28.0984462362708,19.4522051903639,43.4786719613395));
#68436=CARTESIAN_POINT('Ctrl Pts',(28.1518966449034,19.3908187675465,43.482888075984));
#68437=CARTESIAN_POINT('Ctrl Pts',(28.2053457681527,19.3294338209588,43.4871040892388));
#68438=CARTESIAN_POINT('Ctrl Pts',(28.2618566061826,19.2707146097055,43.4913201024935));
#68439=CARTESIAN_POINT('Ctrl Pts',(28.3211252769315,19.2149706124991,43.4955361157483));
#68440=CARTESIAN_POINT('Ctrl Pts',(28.3809171237012,19.1587345522471,43.4997893445675));
#68441=CARTESIAN_POINT('Ctrl Pts',(28.4435153941032,19.1055268343405,43.5040425733868));
#68442=CARTESIAN_POINT('Ctrl Pts',(28.5085726479575,19.0556248552351,43.508295802206));
#68443=CARTESIAN_POINT('Ctrl Pts',(28.5731544536407,19.0060875672794,43.512517947791));
#68444=CARTESIAN_POINT('Ctrl Pts',(28.6401589983129,18.9598080756316,43.5167400933759));
#68445=CARTESIAN_POINT('Ctrl Pts',(28.7092173758703,18.9170140501566,43.5209622389609));
#68446=CARTESIAN_POINT('Ctrl Pts',(28.7790383601472,18.8737474533219,43.5252310093972));
#68447=CARTESIAN_POINT('Ctrl Pts',(28.8509583897956,18.8340440118049,43.5294997798336));
#68448=CARTESIAN_POINT('Ctrl Pts',(28.924572579229,18.7980903486623,43.53376855027));
#68449=CARTESIAN_POINT('Ctrl Pts',(28.9981867686625,18.7621366855198,43.5380373207064));
#68450=CARTESIAN_POINT('Ctrl Pts',(29.0734946473876,18.7299329317349,43.5423060911428));
#68451=CARTESIAN_POINT('Ctrl Pts',(29.150074461334,18.7016142993998,43.5465748615792));
#68452=CARTESIAN_POINT('Ctrl Pts',(29.2259674738007,18.6735496410246,43.5508053478033));
#68453=CARTESIAN_POINT('Ctrl Pts',(29.3033946777195,18.6491952695504,43.5550358340274));
#68454=CARTESIAN_POINT('Ctrl Pts',(29.3819587508262,18.6287186450529,43.5592663202515));
#68455=CARTESIAN_POINT('Ctrl Pts',(29.4604100683231,18.6082714087248,43.5634907348575));
#68456=CARTESIAN_POINT('Ctrl Pts',(29.5399945682253,18.5916909825737,43.5677151494634));
#68457=CARTESIAN_POINT('Ctrl Pts',(29.6202967452597,18.5790961009698,43.5719395640694));
#68458=CARTESIAN_POINT('Ctrl Pts',(29.7008511190746,18.5664616639179,43.5761772458594));
#68459=CARTESIAN_POINT('Ctrl Pts',(29.7821272402639,18.5578380076049,43.5804149276494));
#68460=CARTESIAN_POINT('Ctrl Pts',(29.8636921726964,18.5532939640783,43.5846526094394));
#68461=CARTESIAN_POINT('Ctrl Pts',(29.9448553424021,18.5487723030543,43.5888694177666));
#68462=CARTESIAN_POINT('Ctrl Pts',(30.0263040170551,18.5482901901487,43.5930862260937));
#68463=CARTESIAN_POINT('Ctrl Pts',(30.107605143246,18.5518636918776,43.5973030344208));
#68464=CARTESIAN_POINT('Ctrl Pts',(30.1888794259112,18.5554360137289,43.601518450467));
#68465=CARTESIAN_POINT('Ctrl Pts',(30.2700057925672,18.5630612706616,43.6057338665133));
#68466=CARTESIAN_POINT('Ctrl Pts',(30.3505521070748,18.5747034263362,43.6099492825595));
#68467=CARTESIAN_POINT('Ctrl Pts',(30.4310965259356,18.5863453080142,43.6141645993965));
#68468=CARTESIAN_POINT('Ctrl Pts',(30.5110604596274,18.6020038328427,43.6183799162335));
#68469=CARTESIAN_POINT('Ctrl Pts',(30.5900192397141,18.6215913835577,43.6225952330705));
#68470=CARTESIAN_POINT('Ctrl Pts',(30.6697036927838,18.6413589542317,43.6268492909004));
#68471=CARTESIAN_POINT('Ctrl Pts',(30.7483639492194,18.6651280441937,43.6311033487304));
#68472=CARTESIAN_POINT('Ctrl Pts',(30.8255782474139,18.6927568816016,43.6353574065603));
#68473=CARTESIAN_POINT('Ctrl Pts',(30.9022008998325,18.7201740161859,43.6395788681561));
#68474=CARTESIAN_POINT('Ctrl Pts',(30.9773992665641,18.7513917143964,43.6438003297518));
#68475=CARTESIAN_POINT('Ctrl Pts',(31.0507822000554,18.7862233585913,43.6480217913476));
#68476=CARTESIAN_POINT('Ctrl Pts',(31.1250150787245,18.821458434301,43.6522921472946));
#68477=CARTESIAN_POINT('Ctrl Pts',(31.1973897680754,18.8603914793856,43.6565625032417));
#68478=CARTESIAN_POINT('Ctrl Pts',(31.2675295345076,18.9027830037998,43.6608328591887));
#68479=CARTESIAN_POINT('Ctrl Pts',(31.3376693009398,18.945174528214,43.6651032151357));
#68480=CARTESIAN_POINT('Ctrl Pts',(31.4055737783894,18.9910242064388,43.6693735710827));
#68481=CARTESIAN_POINT('Ctrl Pts',(31.4709003813,19.040050429656,43.6736439270298));
#68482=CARTESIAN_POINT('Ctrl Pts',(31.5356384035015,19.0886349355952,43.677875807853));
#68483=CARTESIAN_POINT('Ctrl Pts',(31.5980879816993,19.1405214056606,43.6821076886763));
#68484=CARTESIAN_POINT('Ctrl Pts',(31.6578929244885,19.1954664589066,43.6863395694996));
#68485=CARTESIAN_POINT('Ctrl Pts',(31.717612038061,19.2503326576189,43.6905653769283));
#68486=CARTESIAN_POINT('Ctrl Pts',(31.7746937149698,19.3082484097147,43.6947911843569));
#68487=CARTESIAN_POINT('Ctrl Pts',(31.8288128709315,19.3689286548053,43.6990169917856));
#68488=CARTESIAN_POINT('Ctrl Pts',(31.8830796374524,19.4297744058937,43.7032543251479));
#68489=CARTESIAN_POINT('Ctrl Pts',(31.9343673257176,19.493399463376,43.7074916585102));
#68490=CARTESIAN_POINT('Ctrl Pts',(31.9823837021845,19.5594774880921,43.7117289918724));
#68491=CARTESIAN_POINT('Ctrl Pts',(32.0301831149951,19.6252569369702,43.7159471786975));
#68492=CARTESIAN_POINT('Ctrl Pts',(32.0747404343294,19.6934668590254,43.7201653655225));
#68493=CARTESIAN_POINT('Ctrl Pts',(32.1158073434469,19.7637518309755,43.7243835523476));
#68494=CARTESIAN_POINT('Ctrl Pts',(32.1568606160447,19.8340134643687,43.7286003384978));
#68495=CARTESIAN_POINT('Ctrl Pts',(32.1944255457942,19.9063483783473,43.732817124648));
#68496=CARTESIAN_POINT('Ctrl Pts',(32.2282981000228,19.9803736824529,43.7370339107981));
#68497=CARTESIAN_POINT('Ctrl Pts',(32.2621697754284,20.0543970659728,43.7412505875439));
#68498=CARTESIAN_POINT('Ctrl Pts',(32.2923490733916,20.1301103293388,43.7454672642896));
#68499=CARTESIAN_POINT('Ctrl Pts',(32.3186793550125,20.2071088986255,43.7496839410353));
#68500=CARTESIAN_POINT('Ctrl Pts',(32.3452328349292,20.2847601745446,43.753936361989));
#68501=CARTESIAN_POINT('Ctrl Pts',(32.367871560611,20.3637182022701,43.7581887829428));
#68502=CARTESIAN_POINT('Ctrl Pts',(32.3864861868637,20.4435524014708,43.7624412038965));
#68503=CARTESIAN_POINT('Ctrl Pts',(32.4049710746478,20.5228301797903,43.7666639867273));
#68504=CARTESIAN_POINT('Ctrl Pts',(32.4194877563476,20.6029714819369,43.770886769558));
#68505=CARTESIAN_POINT('Ctrl Pts',(32.4299809185601,20.6835462349192,43.7751095523888));
#68506=CARTESIAN_POINT('Ctrl Pts',(32.4405845521055,20.7649692736884,43.779376792404));
#68507=CARTESIAN_POINT('Ctrl Pts',(32.4470794111771,20.8468344584216,43.7836440324193));
#68508=CARTESIAN_POINT('Ctrl Pts',(32.4494624033538,20.928696531949,43.7879112724345));
#68509=CARTESIAN_POINT('Ctrl Pts',(32.4518453955305,21.0105586054765,43.7921785124497));
#68510=CARTESIAN_POINT('Ctrl Pts',(32.4501165951023,21.0924170865121,43.7964457524649));
#68511=CARTESIAN_POINT('Ctrl Pts',(32.444326595155,21.1738325234752,43.8007129924802));
#68512=CARTESIAN_POINT('Ctrl Pts',(32.4385848805194,21.2545690019261,43.8049446461369));
#68513=CARTESIAN_POINT('Ctrl Pts',(32.4288280197687,21.3351717365329,43.8091762997935));
#68514=CARTESIAN_POINT('Ctrl Pts',(32.415067561655,21.4152094924755,43.8134079534502));
#68515=CARTESIAN_POINT('Ctrl Pts',(32.4013268084274,21.4951326348746,43.8176335474065));
#68516=CARTESIAN_POINT('Ctrl Pts',(32.3835939224315,21.5744919512168,43.8218591413628));
#68517=CARTESIAN_POINT('Ctrl Pts',(32.3619323386008,21.6528597689182,43.8260847353191));
#68518=CARTESIAN_POINT('Ctrl Pts',(32.3402102929162,21.7314463270209,43.8303221237612));
#68519=CARTESIAN_POINT('Ctrl Pts',(32.3145376254357,21.8090353729155,43.8345595122034));
#68520=CARTESIAN_POINT('Ctrl Pts',(32.2850302874115,21.8852044032945,43.8387969006455));
#68521=CARTESIAN_POINT('Ctrl Pts',(32.2556579080544,21.9610250569137,43.843014908407));
#68522=CARTESIAN_POINT('Ctrl Pts',(32.2224860218687,22.0354382173368,43.8472329161685));
#68523=CARTESIAN_POINT('Ctrl Pts',(32.1856788016498,22.1080426102,43.85145092393));
#68524=CARTESIAN_POINT('Ctrl Pts',(32.1488836885224,22.1806231211176,43.8556675442515));
#68525=CARTESIAN_POINT('Ctrl Pts',(32.1084558260338,22.2513956317458,43.8598841645731));
#68526=CARTESIAN_POINT('Ctrl Pts',(32.0646064667045,22.3199812073063,43.8641007848947));
#68527=CARTESIAN_POINT('Ctrl Pts',(32.0207581060368,22.3885652208422,43.8683173091834));
#68528=CARTESIAN_POINT('Ctrl Pts',(31.9734886547699,22.4549620073315,43.8725338334722));
#68529=CARTESIAN_POINT('Ctrl Pts',(31.9230532683568,22.518820719197,43.876750357761));
#68530=CARTESIAN_POINT('Ctrl Pts',(31.8721858686315,22.5832264242669,43.8810029994418));
#68531=CARTESIAN_POINT('Ctrl Pts',(31.8180983200932,22.6450499771179,43.8852556411226));
#68532=CARTESIAN_POINT('Ctrl Pts',(31.7610933379343,22.7039661103096,43.8895082828034));
#68533=CARTESIAN_POINT('Ctrl Pts',(31.7044901900368,22.7624669373302,43.8937309471548));
#68534=CARTESIAN_POINT('Ctrl Pts',(31.6450109930267,22.8181009278192,43.8979536115062));
#68535=CARTESIAN_POINT('Ctrl Pts',(31.5829872353128,22.8705885872732,43.9021762758576));
#68536=CARTESIAN_POINT('Ctrl Pts',(31.5203030036198,22.9236351734122,43.9064439062031));
#68537=CARTESIAN_POINT('Ctrl Pts',(31.4550200838409,22.9734677261952,43.9107115365487));
#68538=CARTESIAN_POINT('Ctrl Pts',(31.3875111489145,23.0198423358366,43.9149791668942));
#68539=CARTESIAN_POINT('Ctrl Pts',(31.3200022139882,23.066216945478,43.9192467972397));
#68540=CARTESIAN_POINT('Ctrl Pts',(31.2502677090293,23.109133413648,43.9235144275852));
#68541=CARTESIAN_POINT('Ctrl Pts',(31.1787045179634,23.1483961248644,43.9277820579308));
#68542=CARTESIAN_POINT('Ctrl Pts',(31.1078303443356,23.1872808108379,43.9320085991118));
#68543=CARTESIAN_POINT('Ctrl Pts',(31.0348951900078,23.2227285053627,43.9362351402929));
#68544=CARTESIAN_POINT('Ctrl Pts',(30.9602666044256,23.2545150916383,43.940461681474));
#68545=CARTESIAN_POINT('Ctrl Pts',(30.8857454103099,23.2862559366194,43.9446821406095));
#68546=CARTESIAN_POINT('Ctrl Pts',(30.8095360495221,23.3143459549914,43.948902599745));
#68547=CARTESIAN_POINT('Ctrl Pts',(30.7320312767652,23.3386065209516,43.9531230588805));
#68548=CARTESIAN_POINT('Ctrl Pts',(30.6541920904257,23.3629717651464,43.9573617282347));
#68549=CARTESIAN_POINT('Ctrl Pts',(30.575046703461,23.3834742016837,43.9616003975889));
#68550=CARTESIAN_POINT('Ctrl Pts',(30.4950139674654,23.399981546182,43.9658390669431));
#68551=CARTESIAN_POINT('Ctrl Pts',(30.4154686292597,23.4163883612766,43.9700519228842));
#68552=CARTESIAN_POINT('Ctrl Pts',(30.3350471806115,23.4288485106995,43.9742647788253));
#68553=CARTESIAN_POINT('Ctrl Pts',(30.2541749284838,23.4372823709473,43.9784776347664));
#68554=CARTESIAN_POINT('Ctrl Pts',(30.1733292166686,23.4457134634065,43.9826891081503));
#68555=CARTESIAN_POINT('Ctrl Pts',(30.0920334583339,23.4501208421543,43.9869005815342));
#68556=CARTESIAN_POINT('Ctrl Pts',(30.0107197320548,23.4504765531106,43.9911120549181));
#68557=CARTESIAN_POINT('Ctrl Pts',(29.9294076336576,23.4508322569456,43.9953234439893));
#68558=CARTESIAN_POINT('Ctrl Pts',(29.8480780341017,23.4471364533416,43.9995348330605));
#68559=CARTESIAN_POINT('Ctrl Pts',(29.7671632146717,23.439413306801,44.0037462221316));
#68560=CARTESIAN_POINT('Ctrl Pts',(29.6853385920691,23.4316033214925,44.0080049639024));
#68561=CARTESIAN_POINT('Ctrl Pts',(29.6039386220286,23.4196748863583,44.0122637056732));
#68562=CARTESIAN_POINT('Ctrl Pts',(29.5234033041919,23.4037066875026,44.016522447444));
#68563=CARTESIAN_POINT('Ctrl Pts',(29.4436458131195,23.3878927128157,44.0207400574056));
#68564=CARTESIAN_POINT('Ctrl Pts',(29.364736785917,23.3681168484542,44.0249576673671));
#68565=CARTESIAN_POINT('Ctrl Pts',(29.287089848896,23.3445062095147,44.0291752773286));
#68566=CARTESIAN_POINT('Ctrl Pts',(29.2083070461721,23.3205501800675,44.0334545850041));
#68567=CARTESIAN_POINT('Ctrl Pts',(29.1308240250191,23.2926464458688,44.0377338926795));
#68568=CARTESIAN_POINT('Ctrl Pts',(29.0550514991216,23.2609782353414,44.0420132003549));
#68569=CARTESIAN_POINT('Ctrl Pts',(28.979278973224,23.229310024814,44.0462925080303));
#68570=CARTESIAN_POINT('Ctrl Pts',(28.9052173589904,23.1938776115835,44.0505718157057));
#68571=CARTESIAN_POINT('Ctrl Pts',(28.8332493702964,23.154911417689,44.0548511233811));
#68572=CARTESIAN_POINT('Ctrl Pts',(28.7619658003649,23.1163157940256,44.0590897346509));
#68573=CARTESIAN_POINT('Ctrl Pts',(28.6924677344914,23.0741080608761,44.0633283459206));
#68574=CARTESIAN_POINT('Ctrl Pts',(28.625144019835,23.0284775778412,44.0675669571904));
#68575=CARTESIAN_POINT('Ctrl Pts',(28.5579170096759,22.9829126389158,44.071799480074));
#68576=CARTESIAN_POINT('Ctrl Pts',(28.4928585273544,22.9339349732179,44.0760320029576));
#68577=CARTESIAN_POINT('Ctrl Pts',(28.4303327142287,22.8817797060175,44.0802645258412));
#68578=CARTESIAN_POINT('Ctrl Pts',(28.3677606663616,22.8295858725807,44.0845001784658));
#68579=CARTESIAN_POINT('Ctrl Pts',(28.3077254335474,22.7742099779915,44.0887358310904));
#68580=CARTESIAN_POINT('Ctrl Pts',(28.2505627290682,22.7159310840109,44.092971483715));
#68581=CARTESIAN_POINT('Ctrl Pts',(28.1935462621439,22.6578012830977,44.0971963004023));
#68582=CARTESIAN_POINT('Ctrl Pts',(28.1393879844096,22.596783633823,44.1014211170895));
#68583=CARTESIAN_POINT('Ctrl Pts',(28.0883864516113,22.5331940162996,44.1056459337768));
#68584=CARTESIAN_POINT('Ctrl Pts',(28.0374023959192,22.4696261895426,44.1098693027121));
#68585=CARTESIAN_POINT('Ctrl Pts',(27.9895732262693,22.4034885060055,44.1140926716474));
#68586=CARTESIAN_POINT('Ctrl Pts',(27.9451577368483,22.3351305267897,44.1183160405828));
#68587=CARTESIAN_POINT('Ctrl Pts',(27.9007439865072,22.2667752241171,44.1225392441529));
#68588=CARTESIAN_POINT('Ctrl Pts',(27.8597439021257,22.1962001875561,44.126762447723));
#68589=CARTESIAN_POINT('Ctrl Pts',(27.8223726012033,22.1237834141906,44.1309856512932));
#68590=CARTESIAN_POINT('Ctrl Pts',(27.7848124509112,22.0510006952556,44.135230196088));
#68591=CARTESIAN_POINT('Ctrl Pts',(27.750918089743,21.9763579869771,44.1394747408829));
#68592=CARTESIAN_POINT('Ctrl Pts',(27.720860061516,21.9002618456911,44.1437192856778));
#68593=CARTESIAN_POINT('Ctrl Pts',(27.690911361364,21.8244424838589,44.1479483920711));
#68594=CARTESIAN_POINT('Ctrl Pts',(27.6647712405932,21.7471807006239,44.1521774984643));
#68595=CARTESIAN_POINT('Ctrl Pts',(27.6425585506347,21.6688946574868,44.1564066048576));
#68596=CARTESIAN_POINT('Ctrl Pts',(27.6202242291552,21.5901799381961,44.1606588688533));
#68597=CARTESIAN_POINT('Ctrl Pts',(27.6018605828103,21.5104301698075,44.164911132849));
#68598=CARTESIAN_POINT('Ctrl Pts',(27.5875361912525,21.4300797850207,44.1691633968447));
#68599=CARTESIAN_POINT('Ctrl Pts',(27.5732117996947,21.3497294002339,44.1734156608404));
#68600=CARTESIAN_POINT('Ctrl Pts',(27.5629266624284,21.2687788724357,44.177667924836));
#68601=CARTESIAN_POINT('Ctrl Pts',(27.5566964741207,21.1876649419204,44.1819201888317));
#68602=CARTESIAN_POINT('Ctrl Pts',(27.5519336184847,21.1256549476737,44.1851709604838));
#68603=CARTESIAN_POINT('Ctrl Pts',(27.5495309641018,21.0634593640365,44.1884217321359));
#68604=CARTESIAN_POINT('Ctrl Pts',(27.5495002973385,21.001207168577,44.1916725037879));
#68605=CARTESIAN_POINT('',(28.3849103233787,19.1570578993166,44.2999992595396));
#68606=CARTESIAN_POINT('Ctrl Pts',(27.549500297338,21.0012071676208,44.1916725038378));
#68607=CARTESIAN_POINT('Ctrl Pts',(27.5494613164988,20.9220776968105,44.1958045965079));
#68608=CARTESIAN_POINT('Ctrl Pts',(27.5532593294191,20.8427755817736,44.1999366891779));
#68609=CARTESIAN_POINT('Ctrl Pts',(27.5609182421575,20.7637153653744,44.2040687818479));
#68610=CARTESIAN_POINT('Ctrl Pts',(27.568565872763,20.6847716103984,44.2081947876462));
#68611=CARTESIAN_POINT('Ctrl Pts',(27.5800630653957,20.6060695276488,44.2123207934445));
#68612=CARTESIAN_POINT('Ctrl Pts',(27.5953817158509,20.5280241981458,44.2164467992429));
#68613=CARTESIAN_POINT('Ctrl Pts',(27.6106878555248,20.4500426084648,44.2205694353216));
#68614=CARTESIAN_POINT('Ctrl Pts',(27.6298091738289,20.3727171850489,44.2246920714003));
#68615=CARTESIAN_POINT('Ctrl Pts',(27.6526658524374,20.2964570733163,44.2288147074791));
#68616=CARTESIAN_POINT('Ctrl Pts',(27.6755115528644,20.2202335897118,44.2329353634343));
#68617=CARTESIAN_POINT('Ctrl Pts',(27.7020889161023,20.1450748694144,44.2370560193895));
#68618=CARTESIAN_POINT('Ctrl Pts',(27.7322676052255,20.0713773448326,44.2411766753447));
#68619=CARTESIAN_POINT('Ctrl Pts',(27.7624419464753,19.9976904379254,44.2452967376329));
#68620=CARTESIAN_POINT('Ctrl Pts',(27.796216397791,19.9254647595421,44.2494167999212));
#68621=CARTESIAN_POINT('Ctrl Pts',(27.8334122084363,19.8550774736048,44.2535368622095));
#68622=CARTESIAN_POINT('Ctrl Pts',(27.8706384784948,19.7846325479659,44.2576602983906));
#68623=CARTESIAN_POINT('Ctrl Pts',(27.9112914753926,19.7160294535448,44.2617837345717));
#68624=CARTESIAN_POINT('Ctrl Pts',(27.9551465739149,19.6496205289519,44.2659071707528));
#68625=CARTESIAN_POINT('Ctrl Pts',(27.9990196432335,19.5831843915309,44.2700322966218));
#68626=CARTESIAN_POINT('Ctrl Pts',(28.046097135931,19.5189446060218,44.2741574224909));
#68627=CARTESIAN_POINT('Ctrl Pts',(28.0961127707103,19.4572220937064,44.2782825483599));
#68628=CARTESIAN_POINT('Ctrl Pts',(28.1462101040697,19.3953987600851,44.2824144124605));
#68629=CARTESIAN_POINT('Ctrl Pts',(28.1992548350109,19.3361012714435,44.2865462765611));
#68630=CARTESIAN_POINT('Ctrl Pts',(28.2549427764082,19.279614712807,44.2906781406616));
#68631=CARTESIAN_POINT('Ctrl Pts',(28.2968184616681,19.2371384909981,44.2937851802876));
#68632=CARTESIAN_POINT('Ctrl Pts',(28.3401879810753,19.1962509880967,44.2968922199136));
#68633=CARTESIAN_POINT('Ctrl Pts',(28.3849103233787,19.1570578993166,44.2999992595396));
#68634=CARTESIAN_POINT('',(27.5495,21.,44.3));
#68635=CARTESIAN_POINT('Origin',(30.,21.,44.3));
#68636=CARTESIAN_POINT('',(27.5535569140831,21.1409484919019,44.3));
#68637=CARTESIAN_POINT('Origin',(30.,21.,44.3));
#68638=CARTESIAN_POINT('',(27.5495009938442,20.9977930044395,43.5073274962121));
#68639=CARTESIAN_POINT('Ctrl Pts',(27.5535569140831,21.1409484919019,44.3));
#68640=CARTESIAN_POINT('Ctrl Pts',(27.6003946584625,21.9539112583056,44.2576897435897));
#68641=CARTESIAN_POINT('Ctrl Pts',(28.5681046611841,23.5154982516648,44.1730692307693));
#68642=CARTESIAN_POINT('Ctrl Pts',(31.3397609818422,23.5691170566576,44.0461384615384));
#68643=CARTESIAN_POINT('Ctrl Pts',(32.8826594919807,21.2691366249369,43.9192076923077));
#68644=CARTESIAN_POINT('Ctrl Pts',(31.792118108548,18.7255142460077,43.792276923077));
#68645=CARTESIAN_POINT('Ctrl Pts',(29.0622776960464,18.2600412506062,43.6653461538461));
#68646=CARTESIAN_POINT('Ctrl Pts',(27.6613697729277,19.7865866467302,43.5703630540116));
#68647=CARTESIAN_POINT('Ctrl Pts',(27.5479559594343,20.7983452768987,43.5176902105872));
#68648=CARTESIAN_POINT('Ctrl Pts',(27.5497643553418,20.9977907903747,43.507327623573));
#68649=CARTESIAN_POINT('',(27.5495000808206,21.0006293661639,42.707327496182));
#68650=CARTESIAN_POINT('Ctrl Pts',(27.5495009938442,20.9977930044395,43.5073274962121));
#68651=CARTESIAN_POINT('Ctrl Pts',(27.5494286713727,21.0780949985435,43.5031556579785));
#68652=CARTESIAN_POINT('Ctrl Pts',(27.5533077961739,21.158500472361,43.498983819745));
#68653=CARTESIAN_POINT('Ctrl Pts',(27.5611421721604,21.2385848813008,43.4948119815114));
#68654=CARTESIAN_POINT('Ctrl Pts',(27.5689715766591,21.3186184707931,43.490642790616));
#68655=CARTESIAN_POINT('Ctrl Pts',(27.5807512071824,21.3983309264438,43.4864735997207));
#68656=CARTESIAN_POINT('Ctrl Pts',(27.5964328306478,21.4772998139662,43.4823044088253));
#68657=CARTESIAN_POINT('Ctrl Pts',(27.6121095754188,21.5562441335559,43.4781365150028));
#68658=CARTESIAN_POINT('Ctrl Pts',(27.6316858108099,21.6344448768983,43.4739686211803));
#68659=CARTESIAN_POINT('Ctrl Pts',(27.6550619445421,21.7114884159741,43.4698007273578));
#68660=CARTESIAN_POINT('Ctrl Pts',(27.678438366853,21.7885329061537,43.4656327820825));
#68661=CARTESIAN_POINT('Ctrl Pts',(27.7056146401583,21.8644197081247,43.4614648368073));
#68662=CARTESIAN_POINT('Ctrl Pts',(27.7364413729418,21.9387505482663,43.4572968915321));
#68663=CARTESIAN_POINT('Ctrl Pts',(27.7672986247002,22.0131549771682,43.4531248199221));
#68664=CARTESIAN_POINT('Ctrl Pts',(27.8018133675902,22.0859999278558,43.4489527483122));
#68665=CARTESIAN_POINT('Ctrl Pts',(27.8397884237585,22.1569080325904,43.4447806767022));
#68666=CARTESIAN_POINT('Ctrl Pts',(27.8777834423162,22.2278534116662,43.4406064119548));
#68667=CARTESIAN_POINT('Ctrl Pts',(27.9192421474788,22.2968595105345,43.4364321472074));
#68668=CARTESIAN_POINT('Ctrl Pts',(27.9639231871326,22.3635767166184,43.43225788246));
#68669=CARTESIAN_POINT('Ctrl Pts',(28.0086803306937,22.430407560167,43.4280765078096));
#68670=CARTESIAN_POINT('Ctrl Pts',(28.0566704805754,22.4949413460911,43.4238951331592));
#68671=CARTESIAN_POINT('Ctrl Pts',(28.1076113994249,22.5568608269249,43.4197137585088));
#68672=CARTESIAN_POINT('Ctrl Pts',(28.1410294454937,22.5974809827798,43.4169707108008));
#68673=CARTESIAN_POINT('Ctrl Pts',(28.1757165693982,22.6369767694273,43.4142276630927));
#68674=CARTESIAN_POINT('Ctrl Pts',(28.2115849037342,22.6752676483024,43.4114846153846));
#68675=CARTESIAN_POINT('Ctrl Pts',(28.2669112616675,22.7343307441901,43.4072535061866));
#68676=CARTESIAN_POINT('Ctrl Pts',(28.325270368973,22.7907608722937,43.4030223969887));
#68677=CARTESIAN_POINT('Ctrl Pts',(28.3863816544145,22.8442304858097,43.3987912877907));
#68678=CARTESIAN_POINT('Ctrl Pts',(28.4474053256908,22.8976234408899,43.3945662446589));
#68679=CARTESIAN_POINT('Ctrl Pts',(28.5111729915882,22.9480640075706,43.390341201527));
#68680=CARTESIAN_POINT('Ctrl Pts',(28.5773660289269,22.995260091905,43.3861161583952));
#68681=CARTESIAN_POINT('Ctrl Pts',(28.6436643454633,23.042531241021,43.3818843953852));
#68682=CARTESIAN_POINT('Ctrl Pts',(28.7123954226579,23.0865472464855,43.3776526323751));
#68683=CARTESIAN_POINT('Ctrl Pts',(28.7832044057296,23.1270540030202,43.373420869365));
#68684=CARTESIAN_POINT('Ctrl Pts',(28.8537738259422,23.1674237160049,43.3692034233696));
#68685=CARTESIAN_POINT('Ctrl Pts',(28.9264067172877,23.2043076417871,43.3649859773742));
#68686=CARTESIAN_POINT('Ctrl Pts',(29.0007228872578,23.2374975981997,43.3607685313787));
#68687=CARTESIAN_POINT('Ctrl Pts',(29.0750145191491,23.2706765957893,43.3565524779204));
#68688=CARTESIAN_POINT('Ctrl Pts',(29.150987901736,23.300163856706,43.352336424462));
#68689=CARTESIAN_POINT('Ctrl Pts',(29.2282403505548,23.3257982056679,43.3481203710036));
#68690=CARTESIAN_POINT('Ctrl Pts',(29.3054909610785,23.3514319446363,43.3439044178702));
#68691=CARTESIAN_POINT('Ctrl Pts',(29.3840201356804,23.3732128085744,43.3396884647369));
#68692=CARTESIAN_POINT('Ctrl Pts',(29.4634087876326,23.3910290924224,43.3354725116035));
#68693=CARTESIAN_POINT('Ctrl Pts',(29.5433109291996,23.4089606128501,43.3312292894827));
#68694=CARTESIAN_POINT('Ctrl Pts',(29.6240832450702,23.4228759621529,43.3269860673619));
#68695=CARTESIAN_POINT('Ctrl Pts',(29.705288575144,23.4327135931012,43.3227428452411));
#68696=CARTESIAN_POINT('Ctrl Pts',(29.7860891322218,23.4425021877689,43.3185207737237));
#68697=CARTESIAN_POINT('Ctrl Pts',(29.8673179250657,23.4482536436492,43.3142987022063));
#68698=CARTESIAN_POINT('Ctrl Pts',(29.9485415435488,23.449959648088,43.3100766306889));
#68699=CARTESIAN_POINT('Ctrl Pts',(30.0303755005355,23.4516784719532,43.3058228332664));
#68700=CARTESIAN_POINT('Ctrl Pts',(30.112203725588,23.449290807471,43.3015690358439));
#68701=CARTESIAN_POINT('Ctrl Pts',(30.1935873294616,23.4428414184862,43.2973152384213));
#68702=CARTESIAN_POINT('Ctrl Pts',(30.2749709333352,23.4363920295015,43.2930614409988));
#68703=CARTESIAN_POINT('Ctrl Pts',(30.3559094524285,23.4258810401938,43.2888076435763));
#68704=CARTESIAN_POINT('Ctrl Pts',(30.4359754457396,23.4114053289964,43.2845538461538));
#68705=CARTESIAN_POINT('Ctrl Pts',(30.5156268278807,23.3970045783573,43.2803220764594));
#68706=CARTESIAN_POINT('Ctrl Pts',(30.5947128374763,23.3786262068457,43.2760903067649));
#68707=CARTESIAN_POINT('Ctrl Pts',(30.672805973043,23.3563281547012,43.2718585370705));
#68708=CARTESIAN_POINT('Ctrl Pts',(30.7507873255897,23.334062020133,43.2676328247585));
#68709=CARTESIAN_POINT('Ctrl Pts',(30.827778183594,23.3078874747667,43.2634071124466));
#68710=CARTESIAN_POINT('Ctrl Pts',(30.9033601775532,23.2779136593846,43.2591814001347));
#68711=CARTESIAN_POINT('Ctrl Pts',(30.9790474227333,23.2478981041582,43.2549498033342));
#68712=CARTESIAN_POINT('Ctrl Pts',(31.053321418879,23.214072790252,43.2507182065337));
#68713=CARTESIAN_POINT('Ctrl Pts',(31.1257762843647,23.1765978056504,43.2464866097332));
#68714=CARTESIAN_POINT('Ctrl Pts',(31.1980005894887,23.1392420710943,43.2422684783982));
#68715=CARTESIAN_POINT('Ctrl Pts',(31.2684169019442,23.0982600572565,43.2380503470632));
#68716=CARTESIAN_POINT('Ctrl Pts',(31.336643916087,23.0538581478738,43.2338322157282));
#68717=CARTESIAN_POINT('Ctrl Pts',(31.4048484800272,23.0094708490068,43.2296154723757));
#68718=CARTESIAN_POINT('Ctrl Pts',(31.4708647870291,22.9616661426764,43.2253987290232));
#68719=CARTESIAN_POINT('Ctrl Pts',(31.5343388049374,22.9106948164642,43.2211819856707));
#68720=CARTESIAN_POINT('Ctrl Pts',(31.5978113671367,22.8597246592251,43.2169653390247));
#68721=CARTESIAN_POINT('Ctrl Pts',(31.6587413944808,22.8055883183896,43.2127486923787));
#68722=CARTESIAN_POINT('Ctrl Pts',(31.7168075005881,22.7485772090258,43.2085320457327));
#68723=CARTESIAN_POINT('Ctrl Pts',(31.7752284416995,22.6912177116162,43.2042896316653));
#68724=CARTESIAN_POINT('Ctrl Pts',(31.8307499903644,22.6309485138542,43.2000472175978));
#68725=CARTESIAN_POINT('Ctrl Pts',(31.8830833737838,22.5681030761335,43.1958048035303));
#68726=CARTESIAN_POINT('Ctrl Pts',(31.9351743937326,22.5055486847277,43.1915820366962));
#68727=CARTESIAN_POINT('Ctrl Pts',(31.9841064758759,22.4404422706323,43.1873592698621));
#68728=CARTESIAN_POINT('Ctrl Pts',(32.0296372758375,22.3731433932882,43.183136503028));
#68729=CARTESIAN_POINT('Ctrl Pts',(32.0754858369806,22.3053748345241,43.1788842653438));
#68730=CARTESIAN_POINT('Ctrl Pts',(32.1178852100249,22.2353835011774,43.1746320276597));
#68731=CARTESIAN_POINT('Ctrl Pts',(32.1566349538099,22.1635617413809,43.1703797899755));
#68732=CARTESIAN_POINT('Ctrl Pts',(32.1953846975949,22.0917399815844,43.1661275522914));
#68733=CARTESIAN_POINT('Ctrl Pts',(32.2304846650877,22.0180882506895,43.1618753146072));
#68734=CARTESIAN_POINT('Ctrl Pts',(32.2617842872632,21.9430175437865,43.1576230769231));
#68735=CARTESIAN_POINT('Ctrl Pts',(32.2929329194873,21.8683089793506,43.1533913521115));
#68736=CARTESIAN_POINT('Ctrl Pts',(32.3204342772004,21.7919158010366,43.1491596272999));
#68737=CARTESIAN_POINT('Ctrl Pts',(32.3441049330204,21.7142284739421,43.1449279024883));
#68738=CARTESIAN_POINT('Ctrl Pts',(32.367741711881,21.636652331364,43.1407022340349));
#68739=CARTESIAN_POINT('Ctrl Pts',(32.3875585431245,21.5577861594449,43.1364765655815));
#68740=CARTESIAN_POINT('Ctrl Pts',(32.4034199553765,21.4780405506839,43.1322508971281));
#68741=CARTESIAN_POINT('Ctrl Pts',(32.4193036618295,21.3981828545116,43.1280192892349));
#68742=CARTESIAN_POINT('Ctrl Pts',(32.4312206572839,21.3174436868484,43.1237876813418));
#68743=CARTESIAN_POINT('Ctrl Pts',(32.4390850326013,21.2362508280205,43.1195560734486));
#68744=CARTESIAN_POINT('Ctrl Pts',(32.4469242857399,21.1553173339147,43.1153379831212));
#68745=CARTESIAN_POINT('Ctrl Pts',(32.4507367093211,21.0739335052662,43.1111198927937));
#68746=CARTESIAN_POINT('Ctrl Pts',(32.4504886192374,20.9925316007048,43.1069018024663));
#68747=CARTESIAN_POINT('Ctrl Pts',(32.4502406107199,20.9111564591811,43.1026850989481));
#68748=CARTESIAN_POINT('Ctrl Pts',(32.445934741115,20.82976371797,43.0984683954298));
#68749=CARTESIAN_POINT('Ctrl Pts',(32.4375894233738,20.7487868374147,43.0942516919116));
#68750=CARTESIAN_POINT('Ctrl Pts',(32.4292442945833,20.6678117902988,43.0900350838659));
#68751=CARTESIAN_POINT('Ctrl Pts',(32.4168599482741,20.5872530473404,43.0858184758203));
#68752=CARTESIAN_POINT('Ctrl Pts',(32.4005066395469,20.5075387086366,43.0816018677746));
#68753=CARTESIAN_POINT('Ctrl Pts',(32.3840530559995,20.4273355794922,43.0773594044344));
#68754=CARTESIAN_POINT('Ctrl Pts',(32.3635817510493,20.3479877143646,43.0731169410942));
#68755=CARTESIAN_POINT('Ctrl Pts',(32.3392160031704,20.2699186754126,43.068874477754));
#68756=CARTESIAN_POINT('Ctrl Pts',(32.314963580141,20.1922127347789,43.0646517460684));
#68757=CARTESIAN_POINT('Ctrl Pts',(32.2868530740405,20.1157741716784,43.0604290143827));
#68758=CARTESIAN_POINT('Ctrl Pts',(32.2550548796411,20.0410016997893,43.056206282697));
#68759=CARTESIAN_POINT('Ctrl Pts',(32.223033809021,19.9657051413519,43.0519539535296));
#68760=CARTESIAN_POINT('Ctrl Pts',(32.1872733645652,19.8920985502412,43.0477016243621));
#68761=CARTESIAN_POINT('Ctrl Pts',(32.1479942456607,19.8205632824909,43.0434492951947));
#68762=CARTESIAN_POINT('Ctrl Pts',(32.1087151267562,19.7490280147407,43.0391969660272));
#68763=CARTESIAN_POINT('Ctrl Pts',(32.0659176360555,19.6795644410844,43.0349446368598));
#68764=CARTESIAN_POINT('Ctrl Pts',(32.0198652116927,19.6125221527557,43.0306923076923));
#68765=CARTESIAN_POINT('Ctrl Pts',(31.9740374401133,19.545806909895,43.0264607222229));
#68766=CARTESIAN_POINT('Ctrl Pts',(31.9248150219584,19.4812398037033,43.0222291367535));
#68767=CARTESIAN_POINT('Ctrl Pts',(31.8724262453245,19.4191868529709,43.017997551284));
#68768=CARTESIAN_POINT('Ctrl Pts',(31.8201124824235,19.3572227537783,43.01377202488));
#68769=CARTESIAN_POINT('Ctrl Pts',(31.7646416629189,19.2977660124396,43.0095464984759));
#68770=CARTESIAN_POINT('Ctrl Pts',(31.7062850155279,19.2411533052068,43.0053209720718));
#68771=CARTESIAN_POINT('Ctrl Pts',(31.6478438939406,19.1844586482192,43.0010893290047));
#68772=CARTESIAN_POINT('Ctrl Pts',(31.5865088627317,19.130616642487,42.9968576859376));
#68773=CARTESIAN_POINT('Ctrl Pts',(31.5225925351889,19.0799317142906,42.9926260428705));
#68774=CARTESIAN_POINT('Ctrl Pts',(31.4588831426806,19.029410883247,42.9884081001401));
#68775=CARTESIAN_POINT('Ctrl Pts',(31.3926094975944,18.9820270212694,42.9841901574096));
#68776=CARTESIAN_POINT('Ctrl Pts',(31.3241162903053,18.9380430897451,42.9799722146792));
#68777=CARTESIAN_POINT('Ctrl Pts',(31.2556456313987,18.8940736379998,42.9757556605212));
#68778=CARTESIAN_POINT('Ctrl Pts',(31.1849572521773,18.8535021449235,42.9715391063633));
#68779=CARTESIAN_POINT('Ctrl Pts',(31.1124251378782,18.8165484748645,42.9673225522054));
#68780=CARTESIAN_POINT('Ctrl Pts',(31.0398946927739,18.779595655227,42.9631060950838));
#68781=CARTESIAN_POINT('Ctrl Pts',(30.9655210116341,18.7462607030743,42.9588896379622));
#68782=CARTESIAN_POINT('Ctrl Pts',(30.8897017252006,18.7167170367703,42.9546731808406));
#68783=CARTESIAN_POINT('Ctrl Pts',(30.8134116811143,18.6869899355164,42.9504305439756));
#68784=CARTESIAN_POINT('Ctrl Pts',(30.7356584561104,18.6611015497436,42.9461879071107));
#68785=CARTESIAN_POINT('Ctrl Pts',(30.6568647556537,18.6391783331264,42.9419452702458));
#68786=CARTESIAN_POINT('Ctrl Pts',(30.57844357748,18.6173587654894,42.9377226917962));
#68787=CARTESIAN_POINT('Ctrl Pts',(30.4989922097044,18.5994670063165,42.9335001133467));
#68788=CARTESIAN_POINT('Ctrl Pts',(30.418937973609,18.585576419874,42.9292775348971));
#68789=CARTESIAN_POINT('Ctrl Pts',(30.338313317874,18.5715868572411,42.9250248688245));
#68790=CARTESIAN_POINT('Ctrl Pts',(30.2570776437222,18.5616557699678,42.9207722027519));
#68791=CARTESIAN_POINT('Ctrl Pts',(30.1756711583688,18.5558048576029,42.9165195366793));
#68792=CARTESIAN_POINT('Ctrl Pts',(30.0942646730153,18.5499539452381,42.9122668706067));
#68793=CARTESIAN_POINT('Ctrl Pts',(30.0126878524215,18.5481831548462,42.9080142045341));
#68794=CARTESIAN_POINT('Ctrl Pts',(29.931377428188,18.5504610244705,42.9037615384615));
#68795=CARTESIAN_POINT('Ctrl Pts',(29.8504684104,18.5527276489002,42.8995298665922));
#68796=CARTESIAN_POINT('Ctrl Pts',(29.7695205115425,18.5590114931233,42.8952981947228));
#68797=CARTESIAN_POINT('Ctrl Pts',(29.6889650674848,18.5693195354479,42.8910665228535));
#68798=CARTESIAN_POINT('Ctrl Pts',(29.6085249427001,18.5796128212783,42.8868409088407));
#68799=CARTESIAN_POINT('Ctrl Pts',(29.5284766140614,18.5939188051355,42.8826152948279));
#68800=CARTESIAN_POINT('Ctrl Pts',(29.4492500856818,18.6121924738626,42.8783896808151));
#68801=CARTESIAN_POINT('Ctrl Pts',(29.3699109256761,18.6304921211737,42.8741580594991));
#68802=CARTESIAN_POINT('Ctrl Pts',(29.291396372574,18.6527707129078,42.869926438183));
#68803=CARTESIAN_POINT('Ctrl Pts',(29.2141317794757,18.6789309812136,42.865694816867));
#68804=CARTESIAN_POINT('Ctrl Pts',(29.1371153003262,18.7050072430268,42.8614767842368));
#68805=CARTESIAN_POINT('Ctrl Pts',(29.0613412126541,18.7349401559119,42.8572587516065));
#68806=CARTESIAN_POINT('Ctrl Pts',(28.9872174939851,18.7685829960516,42.8530407189762));
#68807=CARTESIAN_POINT('Ctrl Pts',(28.913118165142,18.8022147662796,42.8488240742564));
#68808=CARTESIAN_POINT('Ctrl Pts',(28.8406685498018,18.8395538475973,42.8446074295365));
#68809=CARTESIAN_POINT('Ctrl Pts',(28.770256335599,18.8804055175894,42.8403907848167));
#68810=CARTESIAN_POINT('Ctrl Pts',(28.6998457327647,18.9212562526996,42.8361742365938));
#68811=CARTESIAN_POINT('Ctrl Pts',(28.6314728398337,18.9656191824287,42.831957688371));
#68812=CARTESIAN_POINT('Ctrl Pts',(28.5654991754205,19.0132545119516,42.8277411401482));
#68813=CARTESIAN_POINT('Ctrl Pts',(28.4991189763304,19.061183373954,42.8234986092384));
#68814=CARTESIAN_POINT('Ctrl Pts',(28.4351680702968,19.1124248375287,42.8192560783286));
#68815=CARTESIAN_POINT('Ctrl Pts',(28.3739821015297,19.1666925942837,42.8150135474188));
#68816=CARTESIAN_POINT('Ctrl Pts',(28.3130825684725,19.2207063022144,42.8107908774735));
#68817=CARTESIAN_POINT('Ctrl Pts',(28.2549224384151,19.277717663908,42.8065682075282));
#68818=CARTESIAN_POINT('Ctrl Pts',(28.1997953246124,19.3374076336298,42.8023455375829));
#68819=CARTESIAN_POINT('Ctrl Pts',(28.1442792823603,19.3975187233008,42.7980930761909));
#68820=CARTESIAN_POINT('Ctrl Pts',(28.0918395262494,19.4603459967167,42.7938406147989));
#68821=CARTESIAN_POINT('Ctrl Pts',(28.0427332253885,19.5255316134274,42.7895881534068));
#68822=CARTESIAN_POINT('Ctrl Pts',(27.9936269245276,19.5907172301381,42.7853356920148));
#68823=CARTESIAN_POINT('Ctrl Pts',(27.9478542927836,19.6582607618668,42.7810832306228));
#68824=CARTESIAN_POINT('Ctrl Pts',(27.9056259808701,19.7277784320356,42.7768307692308));
#68825=CARTESIAN_POINT('Ctrl Pts',(27.8622815994516,19.7991334134351,42.7724659177794));
#68826=CARTESIAN_POINT('Ctrl Pts',(27.8225174834268,19.872820964484,42.7681010663281));
#68827=CARTESIAN_POINT('Ctrl Pts',(27.7865834615437,19.948459474253,42.7637362148767));
#68828=CARTESIAN_POINT('Ctrl Pts',(27.7507120037736,20.0239662911021,42.7593789629938));
#68829=CARTESIAN_POINT('Ctrl Pts',(27.7186575600616,20.1014169309921,42.7550217111109));
#68830=CARTESIAN_POINT('Ctrl Pts',(27.6906253887226,20.1804030534542,42.750664459228));
#68831=CARTESIAN_POINT('Ctrl Pts',(27.6626474697683,20.2592363092169,42.7463156402026));
#68832=CARTESIAN_POINT('Ctrl Pts',(27.6386764648641,20.3395987325073,42.7419668211772));
#68833=CARTESIAN_POINT('Ctrl Pts',(27.6188700035032,20.4210611519486,42.7376180021518));
#68834=CARTESIAN_POINT('Ctrl Pts',(27.5990863563522,20.5024297383373,42.7332741923437));
#68835=CARTESIAN_POINT('Ctrl Pts',(27.5834578152745,20.5848953908551,42.7289303825357));
#68836=CARTESIAN_POINT('Ctrl Pts',(27.5720924813575,20.668013056101,42.7245865727276));
#68837=CARTESIAN_POINT('Ctrl Pts',(27.5607401778493,20.7510354265526,42.7202477431179));
#68838=CARTESIAN_POINT('Ctrl Pts',(27.5536414091132,20.8347079019049,42.7159089135083));
#68839=CARTESIAN_POINT('Ctrl Pts',(27.5508531415515,20.9185757053959,42.7115700838986));
#68840=CARTESIAN_POINT('Ctrl Pts',(27.5499443350539,20.9459115342094,42.7101558880031));
#68841=CARTESIAN_POINT('Ctrl Pts',(27.549493053573,20.9732680513757,42.7087416921076));
#68842=CARTESIAN_POINT('Ctrl Pts',(27.5495000808205,21.0006293655811,42.7073274962121));
#68843=CARTESIAN_POINT('',(27.5495007121296,21.0018681933898,41.907327496261));
#68844=CARTESIAN_POINT('Ctrl Pts',(27.5495000808206,21.0006293661639,42.707327496182));
#68845=CARTESIAN_POINT('Ctrl Pts',(27.5495225090421,21.0879558832018,42.7028139409837));
#68846=CARTESIAN_POINT('Ctrl Pts',(27.554217143938,21.1751558760659,42.6983003857854));
#68847=CARTESIAN_POINT('Ctrl Pts',(27.5635183022074,21.2617387749678,42.6937868305871));
#68848=CARTESIAN_POINT('Ctrl Pts',(27.5728554788347,21.3486569626314,42.6892557968295));
#68849=CARTESIAN_POINT('Ctrl Pts',(27.5868348224921,21.4349529215464,42.6847247630719));
#68850=CARTESIAN_POINT('Ctrl Pts',(27.6053392195364,21.5201442074171,42.6801937293143));
#68851=CARTESIAN_POINT('Ctrl Pts',(27.6238820452469,21.6055124127238,42.6756532858157));
#68852=CARTESIAN_POINT('Ctrl Pts',(27.6469685873783,21.6897710242904,42.6711128423172));
#68853=CARTESIAN_POINT('Ctrl Pts',(27.6744321572847,21.7724535318893,42.6665723988186));
#68854=CARTESIAN_POINT('Ctrl Pts',(27.701978129605,21.8553841222485,42.6620183320544));
#68855=CARTESIAN_POINT('Ctrl Pts',(27.7339272591392,21.9367288224191,42.6574642652903));
#68856=CARTESIAN_POINT('Ctrl Pts',(27.770064716571,22.0160407874285,42.6529101985262));
#68857=CARTESIAN_POINT('Ctrl Pts',(27.7780268982673,22.033515627137,42.6519067990175));
#68858=CARTESIAN_POINT('Ctrl Pts',(27.7861922314723,22.0508918886417,42.6509033995088));
#68859=CARTESIAN_POINT('Ctrl Pts',(27.7945581291948,22.0681649706386,42.6499000000001));
#68860=CARTESIAN_POINT('Ctrl Pts',(27.8298396974189,22.1410108792463,42.645668355125));
#68861=CARTESIAN_POINT('Ctrl Pts',(27.868800287091,22.2122431200328,42.64143671025));
#68862=CARTESIAN_POINT('Ctrl Pts',(27.9112691944474,22.2814655172635,42.637205065375));
#68863=CARTESIAN_POINT('Ctrl Pts',(27.9536773020586,22.3505888136608,42.632979478648));
#68864=CARTESIAN_POINT('Ctrl Pts',(27.9995835109626,22.4177075883245,42.6287538919211));
#68865=CARTESIAN_POINT('Ctrl Pts',(28.0487702554109,22.4824482229848,42.6245283051941));
#68866=CARTESIAN_POINT('Ctrl Pts',(28.0980273227617,22.5472814181385,42.6202966770931));
#68867=CARTESIAN_POINT('Ctrl Pts',(28.1505740934964,22.6097292533655,42.6160650489921));
#68868=CARTESIAN_POINT('Ctrl Pts',(28.2061472559131,22.6694437943614,42.611833420891));
#68869=CARTESIAN_POINT('Ctrl Pts',(28.2615415066392,22.7289660909534,42.6076154160517));
#68870=CARTESIAN_POINT('Ctrl Pts',(28.3199423871311,22.7857723127494,42.6033974112124));
#68871=CARTESIAN_POINT('Ctrl Pts',(28.3810486282775,22.8395506804646,42.5991794063731));
#68872=CARTESIAN_POINT('Ctrl Pts',(28.4421347609133,22.8933113510861,42.594962789572));
#68873=CARTESIAN_POINT('Ctrl Pts',(28.5059241375879,22.9440458394996,42.5907461727709));
#68874=CARTESIAN_POINT('Ctrl Pts',(28.5720800508865,22.9914805720679,42.5865295559697));
#68875=CARTESIAN_POINT('Ctrl Pts',(28.6382344488063,23.0389142180879,42.5823130357552));
#68876=CARTESIAN_POINT('Ctrl Pts',(28.7067548971705,23.0830479886162,42.5780965155406));
#68877=CARTESIAN_POINT('Ctrl Pts',(28.777274332073,23.1236506753683,42.573879995326));
#68878=CARTESIAN_POINT('Ctrl Pts',(28.8482293329644,23.1645041461694,42.569637431613));
#68879=CARTESIAN_POINT('Ctrl Pts',(28.9212076942577,23.2017825127837,42.5653948678999));
#68880=CARTESIAN_POINT('Ctrl Pts',(28.9958105432727,23.2352972475708,42.5611523041868));
#68881=CARTESIAN_POINT('Ctrl Pts',(29.0700630814104,23.2686546079909,42.5569296621823));
#68882=CARTESIAN_POINT('Ctrl Pts',(29.145924428273,23.2982834848223,42.5527070201778));
#68883=CARTESIAN_POINT('Ctrl Pts',(29.2229831312913,23.3240471242516,42.5484843781733));
#68884=CARTESIAN_POINT('Ctrl Pts',(29.3005871591401,23.3499930864006,42.544231853606));
#68885=CARTESIAN_POINT('Ctrl Pts',(29.3794050952921,23.3720187619487,42.5399793290386));
#68886=CARTESIAN_POINT('Ctrl Pts',(29.4590050457112,23.3900365498113,42.5357268044713));
#68887=CARTESIAN_POINT('Ctrl Pts',(29.5386049961303,23.4080543376739,42.5314742799039));
#68888=CARTESIAN_POINT('Ctrl Pts',(29.6189864824365,23.4220642186554,42.5272217553366));
#68889=CARTESIAN_POINT('Ctrl Pts',(29.6997130576233,23.4320316614382,42.5229692307692));
#68890=CARTESIAN_POINT('Ctrl Pts',(29.7800434783921,23.4419501903846,42.5187375748736));
#68891=CARTESIAN_POINT('Ctrl Pts',(29.8610160728231,23.44790300105,42.5145059189779));
#68892=CARTESIAN_POINT('Ctrl Pts',(29.9422054559273,23.4498183689154,42.5102742630823));
#68893=CARTESIAN_POINT('Ctrl Pts',(30.0232786093278,23.4517309947643,42.5060486651722));
#68894=CARTESIAN_POINT('Ctrl Pts',(30.1045674742399,23.4496176464594,42.5018230672621));
#68895=CARTESIAN_POINT('Ctrl Pts',(30.1856401684111,23.4434582005576,42.4975974693521));
#68896=CARTESIAN_POINT('Ctrl Pts',(30.2668285051076,23.4372899687893,42.4933658440265));
#68897=CARTESIAN_POINT('Ctrl Pts',(30.3477995863987,23.4270640473758,42.4891342187009));
#68898=CARTESIAN_POINT('Ctrl Pts',(30.4281182685965,23.4128126736433,42.4849025933753));
#68899=CARTESIAN_POINT('Ctrl Pts',(30.5081786443274,23.39860713261,42.4806845770403));
#68900=CARTESIAN_POINT('Ctrl Pts',(30.5875903487649,23.3804020565635,42.4764665607053));
#68901=CARTESIAN_POINT('Ctrl Pts',(30.6659279899837,23.3582811881021,42.4722485443703));
#68902=CARTESIAN_POINT('Ctrl Pts',(30.7442398540569,23.3361675985534,42.4680319159814));
#68903=CARTESIAN_POINT('Ctrl Pts',(30.8214779098029,23.3101409016125,42.4638152875924));
#68904=CARTESIAN_POINT('Ctrl Pts',(30.8972296111156,23.2803353426497,42.4595986592035));
#68905=CARTESIAN_POINT('Ctrl Pts',(30.9729795786242,23.2505304658763,42.4553821273247));
#68906=CARTESIAN_POINT('Ctrl Pts',(31.0472428272243,23.2169470702818,42.4511655954459));
#68907=CARTESIAN_POINT('Ctrl Pts',(31.1196259088075,23.1797678945996,42.4469490635671));
#68908=CARTESIAN_POINT('Ctrl Pts',(31.1924556332908,23.1423593032239,42.442706513398));
#68909=CARTESIAN_POINT('Ctrl Pts',(31.2633814775535,23.1013106072616,42.438463963229));
#68910=CARTESIAN_POINT('Ctrl Pts',(31.3320285743873,23.0568544253339,42.4342214130599));
#68911=CARTESIAN_POINT('Ctrl Pts',(31.4003537345997,23.0126067310725,42.4299987593225));
#68912=CARTESIAN_POINT('Ctrl Pts',(31.4664211256126,22.9649837593646,42.4257761055851));
#68913=CARTESIAN_POINT('Ctrl Pts',(31.5298925234446,22.9142568053185,42.4215534518476));
#68914=CARTESIAN_POINT('Ctrl Pts',(31.5938125210454,22.8631713260054,42.4173009534628));
#68915=CARTESIAN_POINT('Ctrl Pts',(31.6550993282679,22.8089381338788,42.4130484550779));
#68916=CARTESIAN_POINT('Ctrl Pts',(31.7134449099166,22.7518723671207,42.408795956693));
#68917=CARTESIAN_POINT('Ctrl Pts',(31.7717904915653,22.6948066003625,42.4045434583082));
#68918=CARTESIAN_POINT('Ctrl Pts',(31.8271945718215,22.6349086502739,42.4002909599233));
#68919=CARTESIAN_POINT('Ctrl Pts',(31.8793912100242,22.5725262890279,42.3960384615384));
#68920=CARTESIAN_POINT('Ctrl Pts',(31.9313319922345,22.510449711861,42.3918068079289));
#68921=CARTESIAN_POINT('Ctrl Pts',(31.9802910094292,22.4456808587614,42.3875751543193));
#68922=CARTESIAN_POINT('Ctrl Pts',(32.025977086745,22.3785380277614,42.3833435007097));
#68923=CARTESIAN_POINT('Ctrl Pts',(32.0715977602865,22.3114913178299,42.3791179050971));
#68924=CARTESIAN_POINT('Ctrl Pts',(32.1139545405212,22.2420777609168,42.3748923094845));
#68925=CARTESIAN_POINT('Ctrl Pts',(32.1527960597098,22.1706491256127,42.3706667138719));
#68926=CARTESIAN_POINT('Ctrl Pts',(32.1916930090643,22.0991185555445,42.3664350879734));
#68927=CARTESIAN_POINT('Ctrl Pts',(32.2270643687437,22.0255675219382,42.3622034620749));
#68928=CARTESIAN_POINT('Ctrl Pts',(32.2587009724443,21.9503789597203,42.3579718361764));
#68929=CARTESIAN_POINT('Ctrl Pts',(32.2902358106805,21.8754322565538,42.3537538221491));
#68930=CARTESIAN_POINT('Ctrl Pts',(32.3180596871435,21.7988589668682,42.3495358081218));
#68931=CARTESIAN_POINT('Ctrl Pts',(32.3420119842269,21.721061797447,42.3453177940945));
#68932=CARTESIAN_POINT('Ctrl Pts',(32.3659563997663,21.6432902273167,42.3411011680118));
#68933=CARTESIAN_POINT('Ctrl Pts',(32.3860316291797,21.5642960210873,42.3368845419292));
#68934=CARTESIAN_POINT('Ctrl Pts',(32.4021264409799,21.4844985155242,42.3326679158466));
#68935=CARTESIAN_POINT('Ctrl Pts',(32.4182208844196,21.4047028362795,42.3284513862695));
#68936=CARTESIAN_POINT('Ctrl Pts',(32.4303350005836,21.3241043501087,42.3242348566925));
#68937=CARTESIAN_POINT('Ctrl Pts',(32.4384086509051,21.2431326822768,42.3200183271154));
#68938=CARTESIAN_POINT('Ctrl Pts',(32.446532129696,21.1616612783767,42.3157757742147));
#68939=CARTESIAN_POINT('Ctrl Pts',(32.4505650354488,21.0798125425336,42.3115332213141));
#68940=CARTESIAN_POINT('Ctrl Pts',(32.450499206192,20.9980275770685,42.3072906684135));
#68941=CARTESIAN_POINT('Ctrl Pts',(32.4504336857344,20.9166262574379,42.3030680169426));
#68942=CARTESIAN_POINT('Ctrl Pts',(32.446307877626,20.8352885765009,42.2988453654717));
#68943=CARTESIAN_POINT('Ctrl Pts',(32.4381659939532,20.7544458594729,42.2946227140009));
#68944=CARTESIAN_POINT('Ctrl Pts',(32.4299665510215,20.6730316227487,42.2903702103854));
#68945=CARTESIAN_POINT('Ctrl Pts',(32.4176940990985,20.5921198486564,42.2861177067698));
#68946=CARTESIAN_POINT('Ctrl Pts',(32.4014460596138,20.5121403144701,42.2818652031543));
#68947=CARTESIAN_POINT('Ctrl Pts',(32.3851980201291,20.4321607802837,42.2776126995387));
#68948=CARTESIAN_POINT('Ctrl Pts',(32.3649745719575,20.3531139300766,42.2733601959232));
#68949=CARTESIAN_POINT('Ctrl Pts',(32.3409233958904,20.2754119069616,42.2691076923077));
#68950=CARTESIAN_POINT('Ctrl Pts',(32.3169901510793,20.1980908838092,42.2648760401919));
#68951=CARTESIAN_POINT('Ctrl Pts',(32.2891771448335,20.1218123082809,42.2606443880762));
#68952=CARTESIAN_POINT('Ctrl Pts',(32.257593604598,20.0469935118384,42.2564127359604));
#68953=CARTESIAN_POINT('Ctrl Pts',(32.226055279343,19.9722818259475,42.2521871418757));
#68954=CARTESIAN_POINT('Ctrl Pts',(32.1907573200585,19.8990261931905,42.247961547791));
#68955=CARTESIAN_POINT('Ctrl Pts',(32.1518586739458,19.8276286862242,42.2437359537063));
#68956=CARTESIAN_POINT('Ctrl Pts',(32.1129044985799,19.7561292566814,42.2395043274301));
#68957=CARTESIAN_POINT('Ctrl Pts',(32.070339503299,19.6864937049849,42.2352727011539));
#68958=CARTESIAN_POINT('Ctrl Pts',(32.0243717201438,19.6191055838038,42.2310410748776));
#68959=CARTESIAN_POINT('Ctrl Pts',(31.9785518230268,19.5519342614669,42.2268230624501));
#68960=CARTESIAN_POINT('Ctrl Pts',(31.9293512482011,19.4869963256597,42.2226050500226));
#68961=CARTESIAN_POINT('Ctrl Pts',(31.877020988831,19.4246452915334,42.2183870375951));
#68962=CARTESIAN_POINT('Ctrl Pts',(31.8247079491204,19.3623147744768,42.2141704131358));
#68963=CARTESIAN_POINT('Ctrl Pts',(31.7692675685974,19.3025698243909,42.2099537886765));
#68964=CARTESIAN_POINT('Ctrl Pts',(31.7109916179181,19.245731510454,42.2057371642172));
#68965=CARTESIAN_POINT('Ctrl Pts',(31.6527170012917,19.1888944976596,42.2015206362849));
#68966=CARTESIAN_POINT('Ctrl Pts',(31.5916072771051,19.134964312447,42.1973041083526));
#68967=CARTESIAN_POINT('Ctrl Pts',(31.5279905945585,19.0842247018659,42.1930875804203));
#68968=CARTESIAN_POINT('Ctrl Pts',(31.463981233096,19.0331718970961,42.1888450256417));
#68969=CARTESIAN_POINT('Ctrl Pts',(31.3974342205449,18.9853494990763,42.184602470863));
#68970=CARTESIAN_POINT('Ctrl Pts',(31.3287155634666,18.9410038364772,42.1803599160844));
#68971=CARTESIAN_POINT('Ctrl Pts',(31.260319316858,18.8968662324537,42.1761372662943));
#68972=CARTESIAN_POINT('Ctrl Pts',(31.1897721917849,18.8561729984999,42.1719146165042));
#68973=CARTESIAN_POINT('Ctrl Pts',(31.1174604169032,18.8191211710289,42.1676919667141));
#68974=CARTESIAN_POINT('Ctrl Pts',(31.044637340427,18.781807357754,42.1634394594412));
#68975=CARTESIAN_POINT('Ctrl Pts',(30.9700249980049,18.7481868438762,42.1591869521684));
#68976=CARTESIAN_POINT('Ctrl Pts',(30.8940372071709,18.7184111408507,42.1549344448955));
#68977=CARTESIAN_POINT('Ctrl Pts',(30.8180494163369,18.6886354378252,42.1506819376227));
#68978=CARTESIAN_POINT('Ctrl Pts',(30.7406866471373,18.6627046365206,42.1464294303498));
#68979=CARTESIAN_POINT('Ctrl Pts',(30.6623751937441,18.6407184668394,42.142176923077));
#68980=CARTESIAN_POINT('Ctrl Pts',(30.5844477702936,18.6188401146884,42.137945269588));
#68981=CARTESIAN_POINT('Ctrl Pts',(30.5052894772563,18.6007859263887,42.133713616099));
#68982=CARTESIAN_POINT('Ctrl Pts',(30.4253100886864,18.5866907412307,42.12948196261));
#68983=CARTESIAN_POINT('Ctrl Pts',(30.3454451981305,18.5726157346555,42.1252563671308));
#68984=CARTESIAN_POINT('Ctrl Pts',(30.2647620005521,18.5624885546738,42.1210307716517));
#68985=CARTESIAN_POINT('Ctrl Pts',(30.1836844484152,18.5563940020105,42.1168051761725));
#68986=CARTESIAN_POINT('Ctrl Pts',(30.1024911885124,18.5502907516614,42.1125735502422));
#68987=CARTESIAN_POINT('Ctrl Pts',(30.0209029037114,18.5482317578359,42.108341924312));
#68988=CARTESIAN_POINT('Ctrl Pts',(29.9393546409158,18.5502505453778,42.1041102983817));
#68989=CARTESIAN_POINT('Ctrl Pts',(29.8580686981897,18.5522628389925,42.0998922845183));
#68990=CARTESIAN_POINT('Ctrl Pts',(29.7768229869487,18.5583267248655,42.095674270655));
#68991=CARTESIAN_POINT('Ctrl Pts',(29.6960506526685,18.5684233418918,42.0914562567916));
#68992=CARTESIAN_POINT('Ctrl Pts',(29.6153048968771,18.5785166365822,42.0872396308841));
#68993=CARTESIAN_POINT('Ctrl Pts',(29.535032669569,18.5926399695743,42.0830230049766));
#68994=CARTESIAN_POINT('Ctrl Pts',(29.4556620061474,18.6107226200274,42.0788063790691));
#68995=CARTESIAN_POINT('Ctrl Pts',(29.3762931594821,18.6288048565774,42.0745898496781));
#68996=CARTESIAN_POINT('Ctrl Pts',(29.2978262886152,18.6508461260489,42.0703733202871));
#68997=CARTESIAN_POINT('Ctrl Pts',(29.2206778357139,18.6767248948408,42.0661567908961));
#68998=CARTESIAN_POINT('Ctrl Pts',(29.1430532357876,18.702763382957,42.0619142378086));
#68999=CARTESIAN_POINT('Ctrl Pts',(29.0667638397788,18.732686765123,42.0576716847211));
#69000=CARTESIAN_POINT('Ctrl Pts',(28.9922152177433,18.7663214012191,42.0534291316336));
#69001=CARTESIAN_POINT('Ctrl Pts',(28.918016303495,18.7997982571465,42.0492064803741));
#69002=CARTESIAN_POINT('Ctrl Pts',(28.8455422592944,18.8369513621315,42.0449838291146));
#69003=CARTESIAN_POINT('Ctrl Pts',(28.7751682390831,18.8775633325234,42.0407611778551));
#69004=CARTESIAN_POINT('Ctrl Pts',(28.7042966979216,18.9184624160579,42.0365086738536));
#69005=CARTESIAN_POINT('Ctrl Pts',(28.6355553915385,18.9628692023489,42.0322561698521));
#69006=CARTESIAN_POINT('Ctrl Pts',(28.5692962188833,19.010518424137,42.0280036658506));
#69007=CARTESIAN_POINT('Ctrl Pts',(28.5030370462281,19.058167645925,42.0237511618491));
#69008=CARTESIAN_POINT('Ctrl Pts',(28.4392603387971,19.1090589578006,42.0194986578476));
#69009=CARTESIAN_POINT('Ctrl Pts',(28.378281283189,19.162888502691,42.0152461538461));
#69010=CARTESIAN_POINT('Ctrl Pts',(28.3184922830461,19.2156675205858,42.0110766408909));
#69011=CARTESIAN_POINT('Ctrl Pts',(28.2611548731725,19.2714813445731,42.0069071279358));
#69012=CARTESIAN_POINT('Ctrl Pts',(28.2065999168397,19.3300699440634,42.0027376149806));
#69013=CARTESIAN_POINT('Ctrl Pts',(28.152135917368,19.3885608615929,41.9985750536543));
#69014=CARTESIAN_POINT('Ctrl Pts',(28.1004454793629,19.4498170163631,41.994412492328));
#69015=CARTESIAN_POINT('Ctrl Pts',(28.0518254290861,19.5135390717397,41.9902499310017));
#69016=CARTESIAN_POINT('Ctrl Pts',(28.0032509230386,19.5772014362711,41.9860912689031));
#69017=CARTESIAN_POINT('Ctrl Pts',(27.957741390077,19.6433247413285,41.9819326068045));
#69018=CARTESIAN_POINT('Ctrl Pts',(27.9155551164059,19.7115746908499,41.9777739447059));
#69019=CARTESIAN_POINT('Ctrl Pts',(27.8733945481879,19.7797830534824,41.9736178166139));
#69020=CARTESIAN_POINT('Ctrl Pts',(27.8345534731361,19.8501150825003,41.9694616885218));
#69021=CARTESIAN_POINT('Ctrl Pts',(27.7992473896177,19.9222067926103,41.9653055604298));
#69022=CARTESIAN_POINT('Ctrl Pts',(27.7639512633416,19.9942781709655,41.961150604475));
#69023=CARTESIAN_POINT('Ctrl Pts',(27.7321883591814,20.0681078141059,41.9569956485201));
#69024=CARTESIAN_POINT('Ctrl Pts',(27.7041278797455,20.1433078397475,41.9528406925653));
#69025=CARTESIAN_POINT('Ctrl Pts',(27.6760519557122,20.2185492557767,41.9486834497066));
#69026=CARTESIAN_POINT('Ctrl Pts',(27.6516826987285,20.2951621122091,41.9445262068478));
#69027=CARTESIAN_POINT('Ctrl Pts',(27.6311404814675,20.3727402201176,41.940368963989));
#69028=CARTESIAN_POINT('Ctrl Pts',(27.6105925262874,20.4503399973964,41.9362105599156));
#69029=CARTESIAN_POINT('Ctrl Pts',(27.5938738431589,20.5289050941591,41.9320521558421));
#69030=CARTESIAN_POINT('Ctrl Pts',(27.5810538343781,20.6080182429969,41.9278937517687));
#69031=CARTESIAN_POINT('Ctrl Pts',(27.5682168450155,20.6872361801638,41.9237298397333));
#69032=CARTESIAN_POINT('Ctrl Pts',(27.5592888964614,20.7670031419257,41.9195659276979));
#69033=CARTESIAN_POINT('Ctrl Pts',(27.5542875075751,20.8468965892053,41.9154020156625));
#69034=CARTESIAN_POINT('Ctrl Pts',(27.5510546653782,20.8985388256912,41.9127105091953));
#69035=CARTESIAN_POINT('Ctrl Pts',(27.5494613475282,20.9502338560456,41.9100190027281));
#69036=CARTESIAN_POINT('Ctrl Pts',(27.5495007121296,21.0018681933898,41.907327496261));
#69037=CARTESIAN_POINT('',(27.5495007304439,20.9981079363645,41.1073274961648));
#69038=CARTESIAN_POINT('Ctrl Pts',(27.5495007121303,21.0018681943271,41.9073274962121));
#69039=CARTESIAN_POINT('Ctrl Pts',(27.5495933993273,21.1234454344049,41.9009901256798));
#69040=CARTESIAN_POINT('Ctrl Pts',(27.5587352425817,21.2446839676752,41.8946527551476));
#69041=CARTESIAN_POINT('Ctrl Pts',(27.5767683012454,21.3645523064678,41.8883153846154));
#69042=CARTESIAN_POINT('Ctrl Pts',(27.5888095170788,21.4445920027784,41.8840837316375));
#69043=CARTESIAN_POINT('Ctrl Pts',(27.6048430969206,21.5241841611566,41.8798520786596));
#69044=CARTESIAN_POINT('Ctrl Pts',(27.6248237724488,21.6028997744862,41.8756204256817));
#69045=CARTESIAN_POINT('Ctrl Pts',(27.6447758437266,21.6815026988775,41.8713948307203));
#69046=CARTESIAN_POINT('Ctrl Pts',(27.668663674594,21.7592311237478,41.8671692357589));
#69047=CARTESIAN_POINT('Ctrl Pts',(27.6963905484858,21.8356636553629,41.8629436407975));
#69048=CARTESIAN_POINT('Ctrl Pts',(27.7241569963262,21.9122052774254,41.8587120147386));
#69049=CARTESIAN_POINT('Ctrl Pts',(27.7557733676511,21.9874468430298,41.8544803886797));
#69050=CARTESIAN_POINT('Ctrl Pts',(27.7910916353731,22.0609778917025,41.8502487626209));
#69051=CARTESIAN_POINT('Ctrl Pts',(27.8262962876953,22.1342723982106,41.8460307492876));
#69052=CARTESIAN_POINT('Ctrl Pts',(27.865178868721,22.205866948534,41.8418127359543));
#69053=CARTESIAN_POINT('Ctrl Pts',(27.9075443638631,22.2753743218361,41.837594722621));
#69054=CARTESIAN_POINT('Ctrl Pts',(27.9498959184177,22.3448588233739,41.833378097247));
#69055=CARTESIAN_POINT('Ctrl Pts',(27.9957278694024,22.4122571152052,41.8291614718731));
#69056=CARTESIAN_POINT('Ctrl Pts',(28.0448000117159,22.4772079257213,41.8249448464991));
#69057=CARTESIAN_POINT('Ctrl Pts',(28.0938710307598,22.5421572495025,41.8207283176444));
#69058=CARTESIAN_POINT('Ctrl Pts',(28.1461818125716,22.6046588331796,41.8165117887897));
#69059=CARTESIAN_POINT('Ctrl Pts',(28.2014505777085,22.6643828362414,41.812295259935));
#69060=CARTESIAN_POINT('Ctrl Pts',(28.257060467454,22.7244754621071,41.8080527062224));
#69061=CARTESIAN_POINT('Ctrl Pts',(28.3156646680406,22.7817557429214,41.8038101525099));
#69062=CARTESIAN_POINT('Ctrl Pts',(28.3769383496614,22.8359251425917,41.7995675987974));
#69063=CARTESIAN_POINT('Ctrl Pts',(28.4379245795284,22.8898404186558,41.7953449480753));
#69064=CARTESIAN_POINT('Ctrl Pts',(28.5015548986921,22.940673687582,41.7911222973533));
#69065=CARTESIAN_POINT('Ctrl Pts',(28.567477076571,22.9881721061946,41.7868996466313));
#69066=CARTESIAN_POINT('Ctrl Pts',(28.6338653296365,23.0360063425097,41.7826471414235));
#69067=CARTESIAN_POINT('Ctrl Pts',(28.7025775734487,23.0804581291693,41.7783946362157));
#69068=CARTESIAN_POINT('Ctrl Pts',(28.7732274609767,23.1213154851408,41.7741421310079));
#69069=CARTESIAN_POINT('Ctrl Pts',(28.8438773485047,23.1621728411124,41.7698896258001));
#69070=CARTESIAN_POINT('Ctrl Pts',(28.9164644286987,23.199435605919,41.7656371205923));
#69071=CARTESIAN_POINT('Ctrl Pts',(28.9905822376341,23.232941116783,41.7613846153845));
#69072=CARTESIAN_POINT('Ctrl Pts',(29.0643366115777,23.2662823341359,41.7571529622394));
#69073=CARTESIAN_POINT('Ctrl Pts',(29.1398825912997,23.29602780231,41.7529213090942));
#69074=CARTESIAN_POINT('Ctrl Pts',(29.2168353211374,23.3219826303791,41.7486896559491));
#69075=CARTESIAN_POINT('Ctrl Pts',(29.2936778858269,23.3479003016444,41.7444640608177));
#69076=CARTESIAN_POINT('Ctrl Pts',(29.3719227641181,23.3700379633509,41.7402384656863));
#69077=CARTESIAN_POINT('Ctrl Pts',(29.4511635628977,23.3882480640228,41.7360128705549));
#69078=CARTESIAN_POINT('Ctrl Pts',(29.5305174563198,23.4064841546501,41.7317812445382));
#69079=CARTESIAN_POINT('Ctrl Pts',(29.6108696808612,23.4207812870483,41.7275496185215));
#69080=CARTESIAN_POINT('Ctrl Pts',(29.6917951688212,23.4310409359034,41.7233179925048));
#69081=CARTESIAN_POINT('Ctrl Pts',(29.7724603315873,23.4412675810023,41.7190999789962));
#69082=CARTESIAN_POINT('Ctrl Pts',(29.853694614712,23.4474826035878,41.7148819654876));
#69083=CARTESIAN_POINT('Ctrl Pts',(29.9350669576142,23.4496395551196,41.7106639519791));
#69084=CARTESIAN_POINT('Ctrl Pts',(30.0164125245543,23.4517957968961,41.7064473264282));
#69085=CARTESIAN_POINT('Ctrl Pts',(30.097895596774,23.4498966071184,41.7022307008773));
#69086=CARTESIAN_POINT('Ctrl Pts',(30.1790823719664,23.4439475759621,41.6980140753264));
#69087=CARTESIAN_POINT('Ctrl Pts',(30.2602672888064,23.4379986809782,41.6937975462935));
#69088=CARTESIAN_POINT('Ctrl Pts',(30.3411554586236,23.4280001640218,41.6895810172605));
#69089=CARTESIAN_POINT('Ctrl Pts',(30.4213169042637,23.4140095932249,41.6853644882275));
#69090=CARTESIAN_POINT('Ctrl Pts',(30.5019731074102,23.3999326724393,41.6811219347214));
#69091=CARTESIAN_POINT('Ctrl Pts',(30.5818931135361,23.3818143172013,41.6768793812152));
#69092=CARTESIAN_POINT('Ctrl Pts',(30.6606498630408,23.3597652443546,41.6726368277091));
#69093=CARTESIAN_POINT('Ctrl Pts',(30.7390371500469,23.3378196077925,41.6684141768072));
#69094=CARTESIAN_POINT('Ctrl Pts',(30.8162716434374,23.3119802524962,41.6641915259054));
#69095=CARTESIAN_POINT('Ctrl Pts',(30.8919497805055,23.2824057130704,41.6599688750035));
#69096=CARTESIAN_POINT('Ctrl Pts',(30.9681629577825,23.2526220833,41.6557163701952));
#69097=CARTESIAN_POINT('Ctrl Pts',(31.0427972497349,23.2190504444013,41.651463865387));
#69098=CARTESIAN_POINT('Ctrl Pts',(31.1154648880174,23.1819001658189,41.6472113605787));
#69099=CARTESIAN_POINT('Ctrl Pts',(31.1881325262999,23.1447498872364,41.6429588557704));
#69100=CARTESIAN_POINT('Ctrl Pts',(31.2588331312703,23.1040212606382,41.6387063509621));
#69101=CARTESIAN_POINT('Ctrl Pts',(31.3272094305348,23.0599673243767,41.6344538461539));
#69102=CARTESIAN_POINT('Ctrl Pts',(31.3952504536625,23.0161294020515,41.6302221930647));
#69103=CARTESIAN_POINT('Ctrl Pts',(31.4612444318076,22.9688347660637,41.6259905399755));
#69104=CARTESIAN_POINT('Ctrl Pts',(31.5248187584053,22.91830081166,41.6217588868863));
#69105=CARTESIAN_POINT('Ctrl Pts',(31.5883020723011,22.8678392014237,41.6175332918114));
#69106=CARTESIAN_POINT('Ctrl Pts',(31.6493722535907,22.8141477698547,41.6133076967365));
#69107=CARTESIAN_POINT('Ctrl Pts',(31.707684758663,22.7574876998233,41.6090821016616));
#69108=CARTESIAN_POINT('Ctrl Pts',(31.7660804899176,22.7007467620378,41.6048504756308));
#69109=CARTESIAN_POINT('Ctrl Pts',(31.8217102822432,22.6410289737294,41.6006188496001));
#69110=CARTESIAN_POINT('Ctrl Pts',(31.8742606257078,22.5786378168919,41.5963872235693));
#69111=CARTESIAN_POINT('Ctrl Pts',(31.9266419216878,22.5164473641305,41.5921692101182));
#69112=CARTESIAN_POINT('Ctrl Pts',(31.9759632377043,22.4516010621735,41.5879511966671));
#69113=CARTESIAN_POINT('Ctrl Pts',(32.0219515443117,22.3844356982017,41.583733183216));
#69114=CARTESIAN_POINT('Ctrl Pts',(32.0679247182423,22.317292435321,41.5795165577228));
#69115=CARTESIAN_POINT('Ctrl Pts',(32.1105667983761,22.2478320090719,41.5752999322296));
#69116=CARTESIAN_POINT('Ctrl Pts',(32.1496469688242,22.1764217608601,41.5710833067364));
#69117=CARTESIAN_POINT('Ctrl Pts',(32.1887262447319,22.10501314722,41.5668667777612));
#69118=CARTESIAN_POINT('Ctrl Pts',(32.2242435509093,22.0316552086384,41.5626502487861));
#69119=CARTESIAN_POINT('Ctrl Pts',(32.2560137991448,21.9567402929051,41.5584337198109));
#69120=CARTESIAN_POINT('Ctrl Pts',(32.2879801347238,21.8813629990782,41.5541911662369));
#69121=CARTESIAN_POINT('Ctrl Pts',(32.3161527995833,21.8044098746383,41.5499486126629));
#69122=CARTESIAN_POINT('Ctrl Pts',(32.3403929236425,21.7262996715986,41.5457060590889));
#69123=CARTESIAN_POINT('Ctrl Pts',(32.3645193320751,21.6485559002924,41.5414834082447));
#69124=CARTESIAN_POINT('Ctrl Pts',(32.3847499518859,21.5696663502626,41.5372607574004));
#69125=CARTESIAN_POINT('Ctrl Pts',(32.4009988267127,21.4900560010084,41.5330381065562));
#69126=CARTESIAN_POINT('Ctrl Pts',(32.4173625809041,21.4098828074685,41.5287856016173));
#69127=CARTESIAN_POINT('Ctrl Pts',(32.4296879964447,21.328979055862,41.5245330966785));
#69128=CARTESIAN_POINT('Ctrl Pts',(32.4379403827214,21.2477840598103,41.5202805917396));
#69129=CARTESIAN_POINT('Ctrl Pts',(32.4461927689982,21.1665890637587,41.5160280868008));
#69130=CARTESIAN_POINT('Ctrl Pts',(32.4503721648465,21.0851033004309,41.5117755818619));
#69131=CARTESIAN_POINT('Ctrl Pts',(32.450497108944,21.003764180767,41.507523076923));
#69132=CARTESIAN_POINT('Ctrl Pts',(32.450621440387,20.9228239017932,41.503291423845));
#69133=CARTESIAN_POINT('Ctrl Pts',(32.446731491831,20.8417260842945,41.499059770767));
#69134=CARTESIAN_POINT('Ctrl Pts',(32.4388075440206,20.7609016661948,41.494828117689));
#69135=CARTESIAN_POINT('Ctrl Pts',(32.4308949400967,20.6801929559527,41.4906025226257));
#69136=CARTESIAN_POINT('Ctrl Pts',(32.418959851677,20.5997573264625,41.4863769275624));
#69137=CARTESIAN_POINT('Ctrl Pts',(32.4030345676143,20.5200259206469,41.482151332499));
#69138=CARTESIAN_POINT('Ctrl Pts',(32.3870865542285,20.440180718376,41.4779197064654));
#69139=CARTESIAN_POINT('Ctrl Pts',(32.3671369628849,20.361042220484,41.4736880804318));
#69140=CARTESIAN_POINT('Ctrl Pts',(32.343270453307,20.2830384719816,41.4694564543982));
#69141=CARTESIAN_POINT('Ctrl Pts',(32.3194807192105,20.2052856514719,41.4652384409594));
#69142=CARTESIAN_POINT('Ctrl Pts',(32.2917993492479,20.1286607416087,41.4610204275207));
#69143=CARTESIAN_POINT('Ctrl Pts',(32.2603609495727,20.0535758732752,41.4568024140819));
#69144=CARTESIAN_POINT('Ctrl Pts',(32.2289328948586,19.9785157119892,41.4525857886014));
#69145=CARTESIAN_POINT('Ctrl Pts',(32.1937504448952,19.9049950142763,41.4483691631209));
#69146=CARTESIAN_POINT('Ctrl Pts',(32.154996782894,19.8334070479742,41.4441525376403));
#69147=CARTESIAN_POINT('Ctrl Pts',(32.1162440079618,19.7618207203161,41.4399360086781));
#69148=CARTESIAN_POINT('Ctrl Pts',(32.0739204057914,19.692167444326,41.4357194797158));
#69149=CARTESIAN_POINT('Ctrl Pts',(32.0282549853941,19.6248156617297,41.4315029507536));
#69150=CARTESIAN_POINT('Ctrl Pts',(31.9823077157539,19.5570481805859,41.4272603971651));
#69151=CARTESIAN_POINT('Ctrl Pts',(31.9329774887394,19.4916111026947,41.4230178435767));
#69152=CARTESIAN_POINT('Ctrl Pts',(31.8805405793361,19.4288483906795,41.4187752899883));
#69153=CARTESIAN_POINT('Ctrl Pts',(31.8283496630769,19.3663801124333,41.4145526391574));
#69154=CARTESIAN_POINT('Ctrl Pts',(31.7730815067821,19.3065614702871,41.4103299883266));
#69155=CARTESIAN_POINT('Ctrl Pts',(31.7150463420298,19.2496953708882,41.4061073374958));
#69156=CARTESIAN_POINT('Ctrl Pts',(31.6566008687312,19.1924272282336,41.4018548325285));
#69157=CARTESIAN_POINT('Ctrl Pts',(31.5953494668567,19.1381538576023,41.3976023275613));
#69158=CARTESIAN_POINT('Ctrl Pts',(31.5316422378551,19.0871428947205,41.3933498225941));
#69159=CARTESIAN_POINT('Ctrl Pts',(31.4679350088536,19.0361319318388,41.3890973176268));
#69160=CARTESIAN_POINT('Ctrl Pts',(31.4017723745344,18.988383603147,41.3848448126596));
#69161=CARTESIAN_POINT('Ctrl Pts',(31.3335317365672,18.9441198095297,41.3805923076924));
#69162=CARTESIAN_POINT('Ctrl Pts',(31.265625711934,18.9000730604185,41.3763606545944));
#69163=CARTESIAN_POINT('Ctrl Pts',(31.195408041103,18.8593119702202,41.3721290014965));
#69164=CARTESIAN_POINT('Ctrl Pts',(31.1232299195457,18.8220870545779,41.3678973483986));
#69165=CARTESIAN_POINT('Ctrl Pts',(31.0511551278423,18.7849154299468,41.3636717533151));
#69166=CARTESIAN_POINT('Ctrl Pts',(30.9771258691552,18.7512701368023,41.3594461582315));
#69167=CARTESIAN_POINT('Ctrl Pts',(30.901521746224,18.7213581257501,41.3552205631479));
#69168=CARTESIAN_POINT('Ctrl Pts',(30.8258097179442,18.6914034230316,41.3509889371193));
#69169=CARTESIAN_POINT('Ctrl Pts',(30.7485187292922,18.6651929079815,41.3467573110907));
#69170=CARTESIAN_POINT('Ctrl Pts',(30.6700542134318,18.6428878683732,41.3425256850621));
#69171=CARTESIAN_POINT('Ctrl Pts',(30.5918421073127,18.6206545810623,41.3383076716025));
#69172=CARTESIAN_POINT('Ctrl Pts',(30.5124644565581,18.6023018244049,41.3340896581428));
#69173=CARTESIAN_POINT('Ctrl Pts',(30.4323404455075,18.5879403014895,41.3298716446831));
#69174=CARTESIAN_POINT('Ctrl Pts',(30.3522427996554,18.5735835043036,41.3256550191815));
#69175=CARTESIAN_POINT('Ctrl Pts',(30.2713997383858,18.5632154146701,41.3214383936798));
#69176=CARTESIAN_POINT('Ctrl Pts',(30.1902409772808,18.5568957000236,41.3172217681781));
#69177=CARTESIAN_POINT('Ctrl Pts',(30.1090840738914,18.5505761300347,41.3130052391946));
#69178=CARTESIAN_POINT('Ctrl Pts',(30.0276119485251,18.5483047857458,41.3087887102111));
#69179=CARTESIAN_POINT('Ctrl Pts',(29.9462583465789,18.550089372102,41.3045721812275));
#69180=CARTESIAN_POINT('Ctrl Pts',(29.8644026270489,18.5518849729943,41.3003296276637));
#69181=CARTESIAN_POINT('Ctrl Pts',(29.7826673750212,18.557786748148,41.2960870740998));
#69182=CARTESIAN_POINT('Ctrl Pts',(29.7014914389796,18.5677494189542,41.291844520536));
#69183=CARTESIAN_POINT('Ctrl Pts',(29.6206963163348,18.5776653527754,41.2876218696837));
#69184=CARTESIAN_POINT('Ctrl Pts',(29.5404557258618,18.5916040309419,41.2833992188313));
#69185=CARTESIAN_POINT('Ctrl Pts',(29.461192472287,18.6094693689309,41.2791765679789));
#69186=CARTESIAN_POINT('Ctrl Pts',(29.3813688289045,18.627461014545,41.2749240630594));
#69187=CARTESIAN_POINT('Ctrl Pts',(29.3025368568059,18.6494349311086,41.2706715581398));
#69188=CARTESIAN_POINT('Ctrl Pts',(29.2251113855144,18.6752424029287,41.2664190532202));
#69189=CARTESIAN_POINT('Ctrl Pts',(29.147685914223,18.7010498747488,41.2621665483007));
#69190=CARTESIAN_POINT('Ctrl Pts',(29.0716673629024,18.7306906705246,41.2579140433811));
#69191=CARTESIAN_POINT('Ctrl Pts',(28.9974469742688,18.7639683185167,41.2536615384615));
#69192=CARTESIAN_POINT('Ctrl Pts',(28.9235905195819,18.7970827921305,41.2494298853716));
#69193=CARTESIAN_POINT('Ctrl Pts',(28.8512383675905,18.8339223611666,41.2451982322817));
#69194=CARTESIAN_POINT('Ctrl Pts',(28.7807915643565,18.8743280967055,41.2409665791917));
#69195=CARTESIAN_POINT('Ctrl Pts',(28.7104456124311,18.9146759875855,41.2367409841162));
#69196=CARTESIAN_POINT('Ctrl Pts',(28.6419999916318,18.958579676045,41.2325153890407));
#69197=CARTESIAN_POINT('Ctrl Pts',(28.5758345844244,19.0058327254018,41.2282897939653));
#69198=CARTESIAN_POINT('Ctrl Pts',(28.5095747430381,19.0531532163886,41.2240581679347));
#69199=CARTESIAN_POINT('Ctrl Pts',(28.4456020499601,19.103832428829,41.219826541904));
#69200=CARTESIAN_POINT('Ctrl Pts',(28.3842720633739,19.1576174434157,41.2155949158734));
#69201=CARTESIAN_POINT('Ctrl Pts',(28.3231393672129,19.2112294387506,41.211376902422));
#69202=CARTESIAN_POINT('Ctrl Pts',(28.2646327626603,19.2679269899824,41.2071588889706));
#69203=CARTESIAN_POINT('Ctrl Pts',(28.2090727924445,19.3274181672523,41.2029408755192));
#69204=CARTESIAN_POINT('Ctrl Pts',(28.1535311045098,19.3868897686582,41.1987242500258));
#69205=CARTESIAN_POINT('Ctrl Pts',(28.1009344423944,19.4491528311307,41.1945076245324));
#69206=CARTESIAN_POINT('Ctrl Pts',(28.0515662065552,19.5138788735226,41.190290999039));
#69207=CARTESIAN_POINT('Ctrl Pts',(28.0021991007501,19.5786034343417,41.1860744700638));
#69208=CARTESIAN_POINT('Ctrl Pts',(27.9560605552787,19.6457904927276,41.1818579410886));
#69209=CARTESIAN_POINT('Ctrl Pts',(27.9133925203572,19.715079972956,41.1776414121133));
#69210=CARTESIAN_POINT('Ctrl Pts',(27.8704611364877,19.7847971108387,41.1733988585398));
#69211=CARTESIAN_POINT('Ctrl Pts',(27.8310435131495,19.8566423151158,41.1691563049662));
#69212=CARTESIAN_POINT('Ctrl Pts',(27.7953398755101,19.930222459815,41.1649137513927));
#69213=CARTESIAN_POINT('Ctrl Pts',(27.7598037312989,20.0034574242611,41.1606911005486));
#69214=CARTESIAN_POINT('Ctrl Pts',(27.7279469362205,20.0784106342766,41.1564684497046));
#69215=CARTESIAN_POINT('Ctrl Pts',(27.6999183385823,20.1546748549758,41.1522457988605));
#69216=CARTESIAN_POINT('Ctrl Pts',(27.6716915790724,20.2314782628624,41.1479932939223));
#69217=CARTESIAN_POINT('Ctrl Pts',(27.647347501305,20.3096108346374,41.143740788984));
#69218=CARTESIAN_POINT('Ctrl Pts',(27.6269864242887,20.3886434596001,41.1394882840457));
#69219=CARTESIAN_POINT('Ctrl Pts',(27.6066253472723,20.4676760845629,41.1352357791074));
#69220=CARTESIAN_POINT('Ctrl Pts',(27.5902473043242,20.5476082851275,41.1309832741691));
#69221=CARTESIAN_POINT('Ctrl Pts',(27.5778997037597,20.6280048320844,41.1267307692308));
#69222=CARTESIAN_POINT('Ctrl Pts',(27.5591198811724,20.7502822640921,41.1202630115579));
#69223=CARTESIAN_POINT('Ctrl Pts',(27.5495965430392,20.8740166648451,41.113795253885));
#69224=CARTESIAN_POINT('Ctrl Pts',(27.5495007304446,20.9981079354573,41.1073274962121));
#69225=CARTESIAN_POINT('',(27.5495000708749,20.9994106292385,40.3073274962403));
#69226=CARTESIAN_POINT('Ctrl Pts',(27.5495007304439,20.9981079363645,41.1073274961648));
#69227=CARTESIAN_POINT('Ctrl Pts',(27.549439041719,21.0780038617879,41.1031632428524));
#69228=CARTESIAN_POINT('Ctrl Pts',(27.5532889456246,21.1580443678395,41.0989989895401));
#69229=CARTESIAN_POINT('Ctrl Pts',(27.5610663166378,21.237808196161,41.0948347362277));
#69230=CARTESIAN_POINT('Ctrl Pts',(27.5688342345066,21.317475074114,41.0906755444313));
#69231=CARTESIAN_POINT('Ctrl Pts',(27.5805200929035,21.3968654676096,41.0865163526349));
#69232=CARTESIAN_POINT('Ctrl Pts',(27.596087728639,21.4755586626274,41.0823571608385));
#69233=CARTESIAN_POINT('Ctrl Pts',(27.6116451315382,21.5542001314491,41.0782007029402));
#69234=CARTESIAN_POINT('Ctrl Pts',(27.6310791585009,21.6321448414503,41.0740442450419));
#69235=CARTESIAN_POINT('Ctrl Pts',(27.6543020436233,21.7089790881615,41.0698877871435));
#69236=CARTESIAN_POINT('Ctrl Pts',(27.6775172663571,21.7857879834207,41.065732700668));
#69237=CARTESIAN_POINT('Ctrl Pts',(27.7045187276538,21.8614866835657,41.0615776141926));
#69238=CARTESIAN_POINT('Ctrl Pts',(27.7351683756534,21.9356751377266,41.0574225277171));
#69239=CARTESIAN_POINT('Ctrl Pts',(27.7658179436624,22.0098633982674,41.0532674520857));
#69240=CARTESIAN_POINT('Ctrl Pts',(27.8001154941532,22.0825409780566,41.0491123764544));
#69241=CARTESIAN_POINT('Ctrl Pts',(27.8378748814851,22.1533278900151,41.044957300823));
#69242=CARTESIAN_POINT('Ctrl Pts',(27.8756707991451,22.2241832847885,41.0407982053628));
#69243=CARTESIAN_POINT('Ctrl Pts',(27.9169350126861,22.2931439364258,41.0366391099025));
#69244=CARTESIAN_POINT('Ctrl Pts',(27.9614358506387,22.3598553080893,41.0324800144422));
#69245=CARTESIAN_POINT('Ctrl Pts',(28.0059598064528,22.4266013358252,41.0283187583621));
#69246=CARTESIAN_POINT('Ctrl Pts',(28.0537234454411,22.4910953739531,41.024157502282));
#69247=CARTESIAN_POINT('Ctrl Pts',(28.1044538453399,22.5530148182015,41.0199962462019));
#69248=CARTESIAN_POINT('Ctrl Pts',(28.1552691739708,22.615037922975,41.0158280236835));
#69249=CARTESIAN_POINT('Ctrl Pts',(28.20906085445,22.6744774761023,41.011659801165));
#69250=CARTESIAN_POINT('Ctrl Pts',(28.2655184966037,22.7310471294497,41.0074915786466));
#69251=CARTESIAN_POINT('Ctrl Pts',(28.3002454010097,22.7658429315615,41.0049277190978));
#69252=CARTESIAN_POINT('Ctrl Pts',(28.3359802668707,22.7995536911752,41.0023638595489));
#69253=CARTESIAN_POINT('Ctrl Pts',(28.372645018108,22.8321206327399,40.9998000000001));
#69254=CARTESIAN_POINT('Ctrl Pts',(28.4331602315863,22.8858724067085,40.9955683469084));
#69255=CARTESIAN_POINT('Ctrl Pts',(28.4964546234175,22.9367232445843,40.9913366938168));
#69256=CARTESIAN_POINT('Ctrl Pts',(28.5622186355986,22.9843726963905,40.9871050407252));
#69257=CARTESIAN_POINT('Ctrl Pts',(28.6278885003328,23.0319539334683,40.982879445648));
#69258=CARTESIAN_POINT('Ctrl Pts',(28.6960205903648,23.0763426164863,40.9786538505708));
#69259=CARTESIAN_POINT('Ctrl Pts',(28.7662707158692,23.1172770965271,40.9744282554936));
#69260=CARTESIAN_POINT('Ctrl Pts',(28.8366211054066,23.1582700000373,40.9701966294634));
#69261=CARTESIAN_POINT('Ctrl Pts',(28.9090952189794,23.1957985344274,40.9659650034332));
#69262=CARTESIAN_POINT('Ctrl Pts',(28.9833164672467,23.2296423130691,40.9617333774031));
#69263=CARTESIAN_POINT('Ctrl Pts',(29.0572989556487,23.2633772207848,40.9575153639499));
#69264=CARTESIAN_POINT('Ctrl Pts',(29.1330169379909,23.2934508345848,40.9532973504968));
#69265=CARTESIAN_POINT('Ctrl Pts',(29.2100726278002,23.3196907114203,40.9490793370437));
#69266=CARTESIAN_POINT('Ctrl Pts',(29.2871029620564,23.3459219538955,40.9448627115486));
#69267=CARTESIAN_POINT('Ctrl Pts',(29.3654696899833,23.3683218149037,40.9406460860535));
#69268=CARTESIAN_POINT('Ctrl Pts',(29.4447569435623,23.3867667247299,40.9364294605584));
#69269=CARTESIAN_POINT('Ctrl Pts',(29.5240423822635,23.4052112123538,40.9322129315815));
#69270=CARTESIAN_POINT('Ctrl Pts',(29.6042478517499,23.4197008245721,40.9279964026045));
#69271=CARTESIAN_POINT('Ctrl Pts',(29.6849456907566,23.4301627583821,40.9237798736276));
#69272=CARTESIAN_POINT('Ctrl Pts',(29.7661416002276,23.4406892636886,40.9195373200561));
#69273=CARTESIAN_POINT('Ctrl Pts',(29.8478355080976,23.4471381254094,40.9152947664845));
#69274=CARTESIAN_POINT('Ctrl Pts',(29.9295867453177,23.4494881554245,40.911052212913));
#69275=CARTESIAN_POINT('Ctrl Pts',(30.0109544700066,23.4518271609465,40.9068295620673));
#69276=CARTESIAN_POINT('Ctrl Pts',(30.0923785199467,23.4501057717376,40.9026069112215));
#69277=CARTESIAN_POINT('Ctrl Pts',(30.1734264522537,23.4443554397139,40.8983842603758));
#69278=CARTESIAN_POINT('Ctrl Pts',(30.2550473924294,23.4385644529145,40.8941317554414));
#69279=CARTESIAN_POINT('Ctrl Pts',(30.3362864009185,23.4286873894784,40.889879250507));
#69280=CARTESIAN_POINT('Ctrl Pts',(30.4167110097646,23.4148089332991,40.8856267455725));
#69281=CARTESIAN_POINT('Ctrl Pts',(30.4971356186106,23.4009304771198,40.8813742406381));
#69282=CARTESIAN_POINT('Ctrl Pts',(30.5767453786491,23.383050793877,40.8771217357037));
#69283=CARTESIAN_POINT('Ctrl Pts',(30.6551239638149,23.3613053258813,40.8728692307692));
#69284=CARTESIAN_POINT('Ctrl Pts',(30.7331182253765,23.3396664851821,40.8686375776787));
#69285=CARTESIAN_POINT('Ctrl Pts',(30.8101850962609,23.3141187815989,40.8644059245882));
#69286=CARTESIAN_POINT('Ctrl Pts',(30.8859042005362,23.2847590677076,40.8601742714976));
#69287=CARTESIAN_POINT('Ctrl Pts',(30.961514905702,23.2554413850431,40.8559486764215));
#69288=CARTESIAN_POINT('Ctrl Pts',(31.0357812466064,23.2223226973068,40.8517230813454));
#69289=CARTESIAN_POINT('Ctrl Pts',(31.1082966308324,23.1855500058533,40.8474974862693));
#69290=CARTESIAN_POINT('Ctrl Pts',(31.1809155121908,23.1487248308041,40.8432658602389));
#69291=CARTESIAN_POINT('Ctrl Pts',(31.2517779876693,23.1082353556078,40.8390342342084));
#69292=CARTESIAN_POINT('Ctrl Pts',(31.3204945272184,23.0642781919079,40.834802608178));
#69293=CARTESIAN_POINT('Ctrl Pts',(31.3889900147937,23.0204624325606,40.830584594726));
#69294=CARTESIAN_POINT('Ctrl Pts',(31.4553529499075,22.9732014979876,40.826366581274));
#69295=CARTESIAN_POINT('Ctrl Pts',(31.5192225575701,22.9227358296371,40.822148567822));
#69296=CARTESIAN_POINT('Ctrl Pts',(31.5830711486246,22.8722867672626,40.817931942328));
#69297=CARTESIAN_POINT('Ctrl Pts',(31.6444276771133,22.8186353532303,40.8137153168341));
#69298=CARTESIAN_POINT('Ctrl Pts',(31.702962595359,22.7620637470898,40.8094986913401));
#69299=CARTESIAN_POINT('Ctrl Pts',(31.7614961737458,22.7054934358682,40.8052821623644));
#69300=CARTESIAN_POINT('Ctrl Pts',(31.817207936864,22.6460033892658,40.8010656333886));
#69301=CARTESIAN_POINT('Ctrl Pts',(31.8698045683117,22.5839132319419,40.7968491044128));
#69302=CARTESIAN_POINT('Ctrl Pts',(31.922725828417,22.5214398515128,40.7926065508399));
#69303=CARTESIAN_POINT('Ctrl Pts',(31.9724930520762,22.4563345072282,40.7883639972671));
#69304=CARTESIAN_POINT('Ctrl Pts',(32.0188492070839,22.3889557692946,40.7841214436942));
#69305=CARTESIAN_POINT('Ctrl Pts',(32.064987895431,22.3218931194647,40.7798987928496));
#69306=CARTESIAN_POINT('Ctrl Pts',(32.1077472493203,22.2525787865955,40.7756761420051));
#69307=CARTESIAN_POINT('Ctrl Pts',(32.1469189095396,22.1813930107553,40.7714534911605));
#69308=CARTESIAN_POINT('Ctrl Pts',(32.1863675129417,22.1097039523066,40.7672009862235));
#69309=CARTESIAN_POINT('Ctrl Pts',(32.222177285331,22.0361173156651,40.7629484812865));
#69310=CARTESIAN_POINT('Ctrl Pts',(32.2541845580174,21.9610422615037,40.7586959763495));
#69311=CARTESIAN_POINT('Ctrl Pts',(32.2861918307037,21.8859672073422,40.7544434714125));
#69312=CARTESIAN_POINT('Ctrl Pts',(32.314396498974,21.8094042028156,40.7501909664754));
#69313=CARTESIAN_POINT('Ctrl Pts',(32.3386862843846,21.731776409316,40.7459384615384));
#69314=CARTESIAN_POINT('Ctrl Pts',(32.3628569666116,21.6545292580156,40.7417068084479));
#69315=CARTESIAN_POINT('Ctrl Pts',(32.3832415129416,21.5759388131944,40.7374751553573));
#69316=CARTESIAN_POINT('Ctrl Pts',(32.3996930386648,21.496410687016,40.7332435022668));
#69317=CARTESIAN_POINT('Ctrl Pts',(32.4161210124619,21.4169964129252,40.7290179071907));
#69318=CARTESIAN_POINT('Ctrl Pts',(32.4286270549614,21.3366475749145,40.7247923121146));
#69319=CARTESIAN_POINT('Ctrl Pts',(32.437113879368,21.255785435457,40.7205667170385));
#69320=CARTESIAN_POINT('Ctrl Pts',(32.4456128165421,21.1748078860125,40.716335091008));
#69321=CARTESIAN_POINT('Ctrl Pts',(32.4500809303349,21.0933160214387,40.7121034649776));
#69322=CARTESIAN_POINT('Ctrl Pts',(32.4504718597259,21.0117437085971,40.7078718389471));
#69323=CARTESIAN_POINT('Ctrl Pts',(32.4508615315489,20.9304338030427,40.7036538254951));
#69324=CARTESIAN_POINT('Ctrl Pts',(32.4472001914478,20.8490444322236,40.6994358120431));
#69325=CARTESIAN_POINT('Ctrl Pts',(32.4394938976771,20.7680091096698,40.6952177985911));
#69326=CARTESIAN_POINT('Ctrl Pts',(32.4317901397002,20.6870004521871,40.6910011730972));
#69327=CARTESIAN_POINT('Ctrl Pts',(32.4200441152582,20.6063460739694,40.6867845476032));
#69328=CARTESIAN_POINT('Ctrl Pts',(32.4043138706571,20.5264759125814,40.6825679221093));
#69329=CARTESIAN_POINT('Ctrl Pts',(32.3885839861198,20.4466075794137,40.6783513931335));
#69330=CARTESIAN_POINT('Ctrl Pts',(32.3688701536744,20.3675238832121,40.6741348641577));
#69331=CARTESIAN_POINT('Ctrl Pts',(32.3452815526646,20.2896446743137,40.6699183351819));
#69332=CARTESIAN_POINT('Ctrl Pts',(32.3215473618013,20.2112847916094,40.665675781609));
#69333=CARTESIAN_POINT('Ctrl Pts',(32.2938905308257,20.134144775369,40.6614332280362));
#69334=CARTESIAN_POINT('Ctrl Pts',(32.2624726441201,20.0586351479855,40.6571906744633));
#69335=CARTESIAN_POINT('Ctrl Pts',(32.231202145456,19.9834797524509,40.6529680236187));
#69336=CARTESIAN_POINT('Ctrl Pts',(32.1962060520371,19.9099398820973,40.6487453727742));
#69337=CARTESIAN_POINT('Ctrl Pts',(32.1576905710454,19.8383969483417,40.6445227219296));
#69338=CARTESIAN_POINT('Ctrl Pts',(32.1189027860505,19.7663482068755,40.6402702169926));
#69339=CARTESIAN_POINT('Ctrl Pts',(32.0765459027894,19.6963251583042,40.6360177120556));
#69340=CARTESIAN_POINT('Ctrl Pts',(32.0308746783301,19.6286873839574,40.6317652071186));
#69341=CARTESIAN_POINT('Ctrl Pts',(31.9852034538708,19.5610496096106,40.6275127021816));
#69342=CARTESIAN_POINT('Ctrl Pts',(31.9362182236805,19.4957974510437,40.6232601972446));
#69343=CARTESIAN_POINT('Ctrl Pts',(31.8842134022846,19.4332549331015,40.6190076923077));
#69344=CARTESIAN_POINT('Ctrl Pts',(31.8324635827178,19.3710190878106,40.6147760392168));
#69345=CARTESIAN_POINT('Ctrl Pts',(31.7775301807484,19.3112335620099,40.610544386126));
#69346=CARTESIAN_POINT('Ctrl Pts',(31.7196740854053,19.2542419153888,40.6063127330352));
#69347=CARTESIAN_POINT('Ctrl Pts',(31.6619008165734,19.1973318577381,40.6020871379589));
#69348=CARTESIAN_POINT('Ctrl Pts',(31.6012134927534,19.143208058933,40.5978615428825));
#69349=CARTESIAN_POINT('Ctrl Pts',(31.5379130727012,19.0921809229346,40.5936359478062));
#69350=CARTESIAN_POINT('Ctrl Pts',(31.4745223075221,19.0410809587768,40.5894043217758));
#69351=CARTESIAN_POINT('Ctrl Pts',(31.4085112943313,18.9930868532024,40.5851726957454));
#69352=CARTESIAN_POINT('Ctrl Pts',(31.3402192245448,18.9484730856846,40.580941069715));
#69353=CARTESIAN_POINT('Ctrl Pts',(31.2721468412633,18.9040028347228,40.5767230562627));
#69354=CARTESIAN_POINT('Ctrl Pts',(31.2018084359025,18.8628914758816,40.5725050428105));
#69355=CARTESIAN_POINT('Ctrl Pts',(31.1295713614834,18.8253692751834,40.5682870293582));
#69356=CARTESIAN_POINT('Ctrl Pts',(31.0573580570284,18.7878594213495,40.5640704038639));
#69357=CARTESIAN_POINT('Ctrl Pts',(30.983247736387,18.7539365943576,40.5598537783697));
#69358=CARTESIAN_POINT('Ctrl Pts',(30.9076329737119,18.7237854593578,40.5556371528755));
#69359=CARTESIAN_POINT('Ctrl Pts',(30.8320199418518,18.6936350145148,40.5514206238994));
#69360=CARTESIAN_POINT('Ctrl Pts',(30.7549029685927,18.6672562611193,40.5472040949233));
#69361=CARTESIAN_POINT('Ctrl Pts',(30.6766939168855,18.6447854465357,40.5429875659473));
#69362=CARTESIAN_POINT('Ctrl Pts',(30.5980021555796,18.6221759411272,40.5387450123747));
#69363=CARTESIAN_POINT('Ctrl Pts',(30.5182052418425,18.6035229263023,40.5345024588022));
#69364=CARTESIAN_POINT('Ctrl Pts',(30.4377356556349,18.5889135756291,40.5302599052297));
#69365=CARTESIAN_POINT('Ctrl Pts',(30.3576435694949,18.5743727605495,40.5260372543848));
#69366=CARTESIAN_POINT('Ctrl Pts',(30.2768855800931,18.5638377600858,40.52181460354));
#69367=CARTESIAN_POINT('Ctrl Pts',(30.195893945677,18.5573424693488,40.5175919526951));
#69368=CARTESIAN_POINT('Ctrl Pts',(30.1143297013638,18.5508012569831,40.5133394477588));
#69369=CARTESIAN_POINT('Ctrl Pts',(30.0325289736827,18.5483571130502,40.5090869428224));
#69370=CARTESIAN_POINT('Ctrl Pts',(29.9509320456543,18.5499913090243,40.504834437886));
#69371=CARTESIAN_POINT('Ctrl Pts',(29.8693351176258,18.5516255049984,40.5005819329497));
#69372=CARTESIAN_POINT('Ctrl Pts',(29.7879424582125,18.5573379445842,40.4963294280133));
#69373=CARTESIAN_POINT('Ctrl Pts',(29.7071860201171,18.5670572914298,40.4920769230769));
#69374=CARTESIAN_POINT('Ctrl Pts',(29.6268255652861,18.5767289801717,40.4878452699863));
#69375=CARTESIAN_POINT('Ctrl Pts',(29.5467945237444,18.5904045107437,40.4836136168956));
#69376=CARTESIAN_POINT('Ctrl Pts',(29.4675230525945,18.6080513068877,40.479381963805));
#69377=CARTESIAN_POINT('Ctrl Pts',(29.3883650661059,18.6256728399622,40.4751563687288));
#69378=CARTESIAN_POINT('Ctrl Pts',(29.3099649402285,18.6472542470397,40.4709307736526));
#69379=CARTESIAN_POINT('Ctrl Pts',(29.2327467417191,18.6727113011795,40.4667051785764));
#69380=CARTESIAN_POINT('Ctrl Pts',(29.1554183340175,18.6982046887411,40.4624735525459));
#69381=CARTESIAN_POINT('Ctrl Pts',(29.0792756935947,18.7275847217899,40.4582419265155));
#69382=CARTESIAN_POINT('Ctrl Pts',(29.0047334743213,18.7607155623138,40.4540103004851));
#69383=CARTESIAN_POINT('Ctrl Pts',(28.930431047456,18.7937398253289,40.449792287033));
#69384=CARTESIAN_POINT('Ctrl Pts',(28.857719193688,18.8304906268936,40.4455742735808));
#69385=CARTESIAN_POINT('Ctrl Pts',(28.7869907253848,18.8707844755174,40.4413562601287));
#69386=CARTESIAN_POINT('Ctrl Pts',(28.7162855306319,18.9110650652523,40.4371396346346));
#69387=CARTESIAN_POINT('Ctrl Pts',(28.6475628288216,18.9548861568875,40.4329230091406));
#69388=CARTESIAN_POINT('Ctrl Pts',(28.5811908292864,19.0020183216308,40.4287063836465));
#69389=CARTESIAN_POINT('Ctrl Pts',(28.514820349,19.0491494075234,40.4244898546706));
#69390=CARTESIAN_POINT('Ctrl Pts',(28.4508008423251,19.0995911457962,40.4202733256947));
#69391=CARTESIAN_POINT('Ctrl Pts',(28.3894703292654,19.1530716230228,40.4160567967187));
#69392=CARTESIAN_POINT('Ctrl Pts',(28.3277612816615,19.2068821840374,40.411814243146));
#69393=CARTESIAN_POINT('Ctrl Pts',(28.2687749035352,19.2637688221892,40.4075716895733));
#69394=CARTESIAN_POINT('Ctrl Pts',(28.212819195729,19.3234156678397,40.4033291360006));
#69395=CARTESIAN_POINT('Ctrl Pts',(28.1571259881399,19.3827826973546,40.3991064851559));
#69396=CARTESIAN_POINT('Ctrl Pts',(28.1044353398793,19.4448837011503,40.3948838343112));
#69397=CARTESIAN_POINT('Ctrl Pts',(28.0550103882544,19.5093740710018,40.3906611834665));
#69398=CARTESIAN_POINT('Ctrl Pts',(28.0052360028003,19.574320387013,40.3864086785298));
#69399=CARTESIAN_POINT('Ctrl Pts',(27.9587739428001,19.6416895926669,40.382156173593));
#69400=CARTESIAN_POINT('Ctrl Pts',(27.9158475089461,19.711101771266,40.3779036686563));
#69401=CARTESIAN_POINT('Ctrl Pts',(27.872921075092,19.7805139498651,40.3736511637196));
#69402=CARTESIAN_POINT('Ctrl Pts',(27.8335304411144,19.8519686552971,40.3693986587829));
#69403=CARTESIAN_POINT('Ctrl Pts',(27.797850205218,19.9250644059565,40.3651461538461));
#69404=CARTESIAN_POINT('Ctrl Pts',(27.7596965548658,20.0032272780009,40.3605988580562));
#69405=CARTESIAN_POINT('Ctrl Pts',(27.7256585715111,20.0835251228355,40.3560515622662));
#69406=CARTESIAN_POINT('Ctrl Pts',(27.6959618808451,20.1655189663742,40.3515042664763));
#69407=CARTESIAN_POINT('Ctrl Pts',(27.6663678835467,20.2472292690967,40.3469726955737));
#69408=CARTESIAN_POINT('Ctrl Pts',(27.6410853849827,20.3306235495274,40.3424411246712));
#69409=CARTESIAN_POINT('Ctrl Pts',(27.6202922314064,20.4152426263011,40.3379095537687));
#69410=CARTESIAN_POINT('Ctrl Pts',(27.5995450215131,20.4996747322999,40.3333879956358));
#69411=CARTESIAN_POINT('Ctrl Pts',(27.5832674962484,20.5853259036227,40.3288664375029));
#69412=CARTESIAN_POINT('Ctrl Pts',(27.5715884749131,20.6717200663683,40.32434487937));
#69413=CARTESIAN_POINT('Ctrl Pts',(27.5599448339301,20.7578525071921,40.3198370188163));
#69414=CARTESIAN_POINT('Ctrl Pts',(27.5528719937193,20.844723103544,40.3153291582625));
#69415=CARTESIAN_POINT('Ctrl Pts',(27.5504479634921,20.9318452463886,40.3108212977088));
#69416=CARTESIAN_POINT('Ctrl Pts',(27.5498217181246,20.954353149859,40.3096566972193));
#69417=CARTESIAN_POINT('Ctrl Pts',(27.5495054902598,20.9768777803791,40.3084920967298));
#69418=CARTESIAN_POINT('Ctrl Pts',(27.5495000708749,20.9994106292385,40.3073274962403));
#69419=CARTESIAN_POINT('',(27.5495010177781,21.0022334121089,39.5073274961711));
#69420=CARTESIAN_POINT('Ctrl Pts',(27.5495000708748,20.9994106297869,40.307327496212));
#69421=CARTESIAN_POINT('Ctrl Pts',(27.5494798595713,21.0834457515148,40.3029841775084));
#69422=CARTESIAN_POINT('Ctrl Pts',(27.5537867160569,21.1674327148593,40.2986408588047));
#69423=CARTESIAN_POINT('Ctrl Pts',(27.562379720821,21.2509135798149,40.2942975401011));
#69424=CARTESIAN_POINT('Ctrl Pts',(27.5709805838758,21.3344707879032,40.2899502494386));
#69425=CARTESIAN_POINT('Ctrl Pts',(27.5838753546468,21.4175205550911,40.2856029587762));
#69426=CARTESIAN_POINT('Ctrl Pts',(27.6009716505737,21.4996130789411,40.2812556681138));
#69427=CARTESIAN_POINT('Ctrl Pts',(27.6181014503126,21.5818664804746,40.2768998580147));
#69428=CARTESIAN_POINT('Ctrl Pts',(27.6394491300605,21.6631584772385,40.2725440479157));
#69429=CARTESIAN_POINT('Ctrl Pts',(27.6648718179047,21.7430522344925,40.2681882378167));
#69430=CARTESIAN_POINT('Ctrl Pts',(27.6903228538513,21.8230350789596,40.2638275706801));
#69431=CARTESIAN_POINT('Ctrl Pts',(27.719857803327,21.9016161811874,40.2594669035434));
#69432=CARTESIAN_POINT('Ctrl Pts',(27.7532856978946,21.9783788094164,40.2551062364068));
#69433=CARTESIAN_POINT('Ctrl Pts',(27.7867835005452,22.0553019720808,40.2507364497643));
#69434=CARTESIAN_POINT('Ctrl Pts',(27.8241903190306,22.1303986869069,40.2463666631219));
#69435=CARTESIAN_POINT('Ctrl Pts',(27.8652693153614,22.2032768401587,40.2419968764794));
#69436=CARTESIAN_POINT('Ctrl Pts',(27.8771188557864,22.2242990826717,40.2407363791914));
#69437=CARTESIAN_POINT('Ctrl Pts',(27.8892736786416,22.245136915382,40.2394758819034));
#69438=CARTESIAN_POINT('Ctrl Pts',(27.9017274553734,22.2657814102231,40.2382153846154));
#69439=CARTESIAN_POINT('Ctrl Pts',(27.9435364011762,22.335087660409,40.2339837315247));
#69440=CARTESIAN_POINT('Ctrl Pts',(27.9888610194208,22.4024498658945,40.229752078434));
#69441=CARTESIAN_POINT('Ctrl Pts',(28.0374950160594,22.4674891611213,40.2255204253432));
#69442=CARTESIAN_POINT('Ctrl Pts',(28.0860593884996,22.5324353464021,40.221294830267));
#69443=CARTESIAN_POINT('Ctrl Pts',(28.1379234538329,22.5950648569889,40.2170692351907));
#69444=CARTESIAN_POINT('Ctrl Pts',(28.1928363205505,22.6550255845994,40.2128436401144));
#69445=CARTESIAN_POINT('Ctrl Pts',(28.2478275613135,22.7150718907832,40.208612014084));
#69446=CARTESIAN_POINT('Ctrl Pts',(28.3058760560055,22.7724413974607,40.2043803880536));
#69447=CARTESIAN_POINT('Ctrl Pts',(28.3666877157555,22.8268117670236,40.2001487620232));
#69448=CARTESIAN_POINT('Ctrl Pts',(28.4273037524828,22.8810072343378,40.195930748571));
#69449=CARTESIAN_POINT('Ctrl Pts',(28.4906648674942,22.9322225074378,40.1917127351188));
#69450=CARTESIAN_POINT('Ctrl Pts',(28.5564424855217,22.9801747277433,40.1874947216666));
#69451=CARTESIAN_POINT('Ctrl Pts',(28.6221984591009,23.0281111691351,40.1832780961725));
#69452=CARTESIAN_POINT('Ctrl Pts',(28.6903689812933,23.0727864164253,40.1790614706784));
#69453=CARTESIAN_POINT('Ctrl Pts',(28.7605936890024,23.1139589036354,40.1748448451842));
#69454=CARTESIAN_POINT('Ctrl Pts',(28.8308167892745,23.1551304484111,40.1706283162083));
#69455=CARTESIAN_POINT('Ctrl Pts',(28.9030935800327,23.1927991584072,40.1664117872323));
#69456=CARTESIAN_POINT('Ctrl Pts',(28.9770373519693,23.2267684367114,40.1621952582563));
#69457=CARTESIAN_POINT('Ctrl Pts',(29.0514375080198,23.26094737485,40.1579527046837));
#69458=CARTESIAN_POINT('Ctrl Pts',(29.127524867365,23.2913808457708,40.153710151111));
#69459=CARTESIAN_POINT('Ctrl Pts',(29.2048849627703,23.3179176705766,40.1494675975384));
#69460=CARTESIAN_POINT('Ctrl Pts',(29.2818821453919,23.3443300054511,40.1452449466936));
#69461=CARTESIAN_POINT('Ctrl Pts',(29.3601396835155,23.366882096564,40.1410222958489));
#69462=CARTESIAN_POINT('Ctrl Pts',(29.439235322132,23.3854754716944,40.1367996450041));
#69463=CARTESIAN_POINT('Ctrl Pts',(29.5188901659834,23.4042003017683,40.1325471400675));
#69464=CARTESIAN_POINT('Ctrl Pts',(29.5993945366168,23.4189101351576,40.1282946351309));
#69465=CARTESIAN_POINT('Ctrl Pts',(29.6803103368298,23.4295573196083,40.1240421301944));
#69466=CARTESIAN_POINT('Ctrl Pts',(29.7612261370428,23.4402045040589,40.1197896252578));
#69467=CARTESIAN_POINT('Ctrl Pts',(29.8425528887275,23.4467890642942,40.1155371203212));
#69468=CARTESIAN_POINT('Ctrl Pts',(29.9238528242053,23.4493166103259,40.1112846153846));
#69469=CARTESIAN_POINT('Ctrl Pts',(30.0047541114153,23.4518317627212,40.107052962294));
#69470=CARTESIAN_POINT('Ctrl Pts',(30.0859314452372,23.4503390402701,40.1028213092033));
#69471=CARTESIAN_POINT('Ctrl Pts',(30.1669546582724,23.4448060029543,40.0985896561126));
#69472=CARTESIAN_POINT('Ctrl Pts',(30.2478618788609,23.4392808867083,40.0943640610364));
#69473=CARTESIAN_POINT('Ctrl Pts',(30.3286149570392,23.4297269747436,40.0901384659602));
#69474=CARTESIAN_POINT('Ctrl Pts',(30.4087819842452,23.4161638063998,40.0859128708839));
#69475=CARTESIAN_POINT('Ctrl Pts',(30.4890634293405,23.4025812801087,40.0816812448535));
#69476=CARTESIAN_POINT('Ctrl Pts',(30.5687566800655,23.3849780468442,40.0774496188231));
#69477=CARTESIAN_POINT('Ctrl Pts',(30.647431377453,23.363426085472,40.0732179927927));
#69478=CARTESIAN_POINT('Ctrl Pts',(30.7258529888,23.3419434538938,40.0689999793405));
#69479=CARTESIAN_POINT('Ctrl Pts',(30.8032621357507,23.3165375675207,40.0647819658884));
#69480=CARTESIAN_POINT('Ctrl Pts',(30.8792428911614,23.2873307999374,40.0605639524363));
#69481=CARTESIAN_POINT('Ctrl Pts',(30.9551986447314,23.2581336429844,40.0563473269422));
#69482=CARTESIAN_POINT('Ctrl Pts',(31.0297265066468,23.2251382552068,40.0521307014481));
#69483=CARTESIAN_POINT('Ctrl Pts',(31.102427969672,23.1885161232408,40.047914075954));
#69484=CARTESIAN_POINT('Ctrl Pts',(31.1751277685676,23.1518948295519,40.0436975469781));
#69485=CARTESIAN_POINT('Ctrl Pts',(31.2460008370891,23.1116471668463,40.0394810180021));
#69486=CARTESIAN_POINT('Ctrl Pts',(31.3146721296427,23.0679911608952,40.0352644890262));
#69487=CARTESIAN_POINT('Ctrl Pts',(31.3837672643444,23.0240657082125,40.0310219354535));
#69488=CARTESIAN_POINT('Ctrl Pts',(31.4506329410647,22.9766899371753,40.0267793818808));
#69489=CARTESIAN_POINT('Ctrl Pts',(31.5149171864598,22.9261298419808,40.0225368283081));
#69490=CARTESIAN_POINT('Ctrl Pts',(31.5788998606836,22.8758069350278,40.0183141774634));
#69491=CARTESIAN_POINT('Ctrl Pts',(31.6403249528404,22.8223298638654,40.0140915266187));
#69492=CARTESIAN_POINT('Ctrl Pts',(31.6988805246043,22.7659997772141,40.009868875774));
#69493=CARTESIAN_POINT('Ctrl Pts',(31.7578500835743,22.7092714375103,40.0056163708373));
#69494=CARTESIAN_POINT('Ctrl Pts',(31.8139090610151,22.6496499318426,40.0013638659006));
#69495=CARTESIAN_POINT('Ctrl Pts',(31.866779596433,22.5874773032523,39.9971113609639));
#69496=CARTESIAN_POINT('Ctrl Pts',(31.9196501318509,22.5253046746621,39.9928588560272));
#69497=CARTESIAN_POINT('Ctrl Pts',(31.9693319864446,22.4605813380857,39.9886063510905));
#69498=CARTESIAN_POINT('Ctrl Pts',(32.0155922081882,22.3936779758219,39.9843538461538));
#69499=CARTESIAN_POINT('Ctrl Pts',(32.0616255963278,22.3271026692874,39.9801221930632));
#69500=CARTESIAN_POINT('Ctrl Pts',(32.1044430424686,22.2581196710003,39.9758905399725));
#69501=CARTESIAN_POINT('Ctrl Pts',(32.1437837664059,22.1870726232605,39.9716588868818));
#69502=CARTESIAN_POINT('Ctrl Pts',(32.1830681703498,22.1161272861364,39.9674332918056));
#69503=CARTESIAN_POINT('Ctrl Pts',(32.2188855141122,22.0431241714434,39.9632076967294));
#69504=CARTESIAN_POINT('Ctrl Pts',(32.2510177243999,21.9684366032102,39.9589821016532));
#69505=CARTESIAN_POINT('Ctrl Pts',(32.2831957951843,21.8936424376114,39.9547504756227));
#69506=CARTESIAN_POINT('Ctrl Pts',(32.3116779526552,21.8171594019872,39.9505188495923));
#69507=CARTESIAN_POINT('Ctrl Pts',(32.3362910034261,21.739387988346,39.9462872235619));
#69508=CARTESIAN_POINT('Ctrl Pts',(32.3608248772853,21.6618667550017,39.9420692101098));
#69509=CARTESIAN_POINT('Ctrl Pts',(32.3815143425697,21.5830658595736,39.9378511966576));
#69510=CARTESIAN_POINT('Ctrl Pts',(32.398236362313,21.503401033451,39.9336331832055));
#69511=CARTESIAN_POINT('Ctrl Pts',(32.4149528795936,21.4237624214309,39.9294165577114));
#69512=CARTESIAN_POINT('Ctrl Pts',(32.42770444851,21.3432608978029,39.9251999322173));
#69513=CARTESIAN_POINT('Ctrl Pts',(32.4364187343998,21.2623242281335,39.9209833067233));
#69514=CARTESIAN_POINT('Ctrl Pts',(32.4451328208203,21.1813894110971,39.9167667777473));
#69515=CARTESIAN_POINT('Ctrl Pts',(32.4498097593208,21.1000199300789,39.9125502487714));
#69516=CARTESIAN_POINT('Ctrl Pts',(32.4504290360183,21.0186491136093,39.9083337197955));
#69517=CARTESIAN_POINT('Ctrl Pts',(32.451052134918,20.9367760729878,39.9040911662228));
#69518=CARTESIAN_POINT('Ctrl Pts',(32.4475672928651,20.8549021560147,39.8998486126501));
#69519=CARTESIAN_POINT('Ctrl Pts',(32.4400068056719,20.7734673571538,39.8956060590774));
#69520=CARTESIAN_POINT('Ctrl Pts',(32.4324817863443,20.6924145863861,39.8913834082327));
#69521=CARTESIAN_POINT('Ctrl Pts',(32.4209193978756,20.6117972789425,39.887160757388));
#69522=CARTESIAN_POINT('Ctrl Pts',(32.4054031937343,20.5320408932685,39.8829381065433));
#69523=CARTESIAN_POINT('Ctrl Pts',(32.3897772902115,20.4517206308823,39.8786856016066));
#69524=CARTESIAN_POINT('Ctrl Pts',(32.3701415606893,20.3722739757231,39.8744330966699));
#69525=CARTESIAN_POINT('Ctrl Pts',(32.3466324024204,20.29411996918,39.8701805917332));
#69526=CARTESIAN_POINT('Ctrl Pts',(32.3231232441516,20.2159659626369,39.8659280867965));
#69527=CARTESIAN_POINT('Ctrl Pts',(32.2957408759543,20.1391050305231,39.8616755818598));
#69528=CARTESIAN_POINT('Ctrl Pts',(32.2646701270147,20.0639340483667,39.8574230769231));
#69529=CARTESIAN_POINT('Ctrl Pts',(32.2337517312124,19.9891316616049,39.8531914238322));
#69530=CARTESIAN_POINT('Ctrl Pts',(32.1990654302537,19.915722886428,39.8489597707414));
#69531=CARTESIAN_POINT('Ctrl Pts',(32.1607582373052,19.8441132884588,39.8447281176506));
#69532=CARTESIAN_POINT('Ctrl Pts',(32.1225058847521,19.7726062064496,39.8405025225742));
#69533=CARTESIAN_POINT('Ctrl Pts',(32.0806431528224,19.7028935924912,39.8362769274979));
#69534=CARTESIAN_POINT('Ctrl Pts',(32.0353651668613,19.6353612611655,39.8320513324215));
#69535=CARTESIAN_POINT('Ctrl Pts',(31.9900225581792,19.5677325447443,39.8278197063911));
#69536=CARTESIAN_POINT('Ctrl Pts',(31.9412551341529,19.5022907661456,39.8235880803608));
#69537=CARTESIAN_POINT('Ctrl Pts',(31.8893052009778,19.4393987993218,39.8193564543304));
#69538=CARTESIAN_POINT('Ctrl Pts',(31.837522383828,19.3767091475902,39.8151384408781));
#69539=CARTESIAN_POINT('Ctrl Pts',(31.7825777857254,19.3165532980507,39.8109204274258));
#69540=CARTESIAN_POINT('Ctrl Pts',(31.7247537407076,19.2592602768033,39.8067024139735));
#69541=CARTESIAN_POINT('Ctrl Pts',(31.6669487229759,19.201986108106,39.8024857884793));
#69542=CARTESIAN_POINT('Ctrl Pts',(31.6062664698693,19.1475732238359,39.7982691629851));
#69543=CARTESIAN_POINT('Ctrl Pts',(31.5430269479006,19.0963146037088,39.7940525374908));
#69544=CARTESIAN_POINT('Ctrl Pts',(31.4797888734788,19.0450571568867,39.7898360085148));
#69545=CARTESIAN_POINT('Ctrl Pts',(31.413994008377,18.9969541224548,39.7856194795387));
#69546=CARTESIAN_POINT('Ctrl Pts',(31.345995124287,18.9522579812399,39.7814029505626));
#69547=CARTESIAN_POINT('Ctrl Pts',(31.2775765481877,18.9072859735375,39.7771603969901));
#69548=CARTESIAN_POINT('Ctrl Pts',(31.2069270421898,18.8657633326497,39.7729178434176));
#69549=CARTESIAN_POINT('Ctrl Pts',(31.1344336463167,18.8279018088253,39.7686752898451));
#69550=CARTESIAN_POINT('Ctrl Pts',(31.0622803324936,18.79021790152,39.7644526390002));
#69551=CARTESIAN_POINT('Ctrl Pts',(30.9883008394824,18.7561609829746,39.7602299881554));
#69552=CARTESIAN_POINT('Ctrl Pts',(30.9128978276724,18.7258918657568,39.7560073373105));
#69553=CARTESIAN_POINT('Ctrl Pts',(30.836961717461,18.6954087462384,39.7517548323742));
#69554=CARTESIAN_POINT('Ctrl Pts',(30.7595823337707,18.6687673523469,39.7475023274378));
#69555=CARTESIAN_POINT('Ctrl Pts',(30.681185636754,18.6460806347115,39.7432498225014));
#69556=CARTESIAN_POINT('Ctrl Pts',(30.6027889397373,18.6233939170762,39.7389973175651));
#69557=CARTESIAN_POINT('Ctrl Pts',(30.5233754057877,18.604661923107,39.7347448126287));
#69558=CARTESIAN_POINT('Ctrl Pts',(30.4433786738126,18.5899448965619,39.7304923076923));
#69559=CARTESIAN_POINT('Ctrl Pts',(30.3637741999414,18.5753000338763,39.7262606546018));
#69560=CARTESIAN_POINT('Ctrl Pts',(30.2832944898639,18.5645760415146,39.7220290015113));
#69561=CARTESIAN_POINT('Ctrl Pts',(30.2023599501657,18.5578696389077,39.7177973484208));
#69562=CARTESIAN_POINT('Ctrl Pts',(30.1215412759699,18.5511728371549,39.7135717533447));
#69563=CARTESIAN_POINT('Ctrl Pts',(30.0402695246898,18.5484822400873,39.7093461582686));
#69564=CARTESIAN_POINT('Ctrl Pts',(29.9589746360341,18.5498434397958,39.7051205631925));
#69565=CARTESIAN_POINT('Ctrl Pts',(29.8775637197526,18.5512065822682,39.7008889371621));
#69566=CARTESIAN_POINT('Ctrl Pts',(29.7961300642939,18.5566331641844,39.6966573111316));
#69567=CARTESIAN_POINT('Ctrl Pts',(29.715109958262,18.5661167008013,39.6924256851012));
#69568=CARTESIAN_POINT('Ctrl Pts',(29.6343504831417,18.5755697301414,39.6882076716492));
#69569=CARTESIAN_POINT('Ctrl Pts',(29.5540023659258,18.5890536150994,39.6839896581971));
#69570=CARTESIAN_POINT('Ctrl Pts',(29.4744952008885,18.6065098796714,39.6797716447451));
#69571=CARTESIAN_POINT('Ctrl Pts',(29.3950141980744,18.6239604001737,39.6755550192512));
#69572=CARTESIAN_POINT('Ctrl Pts',(29.3163740515445,18.6453806048803,39.6713383937572));
#69573=CARTESIAN_POINT('Ctrl Pts',(29.238994514479,18.6706608445727,39.6671217682633));
#69574=CARTESIAN_POINT('Ctrl Pts',(29.1616167486238,18.6959405056027,39.6629052392875));
#69575=CARTESIAN_POINT('Ctrl Pts',(29.0854999763348,18.7250798805249,39.6586887103117));
#69576=CARTESIAN_POINT('Ctrl Pts',(29.0110477497606,18.7579197836058,39.6544721813359));
#69577=CARTESIAN_POINT('Ctrl Pts',(28.9361360008617,18.7909623759721,39.650229627763));
#69578=CARTESIAN_POINT('Ctrl Pts',(28.8629098570549,18.8277511550815,39.6459870741902));
#69579=CARTESIAN_POINT('Ctrl Pts',(28.7917572692283,18.8680760441476,39.6417445206173));
#69580=CARTESIAN_POINT('Ctrl Pts',(28.720938473444,18.9082117605147,39.6375218697727));
#69581=CARTESIAN_POINT('Ctrl Pts',(28.6521741878427,18.9518501852333,39.6332992189281));
#69582=CARTESIAN_POINT('Ctrl Pts',(28.5858180661943,18.9987404695798,39.6290765680836));
#69583=CARTESIAN_POINT('Ctrl Pts',(28.5189928075365,19.0459622676921,39.6248240631466));
#69584=CARTESIAN_POINT('Ctrl Pts',(28.4546102735963,19.0964817907916,39.6205715582096));
#69585=CARTESIAN_POINT('Ctrl Pts',(28.3929965731608,19.1500026388864,39.6163190532725));
#69586=CARTESIAN_POINT('Ctrl Pts',(28.3313828727253,19.2035234869813,39.6120665483355));
#69587=CARTESIAN_POINT('Ctrl Pts',(28.2725383042427,19.2600452857358,39.6078140433985));
#69588=CARTESIAN_POINT('Ctrl Pts',(28.2167488821321,19.3192365720831,39.6035615384615));
#69589=CARTESIAN_POINT('Ctrl Pts',(28.1619247299333,19.3774037293825,39.5993826104664));
#69590=CARTESIAN_POINT('Ctrl Pts',(28.1098346741667,19.4383783064752,39.5952036824712));
#69591=CARTESIAN_POINT('Ctrl Pts',(28.0607848511331,19.5018695462661,39.591024754476));
#69592=CARTESIAN_POINT('Ctrl Pts',(28.0117989128589,19.565278092128,39.5868512693101));
#69593=CARTESIAN_POINT('Ctrl Pts',(27.9658456427512,19.6311964262606,39.5826777841441));
#69594=CARTESIAN_POINT('Ctrl Pts',(27.9231939713022,19.6992975093571,39.5785042989781));
#69595=CARTESIAN_POINT('Ctrl Pts',(27.8805840156664,19.7673319856371,39.5743348957232));
#69596=CARTESIAN_POINT('Ctrl Pts',(27.8412695038561,19.8375445733112,39.5701654924682));
#69597=CARTESIAN_POINT('Ctrl Pts',(27.8054777346368,19.9095770193062,39.5659960892133));
#69598=CARTESIAN_POINT('Ctrl Pts',(27.7697093675961,19.9815623674292,39.5618294120912));
#69599=CARTESIAN_POINT('Ctrl Pts',(27.7374593826102,20.0553647856335,39.5576627349692));
#69600=CARTESIAN_POINT('Ctrl Pts',(27.7089097304738,20.130600421623,39.5534960578471));
#69601=CARTESIAN_POINT('Ctrl Pts',(27.6803605581769,20.2058347931124,39.5493294507552));
#69602=CARTESIAN_POINT('Ctrl Pts',(27.6555117808199,20.2825018947326,39.5451628436633));
#69603=CARTESIAN_POINT('Ctrl Pts',(27.634497180122,20.3601979531531,39.5409962365714));
#69604=CARTESIAN_POINT('Ctrl Pts',(27.613483522936,20.4378905231823,39.5368298165515));
#69605=CARTESIAN_POINT('Ctrl Pts',(27.5963038170669,20.5166114951214,39.5326633965316));
#69606=CARTESIAN_POINT('Ctrl Pts',(27.583041376474,20.5959439863545,39.5284969765117));
#69607=CARTESIAN_POINT('Ctrl Pts',(27.5697678174451,20.675342985197,39.5243270636148));
#69608=CARTESIAN_POINT('Ctrl Pts',(27.5604181510839,20.7553540542034,39.5201571507179));
#69609=CARTESIAN_POINT('Ctrl Pts',(27.5550240342586,20.8355531181594,39.515987237821));
#69610=CARTESIAN_POINT('Ctrl Pts',(27.5512900107855,20.8910701188177,39.5131006572847));
#69611=CARTESIAN_POINT('Ctrl Pts',(27.5494503831303,20.9466770746821,39.5102140767484));
#69612=CARTESIAN_POINT('Ctrl Pts',(27.5495010177774,21.0022334113197,39.5073274962121));
#69613=CARTESIAN_POINT('',(27.5495001606026,20.9991128058326,38.7073274961651));
#69614=CARTESIAN_POINT('Ctrl Pts',(27.5495010177781,21.0022334121089,39.5073274961711));
#69615=CARTESIAN_POINT('Ctrl Pts',(27.549598400284,21.1090814633755,39.501775915131));
#69616=CARTESIAN_POINT('Ctrl Pts',(27.5566877679976,21.2156197797143,39.496224334091));
#69617=CARTESIAN_POINT('Ctrl Pts',(27.5706261347395,21.3210807885708,39.490672753051));
#69618=CARTESIAN_POINT('Ctrl Pts',(27.5823778813055,21.4099973073873,39.4859920917776));
#69619=CARTESIAN_POINT('Ctrl Pts',(27.5989973949366,21.4981487045857,39.4813114305042));
#69620=CARTESIAN_POINT('Ctrl Pts',(27.6203735160512,21.5850880676353,39.4766307692308));
#69621=CARTESIAN_POINT('Ctrl Pts',(27.6396990608233,21.6636874797587,39.4723991161391));
#69622=CARTESIAN_POINT('Ctrl Pts',(27.6629591567608,21.7414753688337,39.4681674630475));
#69623=CARTESIAN_POINT('Ctrl Pts',(27.6900694109329,21.8180286814607,39.4639358099558));
#69624=CARTESIAN_POINT('Ctrl Pts',(27.7171408541942,21.8944724007294,39.4597102148786));
#69625=CARTESIAN_POINT('Ctrl Pts',(27.7480513547551,21.9696846193321,39.4554846198013));
#69626=CARTESIAN_POINT('Ctrl Pts',(27.7826659856413,22.0432545800369,39.4512590247241));
#69627=CARTESIAN_POINT('Ctrl Pts',(27.817330020033,22.1169295429869,39.4470273986939));
#69628=CARTESIAN_POINT('Ctrl Pts',(27.8557086376473,22.1889571053602,39.4427957726638));
#69629=CARTESIAN_POINT('Ctrl Pts',(27.8976168188683,22.2589420994209,39.4385641466336));
#69630=CARTESIAN_POINT('Ctrl Pts',(27.9393901870549,22.3287019610819,39.4343461331805));
#69631=CARTESIAN_POINT('Ctrl Pts',(27.9846702200657,22.3964319670426,39.4301281197273));
#69632=CARTESIAN_POINT('Ctrl Pts',(28.0332272382171,22.4617643974009,39.4259101062742));
#69633=CARTESIAN_POINT('Ctrl Pts',(28.081768278443,22.527075329802,39.4216934807791));
#69634=CARTESIAN_POINT('Ctrl Pts',(28.1335838853661,22.5899898805696,39.417476855284));
#69635=CARTESIAN_POINT('Ctrl Pts',(28.1884017569896,22.6501703111866,39.4132602297889));
#69636=CARTESIAN_POINT('Ctrl Pts',(28.243218373837,22.7103493642791,39.409043700812));
#69637=CARTESIAN_POINT('Ctrl Pts',(28.3010368049129,22.7677940787939,39.4048271718351));
#69638=CARTESIAN_POINT('Ctrl Pts',(28.3615462292325,22.8222018250067,39.4006106428582));
#69639=CARTESIAN_POINT('Ctrl Pts',(28.4224291202698,22.8769453781227,39.3963680892867));
#69640=CARTESIAN_POINT('Ctrl Pts',(28.4860359929807,22.9286140160432,39.3921255357152));
#69641=CARTESIAN_POINT('Ctrl Pts',(28.5520160260383,22.9769402270049,39.3878829821437));
#69642=CARTESIAN_POINT('Ctrl Pts',(28.6176865326547,23.0250397293791,39.383660331298));
#69643=CARTESIAN_POINT('Ctrl Pts',(28.685707561096,23.0698278838322,39.3794376804523));
#69644=CARTESIAN_POINT('Ctrl Pts',(28.7557051918887,23.1110851902534,39.3752150296066));
#69645=CARTESIAN_POINT('Ctrl Pts',(28.826197705057,23.1526341853158,39.3709625246722));
#69646=CARTESIAN_POINT('Ctrl Pts',(28.8986944549242,23.1906019893261,39.3667100197378));
#69647=CARTESIAN_POINT('Ctrl Pts',(28.9727912939311,23.2248129189162,39.3624575148033));
#69648=CARTESIAN_POINT('Ctrl Pts',(29.0468881329381,23.2590238485062,39.3582050098689));
#69649=CARTESIAN_POINT('Ctrl Pts',(29.1225845972269,23.2894777852095,39.3539525049345));
#69650=CARTESIAN_POINT('Ctrl Pts',(29.1994610266245,23.3160499999151,39.3497));
#69651=CARTESIAN_POINT('Ctrl Pts',(29.2759604981033,23.3424919197198,39.3454683469109));
#69652=CARTESIAN_POINT('Ctrl Pts',(29.3539145146842,23.3651890349848,39.3412366938217));
#69653=CARTESIAN_POINT('Ctrl Pts',(29.4329219799901,23.3839825438165,39.3370050407325));
#69654=CARTESIAN_POINT('Ctrl Pts',(29.5118163385842,23.4027491479502,39.3327794456578));
#69655=CARTESIAN_POINT('Ctrl Pts',(29.5917607022621,23.4176231380356,39.3285538505831));
#69656=CARTESIAN_POINT('Ctrl Pts',(29.6723368661057,23.4284948261601,39.3243282555084));
#69657=CARTESIAN_POINT('Ctrl Pts',(29.7530280318121,23.4393820308386,39.3200966294776));
#69658=CARTESIAN_POINT('Ctrl Pts',(29.8343523537307,23.4462553632716,39.3158650034468));
#69659=CARTESIAN_POINT('Ctrl Pts',(29.9158775237706,23.4490556667812,39.311633377416));
#69660=CARTESIAN_POINT('Ctrl Pts',(29.9971404381428,23.4518469620855,39.3074153639653));
#69661=CARTESIAN_POINT('Ctrl Pts',(30.0786024449596,23.4505913604899,39.3031973505147));
#69662=CARTESIAN_POINT('Ctrl Pts',(30.1598300409076,23.4452821121546,39.298979337064));
#69663=CARTESIAN_POINT('Ctrl Pts',(30.2410309085164,23.4399746108536,39.2947627115714));
#69664=CARTESIAN_POINT('Ctrl Pts',(30.3219970549808,23.4306161420215,39.2905460860788));
#69665=CARTESIAN_POINT('Ctrl Pts',(30.4022970157302,23.4172520268136,39.2863294605861));
#69666=CARTESIAN_POINT('Ctrl Pts',(30.4825951384213,23.4038882175091,39.2821129316117));
#69667=CARTESIAN_POINT('Ctrl Pts',(30.5622266474021,23.3865190215507,39.2778964026372));
#69668=CARTESIAN_POINT('Ctrl Pts',(30.6407686505217,23.3652411687836,39.2736798736627));
#69669=CARTESIAN_POINT('Ctrl Pts',(30.7197954182962,23.3438319881849,39.2694373200883));
#69670=CARTESIAN_POINT('Ctrl Pts',(30.7977187218238,23.318465845832,39.2651947665138));
#69671=CARTESIAN_POINT('Ctrl Pts',(30.8741234448468,23.2892921292769,39.2609522129393));
#69672=CARTESIAN_POINT('Ctrl Pts',(30.9501697368838,23.2602552728997,39.256729562096));
#69673=CARTESIAN_POINT('Ctrl Pts',(31.0247112581349,23.2274467268812,39.2525069112527));
#69674=CARTESIAN_POINT('Ctrl Pts',(31.0973606725139,23.191061342003,39.2482842604094));
#69675=CARTESIAN_POINT('Ctrl Pts',(31.1705237174829,23.1544187128391,39.2440317554694));
#69676=CARTESIAN_POINT('Ctrl Pts',(31.2417673802195,23.1141487063814,39.2397792505294));
#69677=CARTESIAN_POINT('Ctrl Pts',(31.3107247110944,23.0704953469464,39.2355267455893));
#69678=CARTESIAN_POINT('Ctrl Pts',(31.3796820419693,23.0268419875113,39.2312742406493));
#69679=CARTESIAN_POINT('Ctrl Pts',(31.446352689667,22.9798056003307,39.2270217357093));
#69680=CARTESIAN_POINT('Ctrl Pts',(31.510404074096,22.9296709001678,39.2227692307692));
#69681=CARTESIAN_POINT('Ctrl Pts',(31.5741413872004,22.8797820318761,39.2185375776792));
#69682=CARTESIAN_POINT('Ctrl Pts',(31.6355234891141,22.8266385909933,39.2143059245891));
#69683=CARTESIAN_POINT('Ctrl Pts',(31.6941992637275,22.7704912043795,39.2100742714991));
#69684=CARTESIAN_POINT('Ctrl Pts',(31.7527910383807,22.7144241980977,39.2058486764235));
#69685=CARTESIAN_POINT('Ctrl Pts',(31.8086838475751,22.655362105796,39.2016230813479));
#69686=CARTESIAN_POINT('Ctrl Pts',(31.8615585328514,22.5935965859553,39.1973974862723));
#69687=CARTESIAN_POINT('Ctrl Pts',(31.9145086832022,22.5317429116502,39.1931658602417));
#69688=CARTESIAN_POINT('Ctrl Pts',(31.9644317291242,22.4671783895145,39.1889342342112));
#69689=CARTESIAN_POINT('Ctrl Pts',(32.0110432916244,22.4002339551705,39.1847026081806));
#69690=CARTESIAN_POINT('Ctrl Pts',(32.0575049109165,22.3335048721838,39.1804845947291));
#69691=CARTESIAN_POINT('Ctrl Pts',(32.1006760392652,22.2644115384322,39.1762665812777));
#69692=CARTESIAN_POINT('Ctrl Pts',(32.1403156599763,22.1933143448648,39.1720485678262));
#69693=CARTESIAN_POINT('Ctrl Pts',(32.1799422370754,22.1222405461785,39.1678319423328));
#69694=CARTESIAN_POINT('Ctrl Pts',(32.2160393880842,22.0491646027831,39.1636153168394));
#69695=CARTESIAN_POINT('Ctrl Pts',(32.2484109322814,21.9744734627468,39.159398691346));
#69696=CARTESIAN_POINT('Ctrl Pts',(32.2807817354968,21.8997840323839,39.1551821623708));
#69697=CARTESIAN_POINT('Ctrl Pts',(32.3094269176567,21.8234799058125,39.1509656333956));
#69698=CARTESIAN_POINT('Ctrl Pts',(32.334198124931,21.7459687416832,39.1467491044204));
#69699=CARTESIAN_POINT('Ctrl Pts',(32.3591222211625,21.6679791753136,39.1425065508469));
#69700=CARTESIAN_POINT('Ctrl Pts',(32.3801241981086,21.5887680689479,39.1382639972734));
#69701=CARTESIAN_POINT('Ctrl Pts',(32.3971041453202,21.5087651388298,39.1340214436999));
#69702=CARTESIAN_POINT('Ctrl Pts',(32.4140044359546,21.4291375196302,39.1297987928559));
#69703=CARTESIAN_POINT('Ctrl Pts',(32.4269203299235,21.3487259609619,39.1255761420119));
#69704=CARTESIAN_POINT('Ctrl Pts',(32.4358051785355,21.2679615312307,39.121353491168));
#69705=CARTESIAN_POINT('Ctrl Pts',(32.444752842928,21.186626097884,39.1171009862297));
#69706=CARTESIAN_POINT('Ctrl Pts',(32.4496122121228,21.1049332620539,39.1128484812915));
#69707=CARTESIAN_POINT('Ctrl Pts',(32.4503890010604,21.0233236678556,39.1085959763532));
#69708=CARTESIAN_POINT('Ctrl Pts',(32.451165789998,20.9417140736573,39.104343471415));
#69709=CARTESIAN_POINT('Ctrl Pts',(32.4478600810791,20.8601881926928,39.1000909664767));
#69710=CARTESIAN_POINT('Ctrl Pts',(32.4405304201813,20.7791798963641,39.0958384615385));
#69711=CARTESIAN_POINT('Ctrl Pts',(32.4332366997276,20.6985688181592,39.0916068084402));
#69712=CARTESIAN_POINT('Ctrl Pts',(32.4219311541044,20.6181687409942,39.087375155342));
#69713=CARTESIAN_POINT('Ctrl Pts',(32.4066336390494,20.5384105965297,39.0831435022437));
#69714=CARTESIAN_POINT('Ctrl Pts',(32.3913580238441,20.4587666334451,39.0789179071599));
#69715=CARTESIAN_POINT('Ctrl Pts',(32.3721018763099,20.3797632305195,39.074692312076));
#69716=CARTESIAN_POINT('Ctrl Pts',(32.3489368602303,20.3018267574222,39.0704667169922));
#69717=CARTESIAN_POINT('Ctrl Pts',(32.3257387820782,20.2237790501559,39.0662350909637));
#69718=CARTESIAN_POINT('Ctrl Pts',(32.2986207283465,20.1468017860686,39.0620034649352));
#69719=CARTESIAN_POINT('Ctrl Pts',(32.2677062294127,20.071313450575,39.0577718389066));
#69720=CARTESIAN_POINT('Ctrl Pts',(32.236891178242,19.9960679508499,39.0535538254469));
#69721=CARTESIAN_POINT('Ctrl Pts',(32.2023042310867,19.9223022528441,39.0493358119872));
#69722=CARTESIAN_POINT('Ctrl Pts',(32.16411719618,19.8504144176277,39.0451177985274));
#69723=CARTESIAN_POINT('Ctrl Pts',(32.1259427269048,19.7785502374569,39.0409011730257));
#69724=CARTESIAN_POINT('Ctrl Pts',(32.0841707402906,19.7085631031235,39.036684547524));
#69725=CARTESIAN_POINT('Ctrl Pts',(32.0390196885697,19.6408278403288,39.0324679220224));
#69726=CARTESIAN_POINT('Ctrl Pts',(31.9938696703524,19.5730941279884,39.0282513930389));
#69727=CARTESIAN_POINT('Ctrl Pts',(31.9453409995579,19.5076125708324,39.0240348640554));
#69728=CARTESIAN_POINT('Ctrl Pts',(31.8936954862696,19.4447290733502,39.0198183350719));
#69729=CARTESIAN_POINT('Ctrl Pts',(31.8417312148731,19.3814574564861,39.0155757815082));
#69730=CARTESIAN_POINT('Ctrl Pts',(31.786611784374,19.3208164575192,39.0113332279445));
#69731=CARTESIAN_POINT('Ctrl Pts',(31.7286438286116,19.2631232732853,39.0070906743809));
#69732=CARTESIAN_POINT('Ctrl Pts',(31.670947812728,19.2057007399192,39.0028680235287));
#69733=CARTESIAN_POINT('Ctrl Pts',(31.6104303236937,19.1511986974807,38.9986453726766));
#69734=CARTESIAN_POINT('Ctrl Pts',(31.5474280466105,19.0998903477527,38.9944227218245));
#69735=CARTESIAN_POINT('Ctrl Pts',(31.4839803445355,19.0482192488939,38.990170216905));
#69736=CARTESIAN_POINT('Ctrl Pts',(31.4180129681252,18.999787460934,38.9859177119856));
#69737=CARTESIAN_POINT('Ctrl Pts',(31.3498990722644,18.9548294093891,38.9816652070661));
#69738=CARTESIAN_POINT('Ctrl Pts',(31.2817851764036,18.9098713578442,38.9774127021467));
#69739=CARTESIAN_POINT('Ctrl Pts',(31.2115252018782,18.8683872295464,38.9731601972272));
#69740=CARTESIAN_POINT('Ctrl Pts',(31.1395152976815,18.8305634057779,38.9689076923078));
#69741=CARTESIAN_POINT('Ctrl Pts',(31.0678584887123,18.7929250483256,38.964676039231));
#69742=CARTESIAN_POINT('Ctrl Pts',(30.9942008652579,18.7587703676255,38.9604443861542));
#69743=CARTESIAN_POINT('Ctrl Pts',(30.9189151027149,18.7283166409021,38.9562127330774));
#69744=CARTESIAN_POINT('Ctrl Pts',(30.8437371189115,18.697906511589,38.951987138015));
#69745=CARTESIAN_POINT('Ctrl Pts',(30.7669360525442,18.6711869862405,38.9477615429526));
#69746=CARTESIAN_POINT('Ctrl Pts',(30.6889088743533,18.6483293570661,38.9435359478903));
#69747=CARTESIAN_POINT('Ctrl Pts',(30.6107703320392,18.6254391043893,38.9393043218564));
#69748=CARTESIAN_POINT('Ctrl Pts',(30.5314025984032,18.6064219829982,38.9350726958225));
#69749=CARTESIAN_POINT('Ctrl Pts',(30.4512241812916,18.591401447269,38.9308410697886));
#69750=CARTESIAN_POINT('Ctrl Pts',(30.371303687812,18.576429230667,38.9266230563502));
#69751=CARTESIAN_POINT('Ctrl Pts',(30.2905781738591,18.565428028317,38.9224050429117));
#69752=CARTESIAN_POINT('Ctrl Pts',(30.2094752049009,18.5584696625822,38.9181870294733));
#69753=CARTESIAN_POINT('Ctrl Pts',(30.1283989232716,18.5515135865316,38.9139704039928));
#69754=CARTESIAN_POINT('Ctrl Pts',(30.0469458960343,18.5485977449462,38.9097537785123));
#69755=CARTESIAN_POINT('Ctrl Pts',(29.9655494985754,18.5497421741883,38.9055371530318));
#69756=CARTESIAN_POINT('Ctrl Pts',(29.8841549642704,18.5508865772346,38.9013206240694));
#69757=CARTESIAN_POINT('Ctrl Pts',(29.8028175219104,18.5560910586578,38.897104095107));
#69758=CARTESIAN_POINT('Ctrl Pts',(29.7219697977931,18.5653235416876,38.8928875661446));
#69759=CARTESIAN_POINT('Ctrl Pts',(29.6406230775002,18.5746130080619,38.8886450125556));
#69760=CARTESIAN_POINT('Ctrl Pts',(29.5597726157875,18.5879803301642,38.8844024589666));
#69761=CARTESIAN_POINT('Ctrl Pts',(29.4798512650611,18.6053402029638,38.8801599053776));
#69762=CARTESIAN_POINT('Ctrl Pts',(29.40030484307,18.62261863676,38.875937254546));
#69763=CARTESIAN_POINT('Ctrl Pts',(29.3216792720991,18.6438520687983,38.8717146037144));
#69764=CARTESIAN_POINT('Ctrl Pts',(29.2443867723394,18.6689060722089,38.8674919528828));
#69765=CARTESIAN_POINT('Ctrl Pts',(29.1665478147042,18.694137207392,38.8632394479152));
#69766=CARTESIAN_POINT('Ctrl Pts',(29.0900612987055,18.7232429775573,38.8589869429475));
#69767=CARTESIAN_POINT('Ctrl Pts',(29.0153266796838,18.7560372769902,38.8547344379799));
#69768=CARTESIAN_POINT('Ctrl Pts',(28.9405920606622,18.7888315764231,38.8504819330122));
#69769=CARTESIAN_POINT('Ctrl Pts',(28.8676097348207,18.825314136383,38.8462294280446));
#69770=CARTESIAN_POINT('Ctrl Pts',(28.7967512934842,18.8652534576048,38.8419769230769));
#69771=CARTESIAN_POINT('Ctrl Pts',(28.7262403018338,18.9049969390035,38.8377452699865));
#69772=CARTESIAN_POINT('Ctrl Pts',(28.6575686579746,18.9483119833915,38.833513616896));
#69773=CARTESIAN_POINT('Ctrl Pts',(28.5911211558115,18.9950035779588,38.8292819638055));
#69774=CARTESIAN_POINT('Ctrl Pts',(28.524768779579,19.0416283290596,38.8250563687297));
#69775=CARTESIAN_POINT('Ctrl Pts',(28.4606345982962,19.0916197648742,38.8208307736538));
#69776=CARTESIAN_POINT('Ctrl Pts',(28.3990779776216,19.1447375042157,38.8166051785779));
#69777=CARTESIAN_POINT('Ctrl Pts',(28.3374335006382,19.1979310555244,38.8123735525474));
#69778=CARTESIAN_POINT('Ctrl Pts',(28.2783743476177,19.2542595960153,38.8081419265169));
#69779=CARTESIAN_POINT('Ctrl Pts',(28.2222314025319,19.3134386866003,38.8039103004865));
#69780=CARTESIAN_POINT('Ctrl Pts',(28.1662690618457,19.3724274059088,38.799692287035));
#69781=CARTESIAN_POINT('Ctrl Pts',(28.1132045287195,19.4342480368791,38.7954742735836));
#69782=CARTESIAN_POINT('Ctrl Pts',(28.0633302440097,19.4985805029132,38.7912562601321));
#69783=CARTESIAN_POINT('Ctrl Pts',(28.0134723706798,19.5628918000313,38.7870396346389));
#69784=CARTESIAN_POINT('Ctrl Pts',(27.9668029456149,19.6297129237595,38.7828230091456));
#69785=CARTESIAN_POINT('Ctrl Pts',(27.9235740740609,19.6986908038103,38.7786063836524));
#69786=CARTESIAN_POINT('Ctrl Pts',(27.880346192013,19.7676671049618,38.7743898546774));
#69787=CARTESIAN_POINT('Ctrl Pts',(27.8405589527655,19.8387996698277,38.7701733257024));
#69788=CARTESIAN_POINT('Ctrl Pts',(27.8044202903554,19.9117077650754,38.7659567967275));
#69789=CARTESIAN_POINT('Ctrl Pts',(27.7680585785642,19.9850658522277,38.761714243154));
#69790=CARTESIAN_POINT('Ctrl Pts',(27.735390861715,20.0602210428876,38.7574716895806));
#69791=CARTESIAN_POINT('Ctrl Pts',(27.7065804955838,20.1367635163158,38.7532291360071));
#69792=CARTESIAN_POINT('Ctrl Pts',(27.6779052850677,20.2129469125621,38.7490064851637));
#69793=CARTESIAN_POINT('Ctrl Pts',(27.6530514045033,20.2905041411395,38.7447838343202));
#69794=CARTESIAN_POINT('Ctrl Pts',(27.6321297560303,20.369016040043,38.7405611834768));
#69795=CARTESIAN_POINT('Ctrl Pts',(27.611060191733,20.4480830172075,38.7363086785383));
#69796=CARTESIAN_POINT('Ctrl Pts',(27.5939787781578,20.5281177484648,38.7320561735999));
#69797=CARTESIAN_POINT('Ctrl Pts',(27.5809460876128,20.6086837353699,38.7278036686615));
#69798=CARTESIAN_POINT('Ctrl Pts',(27.5679133970677,20.689249722275,38.723551163723));
#69799=CARTESIAN_POINT('Ctrl Pts',(27.5589294189629,20.7703464861984,38.7192986587846));
#69800=CARTESIAN_POINT('Ctrl Pts',(27.5540014768481,20.8515362847741,38.7150461538462));
#69801=CARTESIAN_POINT('Ctrl Pts',(27.5510199323564,20.9006584114312,38.7124732679681));
#69802=CARTESIAN_POINT('Ctrl Pts',(27.5495179883392,20.949871249837,38.7099003820901));
#69803=CARTESIAN_POINT('Ctrl Pts',(27.549500160603,20.9991128049331,38.7073274962121));
#69804=CARTESIAN_POINT('',(27.5495005462907,20.99836373272,37.907327496241));
#69805=CARTESIAN_POINT('Ctrl Pts',(27.5495001606026,20.9991128058326,38.7073274961651));
#69806=CARTESIAN_POINT('Ctrl Pts',(27.5494711067375,21.0793618588582,38.7031344593114));
#69807=CARTESIAN_POINT('Ctrl Pts',(27.5533883013094,21.1597704716766,38.6989414224577));
#69808=CARTESIAN_POINT('Ctrl Pts',(27.5612725675742,21.2399140686456,38.6947483856039));
#69809=CARTESIAN_POINT('Ctrl Pts',(27.5691459480749,21.3199470117787,38.6905611380538));
#69810=CARTESIAN_POINT('Ctrl Pts',(27.5809754805987,21.3997151977181,38.6863738905036));
#69811=CARTESIAN_POINT('Ctrl Pts',(27.5967299704161,21.478793708087,38.6821866429535));
#69812=CARTESIAN_POINT('Ctrl Pts',(27.6124677386434,21.5577882856565,38.678003839688));
#69813=CARTESIAN_POINT('Ctrl Pts',(27.6321220969125,21.6360941791158,38.6738210364225));
#69814=CARTESIAN_POINT('Ctrl Pts',(27.6556101820904,21.7132928092179,38.6696382331569));
#69815=CARTESIAN_POINT('Ctrl Pts',(27.6790850761053,21.7904480837333,38.665457778999));
#69816=CARTESIAN_POINT('Ctrl Pts',(27.7063892872424,21.8664968763102,38.6612773248411));
#69817=CARTESIAN_POINT('Ctrl Pts',(27.7373894349208,21.941033304826,38.6570968706832));
#69818=CARTESIAN_POINT('Ctrl Pts',(27.7683820864734,22.0155517097361,38.6529174273983));
#69819=CARTESIAN_POINT('Ctrl Pts',(27.8030687180136,22.088558039289,38.6487379841133));
#69820=CARTESIAN_POINT('Ctrl Pts',(27.8412674537946,22.1596654879549,38.6445585408283));
#69821=CARTESIAN_POINT('Ctrl Pts',(27.8794691687436,22.2307784823811,38.6403787715833));
#69822=CARTESIAN_POINT('Ctrl Pts',(27.9211833053754,22.2999918854674,38.6361990023382));
#69823=CARTESIAN_POINT('Ctrl Pts',(27.9661823386697,22.3669440260892,38.6320192330931));
#69824=CARTESIAN_POINT('Ctrl Pts',(28.0112278203437,22.4339652752721,38.6278351494552));
#69825=CARTESIAN_POINT('Ctrl Pts',(28.059564700567,22.4987202098391,38.6236510658172));
#69826=CARTESIAN_POINT('Ctrl Pts',(28.1109228983345,22.5608773026612,38.6194669821793));
#69827=CARTESIAN_POINT('Ctrl Pts',(28.1623107882717,22.6230703309139,38.61528047956));
#69828=CARTESIAN_POINT('Ctrl Pts',(28.2167231511567,22.6826621798126,38.6110939769407));
#69829=CARTESIAN_POINT('Ctrl Pts',(28.2738522415331,22.7393574002889,38.6069074743215));
#69830=CARTESIAN_POINT('Ctrl Pts',(28.3310758382662,22.7961464093884,38.6027140461393));
#69831=CARTESIAN_POINT('Ctrl Pts',(28.3910247788405,22.8500289114947,38.5985206179571));
#69832=CARTESIAN_POINT('Ctrl Pts',(28.453357875113,22.9007494278639,38.5943271897749));
#69833=CARTESIAN_POINT('Ctrl Pts',(28.484136276635,22.9257938506756,38.5922565880551));
#69834=CARTESIAN_POINT('Ctrl Pts',(28.5154955090315,22.9500680076986,38.5901859863352));
#69835=CARTESIAN_POINT('Ctrl Pts',(28.5473920865824,22.9735451603337,38.5881153846154));
#69836=CARTESIAN_POINT('Ctrl Pts',(28.6125785711537,23.0215250116385,38.5838837316473));
#69837=CARTESIAN_POINT('Ctrl Pts',(28.6802666916773,23.0663614446907,38.5796520786793));
#69838=CARTESIAN_POINT('Ctrl Pts',(28.7501206589528,23.107783642318,38.5754204257113));
#69839=CARTESIAN_POINT('Ctrl Pts',(28.8198746236198,23.1491465401236,38.5711948307576));
#69840=CARTESIAN_POINT('Ctrl Pts',(28.8917878804878,23.187104675046,38.5669692358039));
#69841=CARTESIAN_POINT('Ctrl Pts',(28.9654937100691,23.2214290414266,38.5627436408502));
#69842=CARTESIAN_POINT('Ctrl Pts',(29.0393047385103,23.2558023982904,38.5585120147891));
#69843=CARTESIAN_POINT('Ctrl Pts',(29.114913072776,23.2865313416713,38.554280388728));
#69844=CARTESIAN_POINT('Ctrl Pts',(29.1919235115136,23.3134309237052,38.550048762667));
#69845=CARTESIAN_POINT('Ctrl Pts',(29.2686862151446,23.3402439723946,38.5458307493362));
#69846=CARTESIAN_POINT('Ctrl Pts',(29.3468415814648,23.3632520899016,38.5416127360055));
#69847=CARTESIAN_POINT('Ctrl Pts',(29.4259776948736,23.3823200127643,38.5373947226747));
#69848=CARTESIAN_POINT('Ctrl Pts',(29.5050877681678,23.4013816612363,38.5331780973013));
#69849=CARTESIAN_POINT('Ctrl Pts',(29.5851774961455,23.4165055810472,38.5289614719279));
#69850=CARTESIAN_POINT('Ctrl Pts',(29.6658214365974,23.4276068334395,38.5247448465545));
#69851=CARTESIAN_POINT('Ctrl Pts',(29.7464635311333,23.4387078317274,38.5205283176984));
#69852=CARTESIAN_POINT('Ctrl Pts',(29.8276593523034,23.4457862834033,38.5163117888423));
#69853=CARTESIAN_POINT('Ctrl Pts',(29.9089763666407,23.4488088835534,38.5120952599862));
#69854=CARTESIAN_POINT('Ctrl Pts',(29.9907952781647,23.4518501395103,38.5078527062694));
#69855=CARTESIAN_POINT('Ctrl Pts',(30.0727364091553,23.4507852726604,38.5036101525526));
#69856=CARTESIAN_POINT('Ctrl Pts',(30.1543590031072,23.4456335678429,38.4993675988358));
#69857=CARTESIAN_POINT('Ctrl Pts',(30.235598682978,23.4405060310923,38.4951449481076));
#69858=CARTESIAN_POINT('Ctrl Pts',(30.316522348417,23.4313300241304,38.4909222973795));
#69859=CARTESIAN_POINT('Ctrl Pts',(30.3967022585897,23.4181764964596,38.4866996466513));
#69860=CARTESIAN_POINT('Ctrl Pts',(30.4774490472264,23.404929972282,38.4824471414402));
#69861=CARTESIAN_POINT('Ctrl Pts',(30.5574410550114,23.3876495660561,38.4781946362291));
#69862=CARTESIAN_POINT('Ctrl Pts',(30.6362553943134,23.3664592375968,38.473942131018));
#69863=CARTESIAN_POINT('Ctrl Pts',(30.7150697336155,23.3452689091375,38.4696896258069));
#69864=CARTESIAN_POINT('Ctrl Pts',(30.7927059723433,23.3201688645899,38.4654371205957));
#69865=CARTESIAN_POINT('Ctrl Pts',(30.8687619484462,23.291332129337,38.4611846153846));
#69866=CARTESIAN_POINT('Ctrl Pts',(30.9444449854619,23.2626367944878,38.456952962255));
#69867=CARTESIAN_POINT('Ctrl Pts',(31.0188463182413,23.2301340330647,38.4527213091254));
#69868=CARTESIAN_POINT('Ctrl Pts',(31.0915562155446,23.1939588141772,38.4484896559958));
#69869=CARTESIAN_POINT('Ctrl Pts',(31.1641620216863,23.1578353835702,38.4442640608817));
#69870=CARTESIAN_POINT('Ctrl Pts',(31.2350807889251,23.1180501426292,38.4400384657677));
#69871=CARTESIAN_POINT('Ctrl Pts',(31.3039211072694,23.0747867350688,38.4358128706536));
#69872=CARTESIAN_POINT('Ctrl Pts',(31.3728596767549,23.031461580566,38.4315812446328));
#69873=CARTESIAN_POINT('Ctrl Pts',(31.4397134275358,22.9846485057952,38.427349618612));
#69874=CARTESIAN_POINT('Ctrl Pts',(31.5041124865869,22.9345789923633,38.4231179925912));
#69875=CARTESIAN_POINT('Ctrl Pts',(31.5683043831035,22.8846705453733,38.4188999791042));
#69876=CARTESIAN_POINT('Ctrl Pts',(31.6300569781506,22.8315268517084,38.4146819656172));
#69877=CARTESIAN_POINT('Ctrl Pts',(31.6890330493998,22.7754204031821,38.4104639521303));
#69878=CARTESIAN_POINT('Ctrl Pts',(31.7479897142665,22.719332416774,38.4062473266025));
#69879=CARTESIAN_POINT('Ctrl Pts',(31.8041713332021,22.6602839316853,38.4020307010748));
#69880=CARTESIAN_POINT('Ctrl Pts',(31.857275602916,22.5985861205494,38.3978140755471));
#69881=CARTESIAN_POINT('Ctrl Pts',(31.9103786570626,22.5368897216885,38.3935975465388));
#69882=CARTESIAN_POINT('Ctrl Pts',(31.9604041996819,22.4725444703764,38.3893810175304));
#69883=CARTESIAN_POINT('Ctrl Pts',(32.0070894396749,22.4058955263979,38.3851644885221));
#69884=CARTESIAN_POINT('Ctrl Pts',(32.0540628221351,22.3388352234724,38.3809219349914));
#69885=CARTESIAN_POINT('Ctrl Pts',(32.0976542419384,22.2694430741771,38.3766793814607));
#69886=CARTESIAN_POINT('Ctrl Pts',(32.1376406085571,22.1980996947865,38.37243682793));
#69887=CARTESIAN_POINT('Ctrl Pts',(32.1774393912293,22.1270910012851,38.3682141770562));
#69888=CARTESIAN_POINT('Ctrl Pts',(32.2136667108561,22.0541497886899,38.3639915261824));
#69889=CARTESIAN_POINT('Ctrl Pts',(32.2461499309449,21.9796737914818,38.3597688753086));
#69890=CARTESIAN_POINT('Ctrl Pts',(32.2788628061968,21.9046712517313,38.3555163704495));
#69891=CARTESIAN_POINT('Ctrl Pts',(32.3077782648604,21.8281125885284,38.3512638655903));
#69892=CARTESIAN_POINT('Ctrl Pts',(32.3327708232583,21.7504202397021,38.3470113607312));
#69893=CARTESIAN_POINT('Ctrl Pts',(32.3577633816563,21.6727278908758,38.3427588558721));
#69894=CARTESIAN_POINT('Ctrl Pts',(32.3788329783271,21.593902331211,38.338506351013));
#69895=CARTESIAN_POINT('Ctrl Pts',(32.3959065866391,21.5143752308377,38.3342538461538));
#69896=CARTESIAN_POINT('Ctrl Pts',(32.4128964777229,21.4352380766486,38.3300221926527));
#69897=CARTESIAN_POINT('Ctrl Pts',(32.4259930619774,21.3551102505546,38.3257905391517));
#69898=CARTESIAN_POINT('Ctrl Pts',(32.4350872439232,21.2744091188031,38.3215588856506));
#69899=CARTESIAN_POINT('Ctrl Pts',(32.4441684066871,21.1938235183582,38.3173332901619));
#69900=CARTESIAN_POINT('Ctrl Pts',(32.4492584954736,21.1126667003274,38.3131076946732));
#69901=CARTESIAN_POINT('Ctrl Pts',(32.4502992382381,21.0313670701525,38.3088820991846));
#69902=CARTESIAN_POINT('Ctrl Pts',(32.4513414662691,20.9499514155135,38.304650473257));
#69903=CARTESIAN_POINT('Ctrl Pts',(32.4483226999183,20.8683930028803,38.3004188473294));
#69904=CARTESIAN_POINT('Ctrl Pts',(32.4412365337121,20.7871281219388,38.2961872214019));
#69905=CARTESIAN_POINT('Ctrl Pts',(32.4341731618949,20.7061246493881,38.2919692075354));
#69906=CARTESIAN_POINT('Ctrl Pts',(32.4230685416578,20.6254132889681,38.2877511936689));
#69907=CARTESIAN_POINT('Ctrl Pts',(32.4079684338373,20.5454251748686,38.2835331798025));
#69908=CARTESIAN_POINT('Ctrl Pts',(32.3928732947817,20.4654633812526,38.2793165538943));
#69909=CARTESIAN_POINT('Ctrl Pts',(32.3737853652095,20.3862248177235,38.2750999279861));
#69910=CARTESIAN_POINT('Ctrl Pts',(32.3508018475349,20.3081322932622,38.2708833020779));
#69911=CARTESIAN_POINT('Ctrl Pts',(32.327818855955,20.2300415563456,38.2666667726886));
#69912=CARTESIAN_POINT('Ctrl Pts',(32.3009405858815,20.1530972519152,38.2624502432993));
#69913=CARTESIAN_POINT('Ctrl Pts',(32.2703142331859,20.077707458236,38.2582337139101));
#69914=CARTESIAN_POINT('Ctrl Pts',(32.2394988599176,20.0018523717381,38.2539911608278));
#69915=CARTESIAN_POINT('Ctrl Pts',(32.2048891449142,19.9275714968123,38.2497486077456));
#69916=CARTESIAN_POINT('Ctrl Pts',(32.1666836136029,19.8552588202809,38.2455060546633));
#69917=CARTESIAN_POINT('Ctrl Pts',(32.1286573045634,19.7832853627505,38.2412834034114));
#69918=CARTESIAN_POINT('Ctrl Pts',(32.087069127314,19.7132620536026,38.2370607521594));
#69919=CARTESIAN_POINT('Ctrl Pts',(32.0421593746451,19.6455498021155,38.2328381009075));
#69920=CARTESIAN_POINT('Ctrl Pts',(31.9969321249024,19.5773588474421,38.2285855969101));
#69921=CARTESIAN_POINT('Ctrl Pts',(31.9483364356444,19.5115121398233,38.2243330929127));
#69922=CARTESIAN_POINT('Ctrl Pts',(31.8966589444221,19.4483444007952,38.2200805889153));
#69923=CARTESIAN_POINT('Ctrl Pts',(31.8449814531997,19.385176661767,38.2158280849179));
#69924=CARTESIAN_POINT('Ctrl Pts',(31.7902225253688,19.3246882007041,38.2115755809205));
#69925=CARTESIAN_POINT('Ctrl Pts',(31.7327050305537,19.2671746980455,38.2073230769231));
#69926=CARTESIAN_POINT('Ctrl Pts',(31.6754695701505,19.2099432102233,38.203091424885));
#69927=CARTESIAN_POINT('Ctrl Pts',(31.615288477062,19.1554434792139,38.1988597728469));
#69928=CARTESIAN_POINT('Ctrl Pts',(31.5524530267996,19.1039937105641,38.1946281208089));
#69929=CARTESIAN_POINT('Ctrl Pts',(31.4897075314897,19.0526175971753,38.1904025267852));
#69930=CARTESIAN_POINT('Ctrl Pts',(31.4243155826979,19.0042830662424,38.1861769327614));
#69931=CARTESIAN_POINT('Ctrl Pts',(31.356605318602,18.9592716350428,38.1819513387377));
#69932=CARTESIAN_POINT('Ctrl Pts',(31.2887983943488,18.9141959475288,38.1777197124441));
#69933=CARTESIAN_POINT('Ctrl Pts',(31.2186668743795,18.8724531743048,38.1734880861506));
#69934=CARTESIAN_POINT('Ctrl Pts',(31.1465736768083,18.8342855558384,38.169256459857));
#69935=CARTESIAN_POINT('Ctrl Pts',(31.0747124157323,18.7962407293128,38.1650384474495));
#69936=CARTESIAN_POINT('Ctrl Pts',(31.0009024841709,18.7617483218529,38.1608204350419));
#69937=CARTESIAN_POINT('Ctrl Pts',(30.925530791204,18.7310039655096,38.1566024226343));
#69938=CARTESIAN_POINT('Ctrl Pts',(30.8501838995748,18.7002697257118,38.1523857981795));
#69939=CARTESIAN_POINT('Ctrl Pts',(30.7732766971362,18.6732812632354,38.1481691737247));
#69940=CARTESIAN_POINT('Ctrl Pts',(30.6952170290165,18.6501864898325,38.1439525492699));
#69941=CARTESIAN_POINT('Ctrl Pts',(30.6171591475524,18.6270922450306,38.1397360213266));
#69942=CARTESIAN_POINT('Ctrl Pts',(30.5379492988818,18.6078916428931,38.1355194933833));
#69943=CARTESIAN_POINT('Ctrl Pts',(30.45801009866,18.5926826134626,38.13130296544));
#69944=CARTESIAN_POINT('Ctrl Pts',(30.3775774670841,18.5773797050345,38.1270604106277));
#69945=CARTESIAN_POINT('Ctrl Pts',(30.2964069135791,18.5661179192298,38.1228178558154));
#69946=CARTESIAN_POINT('Ctrl Pts',(30.2149370875309,18.5589444294724,38.1185753010031));
#69947=CARTESIAN_POINT('Ctrl Pts',(30.1338494969048,18.5518045958797,38.1143526511643));
#69948=CARTESIAN_POINT('Ctrl Pts',(30.0524659061688,18.5487147433998,38.1101300013255));
#69949=CARTESIAN_POINT('Ctrl Pts',(29.9712198606749,18.5496690114231,38.1059073514867));
#69950=CARTESIAN_POINT('Ctrl Pts',(29.8893993416474,18.5506300268729,38.1016548441876));
#69951=CARTESIAN_POINT('Ctrl Pts',(29.8077187981425,18.5556925467721,38.0974023368886));
#69952=CARTESIAN_POINT('Ctrl Pts',(29.7266149449956,18.5647975727467,38.0931498295895));
#69953=CARTESIAN_POINT('Ctrl Pts',(29.6455110918486,18.5739025987214,38.0888973222905));
#69954=CARTESIAN_POINT('Ctrl Pts',(29.5649843872258,18.5870499919039,38.0846448149914));
#69955=CARTESIAN_POINT('Ctrl Pts',(29.4854584295428,18.6041291307186,38.0803923076923));
#69956=CARTESIAN_POINT('Ctrl Pts',(29.4063224535612,18.6211245163561,38.0761606539621));
#69957=CARTESIAN_POINT('Ctrl Pts',(29.3278814250196,18.6420767085657,38.0719290002319));
#69958=CARTESIAN_POINT('Ctrl Pts',(29.2505607056619,18.6669138476897,38.0676973465016));
#69959=CARTESIAN_POINT('Ctrl Pts',(29.1733506784166,18.691715430039,38.0634717507943));
#69960=CARTESIAN_POINT('Ctrl Pts',(29.0972582138182,18.7203907723405,38.059246155087));
#69961=CARTESIAN_POINT('Ctrl Pts',(29.022697875521,18.7528171397305,38.0550205593797));
#69962=CARTESIAN_POINT('Ctrl Pts',(28.9480311354006,18.7852897813823,38.0507889335081));
#69963=CARTESIAN_POINT('Ctrl Pts',(28.8749013526776,18.8215240469643,38.0465573076365));
#69964=CARTESIAN_POINT('Ctrl Pts',(28.8037089877696,18.8613466704356,38.0423256817649));
#69965=CARTESIAN_POINT('Ctrl Pts',(28.7327456263722,18.9010411970164,38.0381076677066));
#69966=CARTESIAN_POINT('Ctrl Pts',(28.6637076528252,18.9443008184763,38.0338896536484));
#69967=CARTESIAN_POINT('Ctrl Pts',(28.5969694111176,18.9909068173277,38.0296716395901));
#69968=CARTESIAN_POINT('Ctrl Pts',(28.5302531301217,19.0374974801307,38.0254550135005));
#69969=CARTESIAN_POINT('Ctrl Pts',(28.4658354589435,19.0874320676519,38.0212383874109));
#69970=CARTESIAN_POINT('Ctrl Pts',(28.4040620322853,19.1404483730731,38.0170217613214));
#69971=CARTESIAN_POINT('Ctrl Pts',(28.3422900197819,19.1934634648128,38.0128052317613));
#69972=CARTESIAN_POINT('Ctrl Pts',(28.2831624834224,19.2495598306128,38.0085887022013));
#69973=CARTESIAN_POINT('Ctrl Pts',(28.2269911022462,19.3084357244001,38.0043721726413));
#69974=CARTESIAN_POINT('Ctrl Pts',(28.1704730463874,19.3676749843957,38.000129619793));
#69975=CARTESIAN_POINT('Ctrl Pts',(28.1169480997675,19.4297278655877,37.9958870669447));
#69976=CARTESIAN_POINT('Ctrl Pts',(28.0666940201099,19.4942516019862,37.9916445140964));
#69977=CARTESIAN_POINT('Ctrl Pts',(28.0166756780481,19.5584726630478,37.9874218627011));
#69978=CARTESIAN_POINT('Ctrl Pts',(27.9698978081486,19.6251410341167,37.9831992113059));
#69979=CARTESIAN_POINT('Ctrl Pts',(27.9265908599889,19.6938894426128,37.9789765599106));
#69980=CARTESIAN_POINT('Ctrl Pts',(27.8829777518662,19.7631238703528,37.9747240563358));
#69981=CARTESIAN_POINT('Ctrl Pts',(27.8428850670919,19.8344674429904,37.9704715527609));
#69982=CARTESIAN_POINT('Ctrl Pts',(27.806500350291,19.9075213792816,37.9662190491861));
#69983=CARTESIAN_POINT('Ctrl Pts',(27.7701156334902,19.9805753155728,37.9619665456112));
#69984=CARTESIAN_POINT('Ctrl Pts',(27.7374390167793,20.0553391553627,37.9577140420364));
#69985=CARTESIAN_POINT('Ctrl Pts',(27.7086075710818,20.1313971064427,37.9534615384615));
#69986=CARTESIAN_POINT('Ctrl Pts',(27.6758375656571,20.217845059682,37.9486281157231));
#69987=CARTESIAN_POINT('Ctrl Pts',(27.6479320020787,20.3062327244513,37.9437946929847));
#69988=CARTESIAN_POINT('Ctrl Pts',(27.6250935584466,20.3960383755005,37.9389612702462));
#69989=CARTESIAN_POINT('Ctrl Pts',(27.6023501396508,20.4854703685444,37.9341479581253));
#69990=CARTESIAN_POINT('Ctrl Pts',(27.5846318881965,20.5763083907836,37.9293346460044));
#69991=CARTESIAN_POINT('Ctrl Pts',(27.5720921426097,20.6680155334625,37.9245213338835));
#69992=CARTESIAN_POINT('Ctrl Pts',(27.559640925248,20.7590752411098,37.9197420028331));
#69993=CARTESIAN_POINT('Ctrl Pts',(27.5522954629206,20.8509916422353,37.9149626717827));
#69994=CARTESIAN_POINT('Ctrl Pts',(27.5501578939433,20.943220554848,37.9101833407323));
#69995=CARTESIAN_POINT('Ctrl Pts',(27.5497321325049,20.9615907290592,37.9092313925685));
#69996=CARTESIAN_POINT('Ctrl Pts',(27.5495128261339,20.9799732476796,37.9082794444048));
#69997=CARTESIAN_POINT('Ctrl Pts',(27.5495005462907,20.99836373272,37.907327496241));
#69998=CARTESIAN_POINT('',(27.5495007214883,21.0018804290879,37.1073274961852));
#69999=CARTESIAN_POINT('Ctrl Pts',(27.5495005462904,20.9983637332799,37.907327496212));
#70000=CARTESIAN_POINT('Ctrl Pts',(27.5494458819207,21.0802299757675,37.9030898472844));
#70001=CARTESIAN_POINT('Ctrl Pts',(27.5534980267667,21.1621217478089,37.8988521983568));
#70002=CARTESIAN_POINT('Ctrl Pts',(27.5616380823687,21.2436009208633,37.8946145494291));
#70003=CARTESIAN_POINT('Ctrl Pts',(27.569778459134,21.325083308653,37.8903767333064));
#70004=CARTESIAN_POINT('Ctrl Pts',(27.5820070209178,21.4061526093791,37.8861389171837));
#70005=CARTESIAN_POINT('Ctrl Pts',(27.5982530209687,21.4863760877286,37.8819011010609));
#70006=CARTESIAN_POINT('Ctrl Pts',(27.6145044466303,21.5666263579873,37.8776618696519));
#70007=CARTESIAN_POINT('Ctrl Pts',(27.6347758841636,21.6460297961296,37.8734226382429));
#70008=CARTESIAN_POINT('Ctrl Pts',(27.6589458233662,21.7241654452301,37.869183406834));
#70009=CARTESIAN_POINT('Ctrl Pts',(27.6831472745969,21.8024029652023,37.8649386484446));
#70010=CARTESIAN_POINT('Ctrl Pts',(27.711257234633,21.8793689596193,37.8606938900552));
#70011=CARTESIAN_POINT('Ctrl Pts',(27.7431049575806,21.9546596343739,37.8564491316659));
#70012=CARTESIAN_POINT('Ctrl Pts',(27.7749767907757,22.0300073077653,37.8522011597917));
#70013=CARTESIAN_POINT('Ctrl Pts',(27.8105918197602,22.1036767254342,37.8479531879175));
#70014=CARTESIAN_POINT('Ctrl Pts',(27.8497330746425,22.175288219848,37.8437052160432));
#70015=CARTESIAN_POINT('Ctrl Pts',(27.8889430848691,22.2470255066765,37.8394497822016));
#70016=CARTESIAN_POINT('Ctrl Pts',(27.9316914436912,22.3166972664765,37.83519434836));
#70017=CARTESIAN_POINT('Ctrl Pts',(27.9777178442663,22.3839527205079,37.8309389145183));
#70018=CARTESIAN_POINT('Ctrl Pts',(27.9936105490094,22.4071757199153,37.8294695327558));
#70019=CARTESIAN_POINT('Ctrl Pts',(28.0098937420718,22.4301109208238,37.8280001509933));
#70020=CARTESIAN_POINT('Ctrl Pts',(28.026555639737,22.4527448526656,37.8265307692308));
#70021=CARTESIAN_POINT('Ctrl Pts',(28.0745399183696,22.5179278776648,37.8222991249531));
#70022=CARTESIAN_POINT('Ctrl Pts',(28.125846908268,22.5808528674656,37.8180674806755));
#70023=CARTESIAN_POINT('Ctrl Pts',(28.1802364650657,22.6411614566895,37.8138358363979));
#70024=CARTESIAN_POINT('Ctrl Pts',(28.2345481578057,22.7013837081725,37.8096102501397));
#70025=CARTESIAN_POINT('Ctrl Pts',(28.2919333441418,22.7589966559853,37.8053846638815));
#70026=CARTESIAN_POINT('Ctrl Pts',(28.3521099219312,22.8136726663327,37.8011590776233));
#70027=CARTESIAN_POINT('Ctrl Pts',(28.4123725435083,22.8684268554533,37.796927449389));
#70028=CARTESIAN_POINT('Ctrl Pts',(28.4754342534545,22.9202353343615,37.7926958211547));
#70029=CARTESIAN_POINT('Ctrl Pts',(28.5409726596603,22.9688040710394,37.7884641929204));
#70030=CARTESIAN_POINT('Ctrl Pts',(28.606300067735,23.0172164427205,37.7842461882345));
#70031=CARTESIAN_POINT('Ctrl Pts',(28.6740878845252,23.0624096096378,37.7800281835486));
#70032=CARTESIAN_POINT('Ctrl Pts',(28.7439829970004,23.1041320153868,37.7758101788627));
#70033=CARTESIAN_POINT('Ctrl Pts',(28.8138551107407,23.1458406925286,37.771593562096));
#70034=CARTESIAN_POINT('Ctrl Pts',(28.8858327443596,23.1840806384094,37.7673769453293));
#70035=CARTESIAN_POINT('Ctrl Pts',(28.9595349148795,23.2186443285586,37.7631603285627));
#70036=CARTESIAN_POINT('Ctrl Pts',(29.0332353992417,23.2532072279599,37.7589438082637));
#70037=CARTESIAN_POINT('Ctrl Pts',(29.108659920751,23.284093842521,37.7547272879648));
#70038=CARTESIAN_POINT('Ctrl Pts',(29.1854053821451,23.3111438420319,37.7505107676658));
#70039=CARTESIAN_POINT('Ctrl Pts',(29.2626248679896,23.3383609180176,37.7462682036937));
#70040=CARTESIAN_POINT('Ctrl Pts',(29.3411812239746,23.3616936490656,37.7420256397215));
#70041=CARTESIAN_POINT('Ctrl Pts',(29.4206478681953,23.3810294742765,37.7377830757494));
#70042=CARTESIAN_POINT('Ctrl Pts',(29.4997413649096,23.4002745052299,37.7335604333705));
#70043=CARTESIAN_POINT('Ctrl Pts',(29.5797361492946,23.4155600496186,37.7293377909916));
#70044=CARTESIAN_POINT('Ctrl Pts',(29.6602027203592,23.4268267467515,37.7251151486128));
#70045=CARTESIAN_POINT('Ctrl Pts',(29.7412387295238,23.4381731749644,37.720862623844));
#70046=CARTESIAN_POINT('Ctrl Pts',(29.822752752235,23.4454436107238,37.7166100990752));
#70047=CARTESIAN_POINT('Ctrl Pts',(29.9043041605924,23.4486307513221,37.7123575743064));
#70048=CARTESIAN_POINT('Ctrl Pts',(29.9858555689497,23.4518178919203,37.7081050495376));
#70049=CARTESIAN_POINT('Ctrl Pts',(30.0674438891054,23.4509218057965,37.7038525247687));
#70050=CARTESIAN_POINT('Ctrl Pts',(30.1486337027279,23.4459881995654,37.6995999999999));
#70051=CARTESIAN_POINT('Ctrl Pts',(30.2294251782622,23.4410787988743,37.6953683392104));
#70052=CARTESIAN_POINT('Ctrl Pts',(30.31012424687,23.4321530785102,37.6911366784209));
#70053=CARTESIAN_POINT('Ctrl Pts',(30.3902995772568,23.4192181567592,37.6869050176313));
#70054=CARTESIAN_POINT('Ctrl Pts',(30.4703601280599,23.4063017527358,37.682679414918));
#70055=CARTESIAN_POINT('Ctrl Pts',(30.549897974771,23.3893876201113,37.6784538122047));
#70056=CARTESIAN_POINT('Ctrl Pts',(30.6284848157943,23.3685347973623,37.6742282094914));
#70057=CARTESIAN_POINT('Ctrl Pts',(30.7071836415084,23.3476522597541,37.669996585378));
#70058=CARTESIAN_POINT('Ctrl Pts',(30.7849282821077,23.3228198438784,37.6657649612645));
#70059=CARTESIAN_POINT('Ctrl Pts',(30.8612967875742,23.2941486642575,37.6615333371511));
#70060=CARTESIAN_POINT('Ctrl Pts',(30.9374197943529,23.2655696526963,37.6573153162654));
#70061=CARTESIAN_POINT('Ctrl Pts',(31.0121750576729,23.2331766685513,37.6530972953796));
#70062=CARTESIAN_POINT('Ctrl Pts',(31.0851596140347,23.19712968713,37.6488792744939));
#70063=CARTESIAN_POINT('Ctrl Pts',(31.158120152912,23.1610945679144,37.6446626416586));
#70064=CARTESIAN_POINT('Ctrl Pts',(31.2293107255803,23.1214080450065,37.6404460088234));
#70065=CARTESIAN_POINT('Ctrl Pts',(31.2983502159259,23.0782774037181,37.6362293759882));
#70066=CARTESIAN_POINT('Ctrl Pts',(31.3673881242992,23.035147750726,37.632012839773));
#70067=CARTESIAN_POINT('Ctrl Pts',(31.4342746547473,22.988574383489,37.6277963035577));
#70068=CARTESIAN_POINT('Ctrl Pts',(31.4986563189566,22.9388087805793,37.6235797673425));
#70069=CARTESIAN_POINT('Ctrl Pts',(31.5634351030713,22.8887362127633,37.6193372226281));
#70070=CARTESIAN_POINT('Ctrl Pts',(31.6256776279625,22.8354321721218,37.6150946779136));
#70071=CARTESIAN_POINT('Ctrl Pts',(31.6850577799362,22.7791937860381,37.6108521331992));
#70072=CARTESIAN_POINT('Ctrl Pts',(31.7441595871266,22.723219017693,37.606629475436));
#70073=CARTESIAN_POINT('Ctrl Pts',(31.8004255129353,22.6643377295476,37.6024068176729));
#70074=CARTESIAN_POINT('Ctrl Pts',(31.8535725280332,22.6028783900598,37.5981841599097));
#70075=CARTESIAN_POINT('Ctrl Pts',(31.9070949934372,22.5409848789109,37.5939316717196));
#70076=CARTESIAN_POINT('Ctrl Pts',(31.9574540155029,22.4764771268603,37.5896791835296));
#70077=CARTESIAN_POINT('Ctrl Pts',(32.0044042507991,22.4097211956193,37.5854266953395));
#70078=CARTESIAN_POINT('Ctrl Pts',(32.0513544860953,22.3429652643783,37.5811742071494));
#70079=CARTESIAN_POINT('Ctrl Pts',(32.0948957348547,22.2739615890068,37.5769217189593));
#70080=CARTESIAN_POINT('Ctrl Pts',(32.1348299965297,22.2031006341603,37.5726692307693));
#70081=CARTESIAN_POINT('Ctrl Pts',(32.1745687764439,22.1325865499868,37.5684375588869));
#70082=CARTESIAN_POINT('Ctrl Pts',(32.2108844632371,22.0599696106442,37.5642058870045));
#70083=CARTESIAN_POINT('Ctrl Pts',(32.2435488667623,21.9856159152781,37.5599742151221));
#70084=CARTESIAN_POINT('Ctrl Pts',(32.2761665094876,21.9113686611111,37.5557486010991));
#70085=CARTESIAN_POINT('Ctrl Pts',(32.3051430648768,21.835390010831,37.5515229870761));
#70086=CARTESIAN_POINT('Ctrl Pts',(32.3302955902779,21.7580717063256,37.5472973730531));
#70087=CARTESIAN_POINT('Ctrl Pts',(32.3554838734449,21.6806434832421,37.54306575174));
#70088=CARTESIAN_POINT('Ctrl Pts',(32.3768370303003,21.6018722109653,37.5388341304269));
#70089=CARTESIAN_POINT('Ctrl Pts',(32.3942193012643,21.5221725648228,37.5346025091138));
#70090=CARTESIAN_POINT('Ctrl Pts',(32.4115457538807,21.4427288520135,37.5303844764802));
#70091=CARTESIAN_POINT('Ctrl Pts',(32.4249266687656,21.362363170678,37.5261664438465));
#70092=CARTESIAN_POINT('Ctrl Pts',(32.4342776258916,21.2815007816753,37.5219484112129));
#70093=CARTESIAN_POINT('Ctrl Pts',(32.443625506153,21.2006649998545,37.5177317664923));
#70094=CARTESIAN_POINT('Ctrl Pts',(32.4489460086426,21.1193332963,37.5135151217717));
#70095=CARTESIAN_POINT('Ctrl Pts',(32.4502063051429,21.0379382687796,37.5092984770511));
#70096=CARTESIAN_POINT('Ctrl Pts',(32.4514665728008,20.9565451040173,37.5050819288301));
#70097=CARTESIAN_POINT('Ctrl Pts',(32.4486668131505,20.8750890829333,37.5008653806091));
#70098=CARTESIAN_POINT('Ctrl Pts',(32.4418263104952,20.7940035937858,37.4966488323881));
#70099=CARTESIAN_POINT('Ctrl Pts',(32.4349436561549,20.7124184498347,37.492406301484));
#70100=CARTESIAN_POINT('Ctrl Pts',(32.4239703140359,20.6312088953234,37.4881637705799));
#70101=CARTESIAN_POINT('Ctrl Pts',(32.4089787643902,20.5508101039462,37.4839212396757));
#70102=CARTESIAN_POINT('Ctrl Pts',(32.3940573961245,20.4707876911455,37.4796985697386));
#70103=CARTESIAN_POINT('Ctrl Pts',(32.375155521284,20.3915689103076,37.4754758998014));
#70104=CARTESIAN_POINT('Ctrl Pts',(32.3523953318783,20.3135697759006,37.4712532298643));
#70105=CARTESIAN_POINT('Ctrl Pts',(32.3294745665654,20.2350203481043,37.4670007684767));
#70106=CARTESIAN_POINT('Ctrl Pts',(32.3026409897418,20.1577082952858,37.462748307089));
#70107=CARTESIAN_POINT('Ctrl Pts',(32.2720688187676,20.082038381639,37.4584958457014));
#70108=CARTESIAN_POINT('Ctrl Pts',(32.2414966477935,20.0063684679922,37.4542433843137));
#70109=CARTESIAN_POINT('Ctrl Pts',(32.2071861395641,19.9323410974537,37.4499909229261));
#70110=CARTESIAN_POINT('Ctrl Pts',(32.1693577057091,19.8603345250994,37.4457384615384));
#70111=CARTESIAN_POINT('Ctrl Pts',(32.1317150165931,19.7886815185849,37.4415068805376));
#70112=CARTESIAN_POINT('Ctrl Pts',(32.0904480968269,19.7187614710945,37.4372752995367));
#70113=CARTESIAN_POINT('Ctrl Pts',(32.0457404954556,19.6509647613005,37.4330437185359));
#70114=CARTESIAN_POINT('Ctrl Pts',(32.0010968993028,19.5832651120306,37.4288181956383));
#70115=CARTESIAN_POINT('Ctrl Pts',(31.9530226584073,19.5176831478165,37.4245926727407));
#70116=CARTESIAN_POINT('Ctrl Pts',(31.9017474219834,19.4545851712308,37.4203671498431));
#70117=CARTESIAN_POINT('Ctrl Pts',(31.850397907355,19.3913957898125,37.4161355057791));
#70118=CARTESIAN_POINT('Ctrl Pts',(31.795838349081,19.3306980056242,37.4119038617151));
#70119=CARTESIAN_POINT('Ctrl Pts',(31.7383432947695,19.2728309754022,37.4076722176512));
#70120=CARTESIAN_POINT('Ctrl Pts',(31.6810344151152,19.2151513243322,37.4034542760681));
#70121=CARTESIAN_POINT('Ctrl Pts',(31.6208093379655,19.1602844654005,37.399236334485));
#70122=CARTESIAN_POINT('Ctrl Pts',(31.5579793517154,19.1085321600333,37.395018392902));
#70123=CARTESIAN_POINT('Ctrl Pts',(31.4951700362354,19.0567968809312,37.3908018390018));
#70124=CARTESIAN_POINT('Ctrl Pts',(31.4297578720651,19.0081744158085,37.3865852851017));
#70125=CARTESIAN_POINT('Ctrl Pts',(31.3620883185178,18.9629271828044,37.3823687312016));
#70126=CARTESIAN_POINT('Ctrl Pts',(31.2944203079969,18.9176809815445,37.3781522734489));
#70127=CARTESIAN_POINT('Ctrl Pts',(31.2244953974724,18.875810116809,37.3739358156962));
#70128=CARTESIAN_POINT('Ctrl Pts',(31.1526880019738,18.837533671914,37.3697193579435));
#70129=CARTESIAN_POINT('Ctrl Pts',(31.0804347362346,18.7990195589129,37.3654767191405));
#70130=CARTESIAN_POINT('Ctrl Pts',(31.0062759397416,18.7641448948097,37.3612340803376));
#70131=CARTESIAN_POINT('Ctrl Pts',(30.9306164637358,18.7330850815648,37.3569914415346));
#70132=CARTESIAN_POINT('Ctrl Pts',(30.8553146764312,18.7021721070882,37.3527688602848));
#70133=CARTESIAN_POINT('Ctrl Pts',(30.778526827634,18.6750380975155,37.348546279035));
#70134=CARTESIAN_POINT('Ctrl Pts',(30.7006686104187,18.6518062796324,37.3443236977852));
#70135=CARTESIAN_POINT('Ctrl Pts',(30.6222556453229,18.628408932635,37.3400710302056));
#70136=CARTESIAN_POINT('Ctrl Pts',(30.5427574637281,18.608969716988,37.335818362626));
#70137=CARTESIAN_POINT('Ctrl Pts',(30.4626086443515,18.5935620739002,37.3315656950465));
#70138=CARTESIAN_POINT('Ctrl Pts',(30.3824598249749,18.5781544308125,37.3273130274669));
#70139=CARTESIAN_POINT('Ctrl Pts',(30.3016608466984,18.5667783638181,37.3230603598873));
#70140=CARTESIAN_POINT('Ctrl Pts',(30.2206491032623,18.5594541136808,37.3188076923077));
#70141=CARTESIAN_POINT('Ctrl Pts',(30.140036127004,18.5521659159778,37.3145759577951));
#70142=CARTESIAN_POINT('Ctrl Pts',(30.0589109219233,18.5488624374712,37.3103442232825));
#70143=CARTESIAN_POINT('Ctrl Pts',(29.9777010025348,18.5496014600249,37.3061124887699));
#70144=CARTESIAN_POINT('Ctrl Pts',(29.896607348942,18.5503394245423,37.3018868127041));
#70145=CARTESIAN_POINT('Ctrl Pts',(29.8154296827866,18.5551083913551,37.2976611366383));
#70146=CARTESIAN_POINT('Ctrl Pts',(29.7346003255107,18.5639143564355,37.2934354605725));
#70147=CARTESIAN_POINT('Ctrl Pts',(29.6536575447593,18.5727326784516,37.2892038548436));
#70148=CARTESIAN_POINT('Ctrl Pts',(29.5730645196653,18.58559936205,37.2849722491146));
#70149=CARTESIAN_POINT('Ctrl Pts',(29.4932550900962,18.6024679676203,37.2807406433856));
#70150=CARTESIAN_POINT('Ctrl Pts',(29.413700518321,18.6192827061774,37.2765225505674));
#70151=CARTESIAN_POINT('Ctrl Pts',(29.3349250047692,18.6400737666865,37.2723044577492));
#70152=CARTESIAN_POINT('Ctrl Pts',(29.2573509894203,18.6647435478978,37.268086364931));
#70153=CARTESIAN_POINT('Ctrl Pts',(29.1798025140915,18.689405206973,37.2638696608532));
#70154=CARTESIAN_POINT('Ctrl Pts',(29.103455193983,18.7179429100095,37.2596529567755));
#70155=CARTESIAN_POINT('Ctrl Pts',(29.0287169800055,18.7502089996912,37.2554362526978));
#70156=CARTESIAN_POINT('Ctrl Pts',(28.953980492419,18.7824743440529,37.2512196460224));
#70157=CARTESIAN_POINT('Ctrl Pts',(28.8808534633331,18.8184677185667,37.2470030393471));
#70158=CARTESIAN_POINT('Ctrl Pts',(28.8097231716269,18.8579936223629,37.2427864326717));
#70159=CARTESIAN_POINT('Ctrl Pts',(28.7381567726455,18.8977618636188,37.2385439735388));
#70160=CARTESIAN_POINT('Ctrl Pts',(28.6686121021959,18.94110588085,37.2343015144059));
#70161=CARTESIAN_POINT('Ctrl Pts',(28.6014561967581,18.9877809561547,37.230059055273));
#70162=CARTESIAN_POINT('Ctrl Pts',(28.5346126627082,19.0342389253396,37.2258363296667));
#70163=CARTESIAN_POINT('Ctrl Pts',(28.4701360575167,19.0839967024078,37.2216136040605));
#70164=CARTESIAN_POINT('Ctrl Pts',(28.4083555741484,19.1367720827404,37.2173908784542));
#70165=CARTESIAN_POINT('Ctrl Pts',(28.3461420244647,19.189917405784,37.213138552558));
#70166=CARTESIAN_POINT('Ctrl Pts',(28.2866628888177,19.2461224725628,37.2088862266617));
#70167=CARTESIAN_POINT('Ctrl Pts',(28.2302157062022,19.3050623010191,37.2046339007655));
#70168=CARTESIAN_POINT('Ctrl Pts',(28.1737685235867,19.3640021294754,37.2003815748693));
#70169=CARTESIAN_POINT('Ctrl Pts',(28.1203535568256,19.4256763196491,37.1961292489731));
#70170=CARTESIAN_POINT('Ctrl Pts',(28.0702252177862,19.4897286535422,37.1918769230769));
#70171=CARTESIAN_POINT('Ctrl Pts',(28.0203683885972,19.5534340611271,37.1876476290304));
#70172=CARTESIAN_POINT('Ctrl Pts',(27.9735727040171,19.6197345946428,37.1834183349838));
#70173=CARTESIAN_POINT('Ctrl Pts',(27.930119809746,19.6883040565764,37.1791890409373));
#70174=CARTESIAN_POINT('Ctrl Pts',(27.8867277353166,19.7567775436872,37.1749656665193));
#70175=CARTESIAN_POINT('Ctrl Pts',(27.8466694096143,19.8275132663813,37.1707422921013));
#70176=CARTESIAN_POINT('Ctrl Pts',(27.8101858643266,19.9001526009463,37.1665189176833));
#70177=CARTESIAN_POINT('Ctrl Pts',(27.7737422108834,19.9727125101977,37.1623001611881));
#70178=CARTESIAN_POINT('Ctrl Pts',(27.7408657831866,20.0471714851209,37.1580814046929));
#70179=CARTESIAN_POINT('Ctrl Pts',(27.7117531859141,20.1231438157681,37.1538626481977));
#70180=CARTESIAN_POINT('Ctrl Pts',(27.6826622239771,20.1990596867719,37.1496470269162));
#70181=CARTESIAN_POINT('Ctrl Pts',(27.6573297031452,20.2764862472493,37.1454314056346));
#70182=CARTESIAN_POINT('Ctrl Pts',(27.6359047284464,20.3550164366296,37.1412157843531));
#70183=CARTESIAN_POINT('Ctrl Pts',(27.6144894075789,20.4335112412679,37.1370020625789));
#70184=CARTESIAN_POINT('Ctrl Pts',(27.5969782550267,20.5131082384583,37.1327883408046));
#70185=CARTESIAN_POINT('Ctrl Pts',(27.5834705400339,20.5933851710573,37.1285746190304));
#70186=CARTESIAN_POINT('Ctrl Pts',(27.5699608051698,20.6736741078388,37.1243602671588));
#70187=CARTESIAN_POINT('Ctrl Pts',(27.5604557878433,20.7546427257951,37.1201459152872));
#70188=CARTESIAN_POINT('Ctrl Pts',(27.5550034413766,20.8358595774352,37.1159315634156));
#70189=CARTESIAN_POINT('Ctrl Pts',(27.5512929178413,20.8911306504147,37.1130635410144));
#70190=CARTESIAN_POINT('Ctrl Pts',(27.5494582371227,20.9465165035797,37.1101955186133));
#70191=CARTESIAN_POINT('Ctrl Pts',(27.5495007214879,21.0018804285691,37.1073274962121));
#70192=CARTESIAN_POINT('Ctrl Pts',(27.5495007214883,21.0018804290879,37.1073274961852));
#70193=CARTESIAN_POINT('Ctrl Pts',(27.5495734263339,21.0966264490123,37.102419359567));
#70194=CARTESIAN_POINT('Ctrl Pts',(27.5551449651667,21.1911451718291,37.0975112229488));
#70195=CARTESIAN_POINT('Ctrl Pts',(27.5661129364305,21.2848578799844,37.0926030863306));
#70196=CARTESIAN_POINT('Ctrl Pts',(27.5771936827079,21.3795341621384,37.0876444832076));
#70197=CARTESIAN_POINT('Ctrl Pts',(27.5937823092464,21.4733876385682,37.0826858800847));
#70198=CARTESIAN_POINT('Ctrl Pts',(27.615723715063,21.5658417155771,37.0777272769618));
#70199=CARTESIAN_POINT('Ctrl Pts',(27.6345755168118,21.6452771877251,37.0734669025899));
#70200=CARTESIAN_POINT('Ctrl Pts',(27.6573779156586,21.7236799129869,37.069206528218));
#70201=CARTESIAN_POINT('Ctrl Pts',(27.6840045937171,21.8006969015031,37.0649461538461));
#70202=CARTESIAN_POINT('Ctrl Pts',(27.7104481669317,21.8771842639191,37.0607150769774));
#70203=CARTESIAN_POINT('Ctrl Pts',(27.7407344179044,21.9525035155541,37.0564840001087));
#70204=CARTESIAN_POINT('Ctrl Pts',(27.7747406301215,22.0262411932719,37.0522529232399));
#70205=CARTESIAN_POINT('Ctrl Pts',(27.8086981438002,22.0998732750736,37.0480279054776));
#70206=CARTESIAN_POINT('Ctrl Pts',(27.8463648454955,22.171927862545,37.0438028877154));
#70207=CARTESIAN_POINT('Ctrl Pts',(27.8875688214277,22.242008359793,37.0395778699531));
#70208=CARTESIAN_POINT('Ctrl Pts',(27.9288386499126,22.312200860301,37.0353460997307));
#70209=CARTESIAN_POINT('Ctrl Pts',(27.973656900648,22.3804125166,37.0311143295082));
#70210=CARTESIAN_POINT('Ctrl Pts',(28.0218030873939,22.4462666507099,37.0268825592858));
#70211=CARTESIAN_POINT('Ctrl Pts',(28.0697862084264,22.5118977442826,37.0226651215927));
#70212=CARTESIAN_POINT('Ctrl Pts',(28.1210744961541,22.5751868734316,37.0184476838995));
#70213=CARTESIAN_POINT('Ctrl Pts',(28.175405613739,22.6357889764957,37.0142302462064));
#70214=CARTESIAN_POINT('Ctrl Pts',(28.2297188748722,22.6963711620875,37.0100141946153));
#70215=CARTESIAN_POINT('Ctrl Pts',(28.2870726697613,22.754267729426,37.0057981430241));
#70216=CARTESIAN_POINT('Ctrl Pts',(28.347164964824,22.8091673765837,37.001582091433));
#70217=CARTESIAN_POINT('Ctrl Pts',(28.407255921585,22.864065801084,36.9973661337366));
#70218=CARTESIAN_POINT('Ctrl Pts',(28.4700849132321,22.9159671253415,36.9931501760402));
#70219=CARTESIAN_POINT('Ctrl Pts',(28.5353147666167,22.9645985384065,36.9889342183438));
#70220=CARTESIAN_POINT('Ctrl Pts',(28.6009666757401,23.0135446105717,36.9846909821998));
#70221=CARTESIAN_POINT('Ctrl Pts',(28.66905025467,23.0591780068706,36.9804477460557));
#70222=CARTESIAN_POINT('Ctrl Pts',(28.7391913838261,23.1012643535219,36.9762045099117));
#70223=CARTESIAN_POINT('Ctrl Pts',(28.8089829943779,23.143140980693,36.9719824181375));
#70224=CARTESIAN_POINT('Ctrl Pts',(28.8808112568981,23.1815056551039,36.9677603263633));
#70225=CARTESIAN_POINT('Ctrl Pts',(28.9542837808468,23.2161741445563,36.9635382345891));
#70226=CARTESIAN_POINT('Ctrl Pts',(29.0283082338989,23.2511030653547,36.9592844262601));
#70227=CARTESIAN_POINT('Ctrl Pts',(29.1040013112907,23.2822798553515,36.9550306179312));
#70228=CARTESIAN_POINT('Ctrl Pts',(29.1809439930593,23.3095665193916,36.9507768096022));
#70229=CARTESIAN_POINT('Ctrl Pts',(29.257886674828,23.3368531834316,36.9465230012733));
#70230=CARTESIAN_POINT('Ctrl Pts',(29.3360784870119,23.3602496460209,36.9422691929443));
#70231=CARTESIAN_POINT('Ctrl Pts',(29.4150896273457,23.3796701674731,36.9380153846154));
#70232=CARTESIAN_POINT('Ctrl Pts',(29.4937041069858,23.3989931918194,36.9337829317378));
#70233=CARTESIAN_POINT('Ctrl Pts',(29.5734239395721,23.4144524666238,36.9295504788602));
#70234=CARTESIAN_POINT('Ctrl Pts',(29.6538350226455,23.4259266391326,36.9253180259826));
#70235=CARTESIAN_POINT('Ctrl Pts',(29.7341309568104,23.4373843805925,36.92109163399));
#70236=CARTESIAN_POINT('Ctrl Pts',(29.8151157193599,23.4448682887738,36.9168652419974));
#70237=CARTESIAN_POINT('Ctrl Pts',(29.8963626798454,23.4483074880152,36.9126388500048));
#70238=CARTESIAN_POINT('Ctrl Pts',(29.9777064211677,23.4517507840077,36.9084074235623));
#70239=CARTESIAN_POINT('Ctrl Pts',(30.059312526285,23.4511396355139,36.9041759971198));
#70240=CARTESIAN_POINT('Ctrl Pts',(30.1407452638531,23.4464547861555,36.8999445706773));
#70241=CARTESIAN_POINT('Ctrl Pts',(30.221934964488,23.4417839187833,36.8957257729752));
#70242=CARTESIAN_POINT('Ctrl Pts',(30.3029518648406,23.43306364041,36.8915069752731));
#70243=CARTESIAN_POINT('Ctrl Pts',(30.383363542695,23.4203269705005,36.8872881775711));
#70244=CARTESIAN_POINT('Ctrl Pts',(30.4637486421758,23.407594510427,36.8830707743031));
#70245=CARTESIAN_POINT('Ctrl Pts',(30.5435284578888,23.3908483678063,36.878853371035));
#70246=CARTESIAN_POINT('Ctrl Pts',(30.6222773685781,23.3701732271198,36.874635967767));
#70247=CARTESIAN_POINT('Ctrl Pts',(30.7010243370977,23.3494985963404,36.870418668512));
#70248=CARTESIAN_POINT('Ctrl Pts',(30.778740002042,23.3248952792246,36.8662013692571));
#70249=CARTESIAN_POINT('Ctrl Pts',(30.8550119861844,23.2964983678376,36.8619840700021));
#70250=CARTESIAN_POINT('Ctrl Pts',(30.9317238452976,23.2679376860872,36.8577424487839));
#70251=CARTESIAN_POINT('Ctrl Pts',(31.0069748683008,23.2355396652763,36.8535008275658));
#70252=CARTESIAN_POINT('Ctrl Pts',(31.0803657137938,23.1994908898331,36.8492592063477));
#70253=CARTESIAN_POINT('Ctrl Pts',(31.1534412005239,23.1635970151429,36.8450358112777));
#70254=CARTESIAN_POINT('Ctrl Pts',(31.2246720794835,23.1240839695699,36.8408124162077));
#70255=CARTESIAN_POINT('Ctrl Pts',(31.2936903488492,23.08118128266,36.8365890211377));
#70256=CARTESIAN_POINT('Ctrl Pts',(31.3631553928521,23.0380008746111,36.8323382868455));
#70257=CARTESIAN_POINT('Ctrl Pts',(31.4303786881534,22.9913870572403,36.8280875525533));
#70258=CARTESIAN_POINT('Ctrl Pts',(31.4950176219411,22.9416159661698,36.8238368182612));
#70259=CARTESIAN_POINT('Ctrl Pts',(31.5596565557289,22.8918448750993,36.819586083969));
#70260=CARTESIAN_POINT('Ctrl Pts',(31.6217108088404,22.8389168650207,36.8153353496768));
#70261=CARTESIAN_POINT('Ctrl Pts',(31.6808756159897,22.7831453708465,36.8110846153846));
#70262=CARTESIAN_POINT('Ctrl Pts',(31.7397829612703,22.7276165721833,36.8068523786089));
#70263=CARTESIAN_POINT('Ctrl Pts',(31.7960455326341,22.6690620488109,36.8026201418332));
#70264=CARTESIAN_POINT('Ctrl Pts',(31.8493366530194,22.6077637244941,36.7983879050575));
#70265=CARTESIAN_POINT('Ctrl Pts',(31.9025516273736,22.5465529874539,36.7941617155938));
#70266=CARTESIAN_POINT('Ctrl Pts',(31.9528032811068,22.4826065838145,36.7899355261301));
#70267=CARTESIAN_POINT('Ctrl Pts',(31.9998005337598,22.4162443557431,36.7857093366664));
#70268=CARTESIAN_POINT('Ctrl Pts',(32.0468566060492,22.3497990717075,36.781477857895));
#70269=CARTESIAN_POINT('Ctrl Pts',(32.0906497976773,22.2809322469608,36.7772463791236));
#70270=CARTESIAN_POINT('Ctrl Pts',(32.1309274021744,22.2099994449016,36.7730149003523));
#70271=CARTESIAN_POINT('Ctrl Pts',(32.1710826970664,22.1392820420232,36.7687962711658));
#70272=CARTESIAN_POINT('Ctrl Pts',(32.2077434797372,22.0665115874194,36.7645776419794));
#70273=CARTESIAN_POINT('Ctrl Pts',(32.2407027904726,21.9920691784188,36.7603590127929));
#70274=CARTESIAN_POINT('Ctrl Pts',(32.2736513089402,21.9176511450009,36.7561417649634));
#70275=CARTESIAN_POINT('Ctrl Pts',(32.3029005744618,21.8415626689452,36.751924517134));
#70276=CARTESIAN_POINT('Ctrl Pts',(32.3282907129676,21.7642071747301,36.7477072693046));
#70277=CARTESIAN_POINT('Ctrl Pts',(32.3536803047399,21.6868533462341,36.7434901122864));
#70278=CARTESIAN_POINT('Ctrl Pts',(32.3752107909009,21.6082329956549,36.7392729552682));
#70279=CARTESIAN_POINT('Ctrl Pts',(32.3927718235932,21.5287657801129,36.73505579825));
#70280=CARTESIAN_POINT('Ctrl Pts',(32.4104355964662,21.4488336445275,36.7308139689087));
#70281=CARTESIAN_POINT('Ctrl Pts',(32.4240832019679,21.3680451633441,36.7265721395673));
#70282=CARTESIAN_POINT('Ctrl Pts',(32.4336546040302,21.2868370936308,36.722330310226));
#70283=CARTESIAN_POINT('Ctrl Pts',(32.4431841648433,21.20598402385,36.7181070239818));
#70284=CARTESIAN_POINT('Ctrl Pts',(32.4486731082285,21.1247154972942,36.7138837377377));
#70285=CARTESIAN_POINT('Ctrl Pts',(32.4501144933605,21.0434651518448,36.7096604514935));
#70286=CARTESIAN_POINT('Ctrl Pts',(32.4515653714831,20.9616796900313,36.7054093506036));
#70287=CARTESIAN_POINT('Ctrl Pts',(32.4489151997653,20.8799131266057,36.7011582497136));
#70288=CARTESIAN_POINT('Ctrl Pts',(32.4422099791544,20.7986032082709,36.6969071488237));
#70289=CARTESIAN_POINT('Ctrl Pts',(32.4355047585435,20.7172932899361,36.6926560479337));
#70290=CARTESIAN_POINT('Ctrl Pts',(32.4247446139307,20.6364404775047,36.6884049470438));
#70291=CARTESIAN_POINT('Ctrl Pts',(32.4100274355389,20.5564709592938,36.6841538461538));
#70292=CARTESIAN_POINT('Ctrl Pts',(32.395393134607,20.4769517767627,36.6799266846655));
#70293=CARTESIAN_POINT('Ctrl Pts',(32.3767912539051,20.3980070206159,36.6756995231771));
#70294=CARTESIAN_POINT('Ctrl Pts',(32.3542804263525,20.3200632940535,36.6714723616887));
#70295=CARTESIAN_POINT('Ctrl Pts',(32.3318019203877,20.2422314809689,36.6672512696605));
#70296=CARTESIAN_POINT('Ctrl Pts',(32.3054257420964,20.1653982868145,36.6630301776323));
#70297=CARTESIAN_POINT('Ctrl Pts',(32.2752617080485,20.0899810936645,36.658809085604));
#70298=CARTESIAN_POINT('Ctrl Pts',(32.2450143632446,20.0143556039924,36.6545763352423));
#70299=CARTESIAN_POINT('Ctrl Pts',(32.2109583004433,19.9401544127064,36.6503435848806));
#70300=CARTESIAN_POINT('Ctrl Pts',(32.1732549515911,19.8677839581666,36.6461108345189));
#70301=CARTESIAN_POINT('Ctrl Pts',(32.1357229412312,19.7957423827569,36.6418973193999));
#70302=CARTESIAN_POINT('Ctrl Pts',(32.0945769325993,19.7255153603938,36.6376838042809));
#70303=CARTESIAN_POINT('Ctrl Pts',(32.0500239675645,19.6574829675527,36.6334702891619));
#70304=CARTESIAN_POINT('Ctrl Pts',(32.0054855560905,19.5894727980039,36.6292581504192));
#70305=CARTESIAN_POINT('Ctrl Pts',(31.9575426532041,19.5236562238784,36.6250460116766));
#70306=CARTESIAN_POINT('Ctrl Pts',(31.9064466291453,19.4603859249083,36.6208338729339));
#70307=CARTESIAN_POINT('Ctrl Pts',(31.8553515634987,19.3971168127042,36.6166218131987));
#70308=CARTESIAN_POINT('Ctrl Pts',(31.8011037878849,19.3363942424423,36.6124097534635));
#70309=CARTESIAN_POINT('Ctrl Pts',(31.7439952000058,19.2785381234669,36.6081976937283));
#70310=CARTESIAN_POINT('Ctrl Pts',(31.6864008841917,19.2201899185507,36.6039498089945));
#70311=CARTESIAN_POINT('Ctrl Pts',(31.6258971853853,19.1647575126242,36.5997019242607));
#70312=CARTESIAN_POINT('Ctrl Pts',(31.5628203493671,19.1125300517348,36.5954540395269));
#70313=CARTESIAN_POINT('Ctrl Pts',(31.5001832688747,19.06066670731,36.5912357699563));
#70314=CARTESIAN_POINT('Ctrl Pts',(31.4350092306898,19.0119639924745,36.5870175003856));
#70315=CARTESIAN_POINT('Ctrl Pts',(31.3676580729662,18.9666624369155,36.5827992308149));
#70316=CARTESIAN_POINT('Ctrl Pts',(31.2995976378414,18.9208838090881,36.5785365384996));
#70317=CARTESIAN_POINT('Ctrl Pts',(31.2293143776745,18.878578647648,36.5742738461843));
#70318=CARTESIAN_POINT('Ctrl Pts',(31.1572049201268,18.8399474490573,36.570011153869));
#70319=CARTESIAN_POINT('Ctrl Pts',(31.0850954625791,18.8013162504665,36.5657484615537));
#70320=CARTESIAN_POINT('Ctrl Pts',(31.0111602729967,18.766359162102,36.5614857692384));
#70321=CARTESIAN_POINT('Ctrl Pts',(30.9358146226311,18.7352260064038,36.5572230769231));
#70322=CARTESIAN_POINT('Ctrl Pts',(30.8608852465432,18.7042648570767,36.5529839353921));
#70323=CARTESIAN_POINT('Ctrl Pts',(30.7842798019212,18.6769692289837,36.5487447938612));
#70324=CARTESIAN_POINT('Ctrl Pts',(30.7063906892555,18.6535212670614,36.5445056523303));
#70325=CARTESIAN_POINT('Ctrl Pts',(30.6286132109143,18.6301069118564,36.5402725865355));
#70326=CARTESIAN_POINT('Ctrl Pts',(30.5495561586416,18.6105294015379,36.5360395207408));
#70327=CARTESIAN_POINT('Ctrl Pts',(30.4696318358586,18.5949228310202,36.5318064549461));
#70328=CARTESIAN_POINT('Ctrl Pts',(30.3897700025997,18.5793284626348,36.5275766988105));
#70329=CARTESIAN_POINT('Ctrl Pts',(30.3090426948968,18.5676989705192,36.5233469426749));
#70330=CARTESIAN_POINT('Ctrl Pts',(30.2278763899687,18.5601183223577,36.5191171865393));
#70331=CARTESIAN_POINT('Ctrl Pts',(30.1467939365032,18.5525455056285,36.5148918000894));
#70332=CARTESIAN_POINT('Ctrl Pts',(30.0652738489759,18.5490132479074,36.5106664136395));
#70333=CARTESIAN_POINT('Ctrl Pts',(29.9837496684643,18.5495538821013,36.5064410271896));
#70334=CARTESIAN_POINT('Ctrl Pts',(29.9022532963383,18.5500943318815,36.5022170820443));
#70335=CARTESIAN_POINT('Ctrl Pts',(29.8207532966366,18.5547049112194,36.497993136899));
#70336=CARTESIAN_POINT('Ctrl Pts',(29.7396842522887,18.5633658539917,36.4937691917536));
#70337=CARTESIAN_POINT('Ctrl Pts',(29.658618274113,18.5720264691921,36.4895454063653));
#70338=CARTESIAN_POINT('Ctrl Pts',(29.5779836791669,18.5847370930045,36.4853216209769));
#70339=CARTESIAN_POINT('Ctrl Pts',(29.4982095547469,18.6014261322501,36.4810978355885));
#70340=CARTESIAN_POINT('Ctrl Pts',(29.4182463990515,18.6181547175314,36.4768640415972));
#70341=CARTESIAN_POINT('Ctrl Pts',(29.3391482536535,18.6388805002022,36.4726302476058));
#70342=CARTESIAN_POINT('Ctrl Pts',(29.2613348834451,18.6634803455599,36.4683964536145));
#70343=CARTESIAN_POINT('Ctrl Pts',(29.1835971414072,18.6880562818992,36.4641667745213));
#70344=CARTESIAN_POINT('Ctrl Pts',(29.107142105256,18.7164985677058,36.4599370954281));
#70345=CARTESIAN_POINT('Ctrl Pts',(29.0323693455972,18.7486357099172,36.4557074163349));
#70346=CARTESIAN_POINT('Ctrl Pts',(28.9574636806604,18.7808299744796,36.4514702191739));
#70347=CARTESIAN_POINT('Ctrl Pts',(28.8842466854363,18.8167320167715,36.447233022013));
#70348=CARTESIAN_POINT('Ctrl Pts',(28.8130947299534,18.8561235740053,36.442995824852));
#70349=CARTESIAN_POINT('Ctrl Pts',(28.7419879697471,18.8954901099686,36.4387613191321));
#70350=CARTESIAN_POINT('Ctrl Pts',(28.6729439830911,18.9383414323312,36.4345268134122));
#70351=CARTESIAN_POINT('Ctrl Pts',(28.6063074191304,18.9844178905266,36.4302923076924));
#70352=CARTESIAN_POINT('Ctrl Pts',(28.5400362733839,19.0302416769745,36.4260810229405));
#70353=CARTESIAN_POINT('Ctrl Pts',(28.4758993258002,19.0794261131487,36.4218697381886));
#70354=CARTESIAN_POINT('Ctrl Pts',(28.4142597267235,19.131744654575,36.4176584534367));
#70355=CARTESIAN_POINT('Ctrl Pts',(28.3527073376953,19.1839891737396,36.4134531269705));
#70356=CARTESIAN_POINT('Ctrl Pts',(28.293645636355,19.2393586920566,36.4092478005044));
#70357=CARTESIAN_POINT('Ctrl Pts',(28.2374084176009,19.2975837278574,36.4050424740383));
#70358=CARTESIAN_POINT('Ctrl Pts',(28.1812341943487,19.3557435414544,36.4008418582719));
#70359=CARTESIAN_POINT('Ctrl Pts',(28.1278784918971,19.4167521808891,36.3966412425055));
#70360=CARTESIAN_POINT('Ctrl Pts',(28.0776404842038,19.4803012989321,36.3924406267391));
#70361=CARTESIAN_POINT('Ctrl Pts',(28.0274328768808,19.5438119616936,36.3882425528784));
#70362=CARTESIAN_POINT('Ctrl Pts',(27.9803395107438,19.6098596845769,36.3840444790176));
#70363=CARTESIAN_POINT('Ctrl Pts',(27.9366204240837,19.6781017528979,36.3798464051569));
#70364=CARTESIAN_POINT('Ctrl Pts',(27.8929140772019,19.7463239354233,36.3756495546183));
#70365=CARTESIAN_POINT('Ctrl Pts',(27.852580310588,19.8167387984264,36.3714527040798));
#70366=CARTESIAN_POINT('Ctrl Pts',(27.8158359544079,19.888974495368,36.3672558535413));
#70367=CARTESIAN_POINT('Ctrl Pts',(27.7790907779861,19.961211804822,36.3630589093167));
#70368=CARTESIAN_POINT('Ctrl Pts',(27.745935382464,20.0352696094488,36.3588619650922));
#70369=CARTESIAN_POINT('Ctrl Pts',(27.7165400357545,20.1107526543825,36.3546650208676));
#70370=CARTESIAN_POINT('Ctrl Pts',(27.6871151990702,20.1863114253523,36.3504638661883));
#70371=CARTESIAN_POINT('Ctrl Pts',(27.661458114269,20.2632978531103,36.3462627115089));
#70372=CARTESIAN_POINT('Ctrl Pts',(27.6396901352626,20.3412985559275,36.3420615568296));
#70373=CARTESIAN_POINT('Ctrl Pts',(27.6179108952965,20.4193396098846,36.3378582288188));
#70374=CARTESIAN_POINT('Ctrl Pts',(27.6000248701609,20.498395525103,36.333654900808));
#70375=CARTESIAN_POINT('Ctrl Pts',(27.5861023566467,20.5780421615688,36.3294515727972));
#70376=CARTESIAN_POINT('Ctrl Pts',(27.5721556922805,20.6578269580107,36.3252409534339));
#70377=CARTESIAN_POINT('Ctrl Pts',(27.5621863282676,20.7382040556211,36.3210303340707));
#70378=CARTESIAN_POINT('Ctrl Pts',(27.5562126715831,20.8187439836334,36.3168197147074));
#70379=CARTESIAN_POINT('Ctrl Pts',(27.5517237840708,20.8792654859884,36.3136556566309));
#70380=CARTESIAN_POINT('Ctrl Pts',(27.5494900785215,20.9398788267477,36.3104915985544));
#70381=CARTESIAN_POINT('Ctrl Pts',(27.5495000331448,21.0004030420562,36.3073275404779));
#70382=CARTESIAN_POINT('Origin',(30.,21.,34.5704548813952));
#70383=CARTESIAN_POINT('',(28.0052508090074,20.9982034660445,43.7704548814489));
#70384=CARTESIAN_POINT('Ctrl Pts',(29.0285070491141,22.7421908646526,43.6351577566542));
#70385=CARTESIAN_POINT('Ctrl Pts',(28.9675818954129,22.708217343982,43.639602469207));
#70386=CARTESIAN_POINT('Ctrl Pts',(28.908486328592,22.6710694864593,43.6440471817597));
#70387=CARTESIAN_POINT('Ctrl Pts',(28.8515575689449,22.6309836127479,43.6484918943125));
#70388=CARTESIAN_POINT('Ctrl Pts',(28.7945220419805,22.590822559791,43.6529449427229));
#70389=CARTESIAN_POINT('Ctrl Pts',(28.7396618290827,22.5477127828589,43.6573979911333));
#70390=CARTESIAN_POINT('Ctrl Pts',(28.6872817167157,22.5019315134956,43.6618510395437));
#70391=CARTESIAN_POINT('Ctrl Pts',(28.6372470355454,22.4582001980658,43.6661046932184));
#70392=CARTESIAN_POINT('Ctrl Pts',(28.5894753228672,22.4120318333357,43.6703583468931));
#70393=CARTESIAN_POINT('Ctrl Pts',(28.5441987295342,22.3636972623754,43.6746120005678));
#70394=CARTESIAN_POINT('Ctrl Pts',(28.4973458543333,22.3136799475913,43.6790137430598));
#70395=CARTESIAN_POINT('Ctrl Pts',(28.4529706563383,22.2611349777435,43.6834154855518));
#70396=CARTESIAN_POINT('Ctrl Pts',(28.4113623498905,22.2063407392418,43.6878172280439));
#70397=CARTESIAN_POINT('Ctrl Pts',(28.3698108377044,22.151621293458,43.6922129622713));
#70398=CARTESIAN_POINT('Ctrl Pts',(28.331019032848,22.0946590590543,43.6966086964987));
#70399=CARTESIAN_POINT('Ctrl Pts',(28.2952385622418,22.0357683152292,43.7010044307261));
#70400=CARTESIAN_POINT('Ctrl Pts',(28.2594940914354,21.9769368231398,43.7053957422741));
#70401=CARTESIAN_POINT('Ctrl Pts',(28.2267552069749,21.9161810952028,43.709787053822));
#70402=CARTESIAN_POINT('Ctrl Pts',(28.1972313706564,21.8538459062117,43.71417836537));
#70403=CARTESIAN_POINT('Ctrl Pts',(28.1677266502282,21.7915510775799,43.7185668336618));
#70404=CARTESIAN_POINT('Ctrl Pts',(28.1414330620072,21.7276792694403,43.7229553019535));
#70405=CARTESIAN_POINT('Ctrl Pts',(28.1185141209499,21.6625997656468,43.7273437702453));
#70406=CARTESIAN_POINT('Ctrl Pts',(28.0955949794947,21.5975196928129,43.7317322769088));
#70407=CARTESIAN_POINT('Ctrl Pts',(28.0760507245765,21.5312323717174,43.7361207835724));
#70408=CARTESIAN_POINT('Ctrl Pts',(28.0599961095465,21.4641254868301,43.7405092902359));
#70409=CARTESIAN_POINT('Ctrl Pts',(28.043941154452,21.3970171805032,43.7448978898556));
#70410=CARTESIAN_POINT('Ctrl Pts',(28.0313760922087,21.3290897666479,43.7492864894753));
#70411=CARTESIAN_POINT('Ctrl Pts',(28.0223647706706,21.2607421373988,43.7536750890949));
#70412=CARTESIAN_POINT('Ctrl Pts',(28.0133463364229,21.192340560808,43.7580671526721));
#70413=CARTESIAN_POINT('Ctrl Pts',(28.0078872889507,21.1235186065601,43.7624592162493));
#70414=CARTESIAN_POINT('Ctrl Pts',(28.0059995797444,21.0546798547944,43.7668512798264));
#70415=CARTESIAN_POINT('Ctrl Pts',(28.0054833036828,21.0358529086072,43.7680524803494));
#70416=CARTESIAN_POINT('Ctrl Pts',(28.0052338580162,21.0170247032861,43.7692536808723));
#70417=CARTESIAN_POINT('Ctrl Pts',(28.0052508090066,20.9982034668865,43.7704548813952));
#70418=CARTESIAN_POINT('',(31.0476776298179,22.697468452278,44.2999965101293));
#70419=CARTESIAN_POINT('Ctrl Pts',(28.0052508090074,20.9982034660445,43.7704548814489));
#70420=CARTESIAN_POINT('Ctrl Pts',(28.0053328331714,20.9071294095688,43.7762673691061));
#70421=CARTESIAN_POINT('Ctrl Pts',(28.0116558478415,20.8163314699453,43.7820798567633));
#70422=CARTESIAN_POINT('Ctrl Pts',(28.0240847802233,20.7265285997501,43.7878923444204));
#70423=CARTESIAN_POINT('Ctrl Pts',(28.0338144188917,20.6562289592379,43.7924424862131));
#70424=CARTESIAN_POINT('Ctrl Pts',(28.047284839067,20.5865384317374,43.7969926280058));
#70425=CARTESIAN_POINT('Ctrl Pts',(28.0644114788864,20.5177919127253,43.8015427697985));
#70426=CARTESIAN_POINT('Ctrl Pts',(28.0811824707744,20.4504729683883,43.8059984243752));
#70427=CARTESIAN_POINT('Ctrl Pts',(28.1015025590443,20.383897827886,43.8104540789519));
#70428=CARTESIAN_POINT('Ctrl Pts',(28.1252889150972,20.3184679679995,43.8149097335286));
#70429=CARTESIAN_POINT('Ctrl Pts',(28.149039712796,20.2531359195697,43.8193587273228));
#70430=CARTESIAN_POINT('Ctrl Pts',(28.1762463277037,20.1889462095843,43.823807721117));
#70431=CARTESIAN_POINT('Ctrl Pts',(28.2067755219195,20.1262874993954,43.8282567149113));
#70432=CARTESIAN_POINT('Ctrl Pts',(28.237269005219,20.0637020829835,43.8327005045837));
#70433=CARTESIAN_POINT('Ctrl Pts',(28.2710771353077,20.002644547045,43.8371442942561));
#70434=CARTESIAN_POINT('Ctrl Pts',(28.3080183796402,19.9434841416881,43.8415880839285));
#70435=CARTESIAN_POINT('Ctrl Pts',(28.3449365344237,19.8843607136204,43.8460290960795));
#70436=CARTESIAN_POINT('Ctrl Pts',(28.3849836600036,19.82713247769,43.8504701082304));
#70437=CARTESIAN_POINT('Ctrl Pts',(28.4279327706877,19.7721432538679,43.8549111203814));
#70438=CARTESIAN_POINT('Ctrl Pts',(28.4708695994956,19.7171697549542,43.8593508625651));
#70439=CARTESIAN_POINT('Ctrl Pts',(28.5167064649867,19.6644343823259,43.8637906047489));
#70440=CARTESIAN_POINT('Ctrl Pts',(28.5651746726225,19.6142497185943,43.8682303469327));
#70441=CARTESIAN_POINT('Ctrl Pts',(28.6136454537636,19.564062390219,43.8726703248524));
#70442=CARTESIAN_POINT('Ctrl Pts',(28.6647475129065,19.516426389776,43.8771103027722));
#70443=CARTESIAN_POINT('Ctrl Pts',(28.7181749463016,19.4716178180144,43.8815502806919));
#70444=CARTESIAN_POINT('Ctrl Pts',(28.7716588913163,19.4267618510327,43.8859949548946));
#70445=CARTESIAN_POINT('Ctrl Pts',(28.8274727442014,19.3847395966743,43.8904396290973));
#70446=CARTESIAN_POINT('Ctrl Pts',(28.8852778776969,19.3457865456513,43.8948843032999));
#70447=CARTESIAN_POINT('Ctrl Pts',(28.9431169127208,19.3068106494607,43.8993315842131));
#70448=CARTESIAN_POINT('Ctrl Pts',(29.0029491333274,19.270907791132,43.9037788651263));
#70449=CARTESIAN_POINT('Ctrl Pts',(29.0644097102805,19.238268359743,43.9082261460394));
#70450=CARTESIAN_POINT('Ctrl Pts',(29.1259767210557,19.2055724053013,43.9126811284928));
#70451=CARTESIAN_POINT('Ctrl Pts',(29.18917727366,19.17615136503,43.9171361109462));
#70452=CARTESIAN_POINT('Ctrl Pts',(29.2536256467657,19.150147874198,43.9215910933996));
#70453=CARTESIAN_POINT('Ctrl Pts',(29.2868141369158,19.1367570536426,43.9238852419429));
#70454=CARTESIAN_POINT('Ctrl Pts',(29.320333266343,19.1242717121239,43.9261793904861));
#70455=CARTESIAN_POINT('Ctrl Pts',(29.3541290211179,19.1127061063158,43.9284735390293));
#70456=CARTESIAN_POINT('Ctrl Pts',(29.4196878237881,19.0902705290076,43.9329238503966));
#70457=CARTESIAN_POINT('Ctrl Pts',(29.4865478267324,19.0712102377844,43.9373741617639));
#70458=CARTESIAN_POINT('Ctrl Pts',(29.5543279193972,19.0556739061898,43.9418244731312));
#70459=CARTESIAN_POINT('Ctrl Pts',(29.6220061951333,19.0401609127393,43.9462680993935));
#70460=CARTESIAN_POINT('Ctrl Pts',(29.6906013434222,19.0281614816811,43.9507117256559));
#70461=CARTESIAN_POINT('Ctrl Pts',(29.7597155666627,19.0197750244995,43.9551553519182));
#70462=CARTESIAN_POINT('Ctrl Pts',(29.8287486916828,19.0113984079372,43.9595937640558));
#70463=CARTESIAN_POINT('Ctrl Pts',(29.8982991975004,19.0066264044798,43.9640321761933));
#70464=CARTESIAN_POINT('Ctrl Pts',(29.9679592990589,19.0055073437129,43.9684705883309));
#70465=CARTESIAN_POINT('Ctrl Pts',(30.0375757569679,19.0043889840632,43.9729062197016));
#70466=CARTESIAN_POINT('Ctrl Pts',(30.1073011851581,19.0069190350564,43.9773418510723));
#70467=CARTESIAN_POINT('Ctrl Pts',(30.1767244254279,19.0130938522524,43.981777482443));
#70468=CARTESIAN_POINT('Ctrl Pts',(30.2461278629675,19.019266908104,43.9862118485657));
#70469=CARTESIAN_POINT('Ctrl Pts',(30.315228795419,19.0290826229272,43.9906462146885));
#70470=CARTESIAN_POINT('Ctrl Pts',(30.3836196189453,19.0424853639218,43.9950805808113));
#70471=CARTESIAN_POINT('Ctrl Pts',(30.452014273844,19.0558888557612,43.9995151953549));
#70472=CARTESIAN_POINT('Ctrl Pts',(30.5196982600174,19.0728796760039,44.0039498098985));
#70473=CARTESIAN_POINT('Ctrl Pts',(30.5862743933617,19.0933511340081,44.0083844244422));
#70474=CARTESIAN_POINT('Ctrl Pts',(30.6529218696097,19.1138445292017,44.0128237911133));
#70475=CARTESIAN_POINT('Ctrl Pts',(30.7184586538887,19.1378258619552,44.0172631577845));
#70476=CARTESIAN_POINT('Ctrl Pts',(30.7825038930611,19.1651389099323,44.0217025244557));
#70477=CARTESIAN_POINT('Ctrl Pts',(30.8465870812085,19.1924681418162,44.0261445216021));
#70478=CARTESIAN_POINT('Ctrl Pts',(30.9091765248711,19.2231328019344,44.0305865187486));
#70479=CARTESIAN_POINT('Ctrl Pts',(30.9699150404523,19.2569301859064,44.035028515895));
#70480=CARTESIAN_POINT('Ctrl Pts',(31.0307601390871,19.2907868770306,44.0394783077926));
#70481=CARTESIAN_POINT('Ctrl Pts',(31.0897474111735,19.3277870042404,44.0439280996903));
#70482=CARTESIAN_POINT('Ctrl Pts',(31.1465484532773,19.3676844034356,44.048377891588));
#70483=CARTESIAN_POINT('Ctrl Pts',(31.1764455659519,19.3886843181375,44.0507200304787));
#70484=CARTESIAN_POINT('Ctrl Pts',(31.2057375495987,19.4104862182316,44.0530621693694));
#70485=CARTESIAN_POINT('Ctrl Pts',(31.2343804588746,19.4330499544502,44.0554043082601));
#70486=CARTESIAN_POINT('Ctrl Pts',(31.2889592555873,19.4760449435517,44.0598672320908));
#70487=CARTESIAN_POINT('Ctrl Pts',(31.3413948198101,19.5219782247501,44.0643301559215));
#70488=CARTESIAN_POINT('Ctrl Pts',(31.3913545013924,19.5706084462418,44.0687930797522));
#70489=CARTESIAN_POINT('Ctrl Pts',(31.4412392636534,19.6191657420649,44.0732493110018));
#70490=CARTESIAN_POINT('Ctrl Pts',(31.488655166713,19.670411612911,44.0777055422513));
#70491=CARTESIAN_POINT('Ctrl Pts',(31.5333019901385,19.7240640417571,44.0821617735008));
#70492=CARTESIAN_POINT('Ctrl Pts',(31.5778958543375,19.777652829096,44.0866127188523));
#70493=CARTESIAN_POINT('Ctrl Pts',(31.6197268532869,19.8336421310425,44.0910636642037));
#70494=CARTESIAN_POINT('Ctrl Pts',(31.6585323280854,19.8917139001162,44.0955146095551));
#70495=CARTESIAN_POINT('Ctrl Pts',(31.6973131081661,19.9497487139417,44.0999627224495));
#70496=CARTESIAN_POINT('Ctrl Pts',(31.7330719139705,20.0098629612187,44.1044108353439));
#70497=CARTESIAN_POINT('Ctrl Pts',(31.7655879444851,20.0717076038289,44.1088589482383));
#70498=CARTESIAN_POINT('Ctrl Pts',(31.7980942134645,20.1335336802537,44.1133057257787));
#70499=CARTESIAN_POINT('Ctrl Pts',(31.827359413291,20.1970886894234,44.1177525033191));
#70500=CARTESIAN_POINT('Ctrl Pts',(31.8532083461037,20.2619983818231,44.1221992808596));
#70501=CARTESIAN_POINT('Ctrl Pts',(31.8790582080234,20.3269104073192,44.1266462182338));
#70502=CARTESIAN_POINT('Ctrl Pts',(31.9014913810092,20.3931767590138,44.131093155608));
#70503=CARTESIAN_POINT('Ctrl Pts',(31.9203811980705,20.4604042099892,44.1355400929822));
#70504=CARTESIAN_POINT('Ctrl Pts',(31.939290276191,20.527700209639,44.1399915646895));
#70505=CARTESIAN_POINT('Ctrl Pts',(31.9546486547361,20.5959587944747,44.1444430363969));
#70506=CARTESIAN_POINT('Ctrl Pts',(31.9663801219466,20.6647735414483,44.1488945081043));
#70507=CARTESIAN_POINT('Ctrl Pts',(31.9781182417616,20.7336273114429,44.1533485041234));
#70508=CARTESIAN_POINT('Ctrl Pts',(31.9862252989082,20.8030373871522,44.1578025001425));
#70509=CARTESIAN_POINT('Ctrl Pts',(31.9906769543349,20.8725918920163,44.1622564961616));
#70510=CARTESIAN_POINT('Ctrl Pts',(31.9951361092244,20.9422635715885,44.1667179955867));
#70511=CARTESIAN_POINT('Ctrl Pts',(31.9959275639082,21.0120796786559,44.1711794950117));
#70512=CARTESIAN_POINT('Ctrl Pts',(31.9930790999361,21.081628817816,44.1756409944367));
#70513=CARTESIAN_POINT('Ctrl Pts',(31.9916544776593,21.1164129168766,44.1778723554548));
#70514=CARTESIAN_POINT('Ctrl Pts',(31.9893201909051,21.1511303235671,44.1801037164728));
#70515=CARTESIAN_POINT('Ctrl Pts',(31.9860845360349,21.1857303912212,44.1823350774908));
#70516=CARTESIAN_POINT('Ctrl Pts',(31.9796904185953,21.2541050803869,44.1867445664418));
#70517=CARTESIAN_POINT('Ctrl Pts',(31.9697474260424,21.3222956334465,44.1911540553928));
#70518=CARTESIAN_POINT('Ctrl Pts',(31.9562734759691,21.3898995379838,44.1955635443437));
#70519=CARTESIAN_POINT('Ctrl Pts',(31.9428220864341,21.4573902477656,44.1999656501261));
#70520=CARTESIAN_POINT('Ctrl Pts',(31.9258515746657,21.5242957730104,44.2043677559085));
#70521=CARTESIAN_POINT('Ctrl Pts',(31.9054316214507,21.5902185175643,44.2087698616909));
#70522=CARTESIAN_POINT('Ctrl Pts',(31.8850307753997,21.656079577516,44.2131678483769));
#70523=CARTESIAN_POINT('Ctrl Pts',(31.8611870322523,21.7209592040553,44.2175658350628));
#70524=CARTESIAN_POINT('Ctrl Pts',(31.8340208395287,21.7844712376336,44.2219638217487));
#70525=CARTESIAN_POINT('Ctrl Pts',(31.8068703863029,21.8479464737289,44.2263592603374));
#70526=CARTESIAN_POINT('Ctrl Pts',(31.7764014968065,21.9100552290098,44.2307546989261));
#70527=CARTESIAN_POINT('Ctrl Pts',(31.7427834152148,21.9704295596035,44.2351501375147));
#70528=CARTESIAN_POINT('Ctrl Pts',(31.7091728334126,22.0307904214105,44.2395445955339));
#70529=CARTESIAN_POINT('Ctrl Pts',(31.6724146977926,22.08941718992,44.2439390535531));
#70530=CARTESIAN_POINT('Ctrl Pts',(31.6327241542048,22.1459665783853,44.2483335115723));
#70531=CARTESIAN_POINT('Ctrl Pts',(31.5930017075813,22.2025614209311,44.2527315018322));
#70532=CARTESIAN_POINT('Ctrl Pts',(31.5503424298924,22.2570751355507,44.257129492092));
#70533=CARTESIAN_POINT('Ctrl Pts',(31.5050041369246,22.3091944509277,44.2615274823519));
#70534=CARTESIAN_POINT('Ctrl Pts',(31.4596489554362,22.3613331807571,44.2659271108637));
#70535=CARTESIAN_POINT('Ctrl Pts',(31.4116131179426,22.411075373252,44.2703267393756));
#70536=CARTESIAN_POINT('Ctrl Pts',(31.3611920146618,22.458143978392,44.2747263678874));
#70537=CARTESIAN_POINT('Ctrl Pts',(31.3106822662604,22.5052953346404,44.2791337313669));
#70538=CARTESIAN_POINT('Ctrl Pts',(31.2577792577581,22.5497633897621,44.2835410948463));
#70539=CARTESIAN_POINT('Ctrl Pts',(31.2028116783259,22.5913112922942,44.2879484583258));
#70540=CARTESIAN_POINT('Ctrl Pts',(31.1527248749113,22.6291700018809,44.2919644755936));
#70541=CARTESIAN_POINT('Ctrl Pts',(31.1009244884018,22.6646044879896,44.2959804928615));
#70542=CARTESIAN_POINT('Ctrl Pts',(31.0476776298179,22.697468452278,44.2999965101293));
#70543=CARTESIAN_POINT('',(31.9448291324621,20.5565282331122,44.3));
#70544=CARTESIAN_POINT('Origin',(30.,21.,44.3));
#70545=CARTESIAN_POINT('Ctrl Pts',(31.9448291324621,20.5565282331122,44.3));
#70546=CARTESIAN_POINT('Ctrl Pts',(31.9434341237209,20.5504104735555,44.2995994828922));
#70547=CARTESIAN_POINT('Ctrl Pts',(31.9420102376063,20.5442992487752,44.2992002906137));
#70548=CARTESIAN_POINT('Ctrl Pts',(31.9388490264969,20.5310154843226,44.2983343572612));
#70549=CARTESIAN_POINT('Ctrl Pts',(31.9371006814741,20.5238456379719,44.2978681050606));
#70550=CARTESIAN_POINT('Ctrl Pts',(31.9302822551317,20.4965429444236,44.2960964363976));
#70551=CARTESIAN_POINT('Ctrl Pts',(31.9249376115805,20.4764793757493,44.2948024403774));
#70552=CARTESIAN_POINT('Ctrl Pts',(31.8850789379699,20.3357244790958,44.2857598111901));
#70553=CARTESIAN_POINT('Ctrl Pts',(31.8395502834143,20.218434501564,44.2783986236436));
#70554=CARTESIAN_POINT('Ctrl Pts',(31.7403021141881,20.0204172501169,44.2652348708085));
#70555=CARTESIAN_POINT('Ctrl Pts',(31.6911800408815,19.9378599127613,44.2594922868282));
#70556=CARTESIAN_POINT('Ctrl Pts',(31.6202738014925,19.8361586323494,44.251833574737));
#70557=CARTESIAN_POINT('Ctrl Pts',(31.6037532576586,19.8134970278139,44.2500870503018));
#70558=CARTESIAN_POINT('Ctrl Pts',(31.5748580673,19.7755672983547,44.2470893540965));
#70559=CARTESIAN_POINT('Ctrl Pts',(31.5627252727568,19.7601197417334,44.2458466737178));
#70560=CARTESIAN_POINT('Ctrl Pts',(31.5390912707049,19.7309268221743,44.2434543449884));
#70561=CARTESIAN_POINT('Ctrl Pts',(31.5276290235602,19.7171523064516,44.2423062033946));
#70562=CARTESIAN_POINT('Ctrl Pts',(31.4968352044298,19.681144480257,44.2392517230607));
#70563=CARTESIAN_POINT('Ctrl Pts',(31.4771945495343,19.6591824771764,44.2373337287763));
#70564=CARTESIAN_POINT('Ctrl Pts',(31.3953917591754,19.5716909362662,44.2294580918896));
#70565=CARTESIAN_POINT('Ctrl Pts',(31.3293067501396,19.5099917109462,44.223343944255));
#70566=CARTESIAN_POINT('Ctrl Pts',(31.153516201105,19.3668971435795,44.2076775235069));
#70567=CARTESIAN_POINT('Ctrl Pts',(31.0392125324802,19.2918843519338,44.1979865621142));
#70568=CARTESIAN_POINT('Ctrl Pts',(30.8674702770602,19.2028404416543,44.1845936060368));
#70569=CARTESIAN_POINT('Ctrl Pts',(30.8156749929514,19.1787469412871,44.1806954665008));
#70570=CARTESIAN_POINT('Ctrl Pts',(30.7479157348429,19.1506993044561,44.1758293491229));
#70571=CARTESIAN_POINT('Ctrl Pts',(30.7328429118829,19.1446746062218,44.1747613604616));
#70572=CARTESIAN_POINT('Ctrl Pts',(30.7080722645547,19.135122616491,44.1730315622435));
#70573=CARTESIAN_POINT('Ctrl Pts',(30.6984179649346,19.1314855244572,44.1723636043077));
#70574=CARTESIAN_POINT('Ctrl Pts',(30.6803701863742,19.124845759858,44.1711270292059));
#70575=CARTESIAN_POINT('Ctrl Pts',(30.6719845429981,19.1218243447877,44.1705573744103));
#70576=CARTESIAN_POINT('Ctrl Pts',(30.6492634307127,19.113809400193,44.1690265898844));
#70577=CARTESIAN_POINT('Ctrl Pts',(30.6348907043012,19.108923108541,44.1680717854463));
#70578=CARTESIAN_POINT('Ctrl Pts',(30.5764365610879,19.0897920506394,44.1642376028347));
#70579=CARTESIAN_POINT('Ctrl Pts',(30.5319176847037,19.0769197069819,44.1614295950262));
#70580=CARTESIAN_POINT('Ctrl Pts',(30.344094779711,19.0296348695956,44.1498867395038));
#70581=CARTESIAN_POINT('Ctrl Pts',(30.1976508102751,19.0096031788969,44.141581842313));
#70582=CARTESIAN_POINT('Ctrl Pts',(29.9797068464994,19.0041026333218,44.1287496328143));
#70583=CARTESIAN_POINT('Ctrl Pts',(29.9090472334075,19.0060731760548,44.1245226979111));
#70584=CARTESIAN_POINT('Ctrl Pts',(29.8143918401592,19.0137549757,44.1186802605285));
#70585=CARTESIAN_POINT('Ctrl Pts',(29.7901769533301,19.0161668690963,44.1171699639898));
#70586=CARTESIAN_POINT('Ctrl Pts',(29.7491995082393,19.0210069945519,44.1145843950081));
#70587=CARTESIAN_POINT('Ctrl Pts',(29.7324123691852,19.0232068817404,44.113516659659));
#70588=CARTESIAN_POINT('Ctrl Pts',(29.6985766404238,19.0280798026475,44.1113463537843));
#70589=CARTESIAN_POINT('Ctrl Pts',(29.6815307075488,19.0307609124588,44.1102436023418));
#70590=CARTESIAN_POINT('Ctrl Pts',(29.6388756411331,19.0380383161197,44.1074595371683));
#70591=CARTESIAN_POINT('Ctrl Pts',(29.6133183095037,19.0429150222135,44.1057690623826));
#70592=CARTESIAN_POINT('Ctrl Pts',(29.5111896500796,19.0644811501401,44.0989203643151));
#70593=CARTESIAN_POINT('Ctrl Pts',(29.4355451836378,19.0851744811417,44.093631610921));
#70594=CARTESIAN_POINT('Ctrl Pts',(29.2306762636094,19.1544143677903,44.0787351828451));
#70595=CARTESIAN_POINT('Ctrl Pts',(29.1049738117217,19.2119929358024,44.0689159558757));
#70596=CARTESIAN_POINT('Ctrl Pts',(28.9536059122473,19.3013178496884,44.056741005391));
#70597=CARTESIAN_POINT('Ctrl Pts',(28.9215447122107,19.3214898956802,44.0541427708433));
#70598=CARTESIAN_POINT('Ctrl Pts',(28.8682915300466,19.3571516045234,44.0498173886977));
#70599=CARTESIAN_POINT('Ctrl Pts',(28.846795937031,19.3721684775037,44.0480686809835));
#70600=CARTESIAN_POINT('Ctrl Pts',(28.8160184572405,19.3945854679002,44.045568163435));
#70601=CARTESIAN_POINT('Ctrl Pts',(28.8064976028942,19.4016508017566,44.0447951148783));
#70602=CARTESIAN_POINT('Ctrl Pts',(28.7902319383214,19.4139477813066,44.0434760750596));
#70603=CARTESIAN_POINT('Ctrl Pts',(28.7834569623165,19.4191383857587,44.0429272185943));
#70604=CARTESIAN_POINT('Ctrl Pts',(28.7676038716615,19.4314463965378,44.0416437408695));
#70605=CARTESIAN_POINT('Ctrl Pts',(28.7585536040441,19.438599511443,44.0409116461403));
#70606=CARTESIAN_POINT('Ctrl Pts',(28.7325964807534,19.4594837767966,44.0388120545902));
#70607=CARTESIAN_POINT('Ctrl Pts',(28.7158512568176,19.4734142637928,44.0374577484468));
#70608=CARTESIAN_POINT('Ctrl Pts',(28.6324696291209,19.5451232207159,44.0306952999249));
#70609=CARTESIAN_POINT('Ctrl Pts',(28.5694825819699,19.6070072090484,44.0255224834918));
#70610=CARTESIAN_POINT('Ctrl Pts',(28.4391897744712,19.7532113638835,44.0141326645876));
#70611=CARTESIAN_POINT('Ctrl Pts',(28.3742085905228,19.8392192795495,44.0079492782131));
#70612=CARTESIAN_POINT('Ctrl Pts',(28.2830417138283,19.9826658339708,43.9978668915263));
#70613=CARTESIAN_POINT('Ctrl Pts',(28.2520883539796,20.0368186272763,43.9941094895549));
#70614=CARTESIAN_POINT('Ctrl Pts',(28.2127028900028,20.1138943953514,43.9887693158053));
#70615=CARTESIAN_POINT('Ctrl Pts',(28.2020767659583,20.1356585933408,43.9872624131843));
#70616=CARTESIAN_POINT('Ctrl Pts',(28.1843870541664,20.1736287264136,43.9846323230322));
#70617=CARTESIAN_POINT('Ctrl Pts',(28.1771376361307,20.1897453357007,43.9835156339193));
#70618=CARTESIAN_POINT('Ctrl Pts',(28.162622978667,20.2231947566915,43.9811962821705));
#70619=CARTESIAN_POINT('Ctrl Pts',(28.1553866715127,20.2405381290434,43.9799927779853));
#70620=CARTESIAN_POINT('Ctrl Pts',(28.1371717116799,20.2859909618703,43.9768351449418));
#70621=CARTESIAN_POINT('Ctrl Pts',(28.1265843196647,20.3142510190077,43.9748683662749));
#70622=CARTESIAN_POINT('Ctrl Pts',(28.0666613934466,20.4859580264117,43.9628918679428));
#70623=CARTESIAN_POINT('Ctrl Pts',(28.0331874819878,20.6343895543651,43.9523734764335));
#70624=CARTESIAN_POINT('Ctrl Pts',(28.0100422816045,20.8480265193637,43.9374458910679));
#70625=CARTESIAN_POINT('Ctrl Pts',(28.0062240924429,20.9111964719612,43.9330659629323));
#70626=CARTESIAN_POINT('Ctrl Pts',(28.0049358837812,21.0117371358053,43.9262358786079));
#70627=CARTESIAN_POINT('Ctrl Pts',(28.0055040430015,21.0490392613042,43.9237329406731));
#70628=CARTESIAN_POINT('Ctrl Pts',(28.0077299826456,21.1004382239322,43.9203457283881));
#70629=CARTESIAN_POINT('Ctrl Pts',(28.0084923414103,21.1145640945553,43.9194212722629));
#70630=CARTESIAN_POINT('Ctrl Pts',(28.0100506279022,21.1386695514292,43.917856060892));
#70631=CARTESIAN_POINT('Ctrl Pts',(28.0107715164431,21.148653307395,43.9172114414416));
#70632=CARTESIAN_POINT('Ctrl Pts',(28.0124768064266,21.1700289388491,43.9158395624887));
#70633=CARTESIAN_POINT('Ctrl Pts',(28.0134840410073,21.1814184245903,43.9151135253773));
#70634=CARTESIAN_POINT('Ctrl Pts',(28.0166135546796,21.2136456250799,43.9130715667147));
#70635=CARTESIAN_POINT('Ctrl Pts',(28.0189662306404,21.2344600798231,43.9117674433768));
#70636=CARTESIAN_POINT('Ctrl Pts',(28.0365042699389,21.3703995258375,43.9033242060423));
#70637=CARTESIAN_POINT('Ctrl Pts',(28.0613916600583,21.4840613045464,43.8966043146279));
#70638=CARTESIAN_POINT('Ctrl Pts',(28.122258555724,21.678857585042,43.8847528504098));
#70639=CARTESIAN_POINT('Ctrl Pts',(28.154006040805,21.7609636447577,43.8796461401918));
#70640=CARTESIAN_POINT('Ctrl Pts',(28.2144316857153,21.8909810290603,43.8710939289265));
#70641=CARTESIAN_POINT('Ctrl Pts',(28.239882461285,21.9402589313771,43.8677368774083));
#70642=CARTESIAN_POINT('Ctrl Pts',(28.2788407859681,22.0085515453623,43.8628762981749));
#70643=CARTESIAN_POINT('Ctrl Pts',(28.2906806585351,22.0284904367803,43.8614310521531));
#70644=CARTESIAN_POINT('Ctrl Pts',(28.3120232764009,22.0630455680405,43.8588775283063));
#70645=CARTESIAN_POINT('Ctrl Pts',(28.321375194925,22.0777523053833,43.8577748301383));
#70646=CARTESIAN_POINT('Ctrl Pts',(28.3413259836677,22.1082370171956,43.8554545567587));
#70647=CARTESIAN_POINT('Ctrl Pts',(28.3519600234487,22.1239897567119,43.8542357429379));
#70648=CARTESIAN_POINT('Ctrl Pts',(28.3808708824625,22.1655243923786,43.8509676018097));
#70649=CARTESIAN_POINT('Ctrl Pts',(28.3995374150165,22.1910270921372,43.8489036608418));
#70650=CARTESIAN_POINT('Ctrl Pts',(28.5086300313856,22.3328746005923,43.8370880648462));
#70651=CARTESIAN_POINT('Ctrl Pts',(28.6111104106896,22.4393438778738,43.8268576130645));
#70652=CARTESIAN_POINT('Ctrl Pts',(28.8010860846217,22.5973712411959,43.809619513463));
#70653=CARTESIAN_POINT('Ctrl Pts',(28.8825082063805,22.6553565383366,43.8026740450259));
#70654=CARTESIAN_POINT('Ctrl Pts',(28.9840587730104,22.7167544829962,43.7947754624454));
#70655=CARTESIAN_POINT('Ctrl Pts',(29.0003196373933,22.7262739544709,43.7935327649782));
#70656=CARTESIAN_POINT('Ctrl Pts',(29.0206372328177,22.7377849317006,43.7920094303564));
#70657=CARTESIAN_POINT('Ctrl Pts',(29.0245683961202,22.7399945647539,43.7917160345296));
#70658=CARTESIAN_POINT('Ctrl Pts',(29.0285070491189,22.7421908646553,43.7914234503344));
#70659=CARTESIAN_POINT('Ctrl Pts',(31.0764316815492,23.2048264539079,36.0477323453659));
#70660=CARTESIAN_POINT('Ctrl Pts',(30.343759082817,23.5625289824132,36.0900426017762));
#70661=CARTESIAN_POINT('Ctrl Pts',(28.5060462149485,23.4833658723433,36.1746631145967));
#70662=CARTESIAN_POINT('Ctrl Pts',(27.1003088914074,21.0900268756385,36.3015938838274));
#70663=CARTESIAN_POINT('Ctrl Pts',(28.3516935167001,18.6154236179253,36.4285246530582));
#70664=CARTESIAN_POINT('Ctrl Pts',(31.106936958626,18.3203304537226,36.555455422289));
#70665=CARTESIAN_POINT('Ctrl Pts',(32.8517167152586,20.4752346214199,36.6823861915197));
#70666=CARTESIAN_POINT('Ctrl Pts',(31.9886999989277,23.1097649269993,36.8093169607505));
#70667=CARTESIAN_POINT('Ctrl Pts',(29.307978492492,23.8155985483982,36.9362477299812));
#70668=CARTESIAN_POINT('Ctrl Pts',(27.2597204992662,21.947373336303,37.0631784992121));
#70669=CARTESIAN_POINT('Ctrl Pts',(27.71672768337,19.2130704126436,37.1901092684428));
#70670=CARTESIAN_POINT('Ctrl Pts',(30.2610646213885,18.1123776609252,37.3170400376736));
#70671=CARTESIAN_POINT('Ctrl Pts',(32.5667581606509,19.6515629228612,37.4439708069043));
#70672=CARTESIAN_POINT('Ctrl Pts',(32.5259010455236,22.4234923255752,37.5709015761352));
#70673=CARTESIAN_POINT('Ctrl Pts',(30.1758619809016,23.8940609300158,37.6978323453659));
#70674=CARTESIAN_POINT('Ctrl Pts',(27.6650464678629,22.7188684463249,37.8247631145967));
#70675=CARTESIAN_POINT('Ctrl Pts',(27.2888550599909,19.9722806185091,37.9516938838274));
#70676=CARTESIAN_POINT('Ctrl Pts',(29.3912011683962,18.1652373451714,38.0786246530582));
#70677=CARTESIAN_POINT('Ctrl Pts',(32.050113649744,18.9497440858611,38.2055554222889));
#70678=CARTESIAN_POINT('Ctrl Pts',(32.8348048707721,21.6086019464631,38.3324861915198));
#70679=CARTESIAN_POINT('Ctrl Pts',(31.0279076233404,23.7110737866463,38.4594169607505));
#70680=CARTESIAN_POINT('Ctrl Pts',(28.281293579258,23.335072457048,38.5863477299813));
#70681=CARTESIAN_POINT('Ctrl Pts',(27.1059269935297,20.8243397017099,38.7132784992121));
#70682=CARTESIAN_POINT('Ctrl Pts',(28.5763320889074,18.4741962054449,38.8402092684428));
#70683=CARTESIAN_POINT('Ctrl Pts',(31.3482593864868,18.4331513966575,38.9671400376736));
#70684=CARTESIAN_POINT('Ctrl Pts',(32.8876032221475,20.7387285822562,39.0940708069044));
#70685=CARTESIAN_POINT('Ctrl Pts',(31.7870900669591,23.2831610144047,39.2210015761351));
#70686=CARTESIAN_POINT('Ctrl Pts',(29.0528129048075,23.7403196403237,39.3479323453659));
#70687=CARTESIAN_POINT('Ctrl Pts',(27.18445750707,21.6922684411505,39.4748631145967));
#70688=CARTESIAN_POINT('Ctrl Pts',(27.8900809299641,19.0113430053537,39.6017938838274));
#70689=CARTESIAN_POINT('Ctrl Pts',(30.5245997659872,18.1484547680464,39.7287246530582));
#70690=CARTESIAN_POINT('Ctrl Pts',(32.6795276561991,19.8924591817973,39.855655422289));
#70691=CARTESIAN_POINT('Ctrl Pts',(32.3848219663657,22.6489812955596,39.9825861915197));
#70692=CARTESIAN_POINT('Ctrl Pts',(29.9099036715976,23.8979989261478,40.1095169607505));
#70693=CARTESIAN_POINT('Ctrl Pts',(27.5173517562181,22.4976557755345,40.2364477299813));
#70694=CARTESIAN_POINT('Ctrl Pts',(27.3944455716353,19.7281504628318,40.363378499212));
#70695=CARTESIAN_POINT('Ctrl Pts',(29.6535463828245,18.1213744572335,40.4903092684429));
#70696=CARTESIAN_POINT('Ctrl Pts',(32.2293763057922,19.1462480177964,40.6172400376735));
#70697=CARTESIAN_POINT('Ctrl Pts',(32.7671025918857,21.8658281413979,40.7441708069044));
#70698=CARTESIAN_POINT('Ctrl Pts',(30.7751339845446,23.7938651417188,40.8711015761351));
#70699=CARTESIAN_POINT('Ctrl Pts',(28.0745351703353,23.1677408318724,40.9980323453659));
#70700=CARTESIAN_POINT('Ctrl Pts',(27.1342030555683,20.5598602512758,41.1249631145967));
#70701=CARTESIAN_POINT('Ctrl Pts',(28.8137925577971,18.3543569729932,41.2518938838274));
#70702=CARTESIAN_POINT('Ctrl Pts',(31.5778170627554,18.5675098269038,41.3788246530582));
#70703=CARTESIAN_POINT('Ctrl Pts',(32.8993956773707,21.004453729579,41.5057554222889));
#70704=CARTESIAN_POINT('Ctrl Pts',(31.5703365926297,23.4373260128722,41.6326861915198));
#70705=CARTESIAN_POINT('Ctrl Pts',(28.8056702945361,23.6419863162043,41.7596169607505));
#70706=CARTESIAN_POINT('Ctrl Pts',(27.1328643882722,21.4313334472583,41.8865477299813));
#70707=CARTESIAN_POINT('Ctrl Pts',(28.0812039396034,18.8263540621345,42.0134784992121));
#70708=CARTESIAN_POINT('Ctrl Pts',(30.7837135247371,18.2085293479113,42.1404092684429));
#70709=CARTESIAN_POINT('Ctrl Pts',(32.7697495648629,20.1426770302188,42.2673400376736));
#70710=CARTESIAN_POINT('Ctrl Pts',(32.2236706232122,22.8605921026094,42.3942708069045));
#70711=CARTESIAN_POINT('Ctrl Pts',(29.6447046345813,23.8775479033933,42.5212015761351));
#70712=CARTESIAN_POINT('Ctrl Pts',(27.3905500410461,22.2638382074801,42.6481323453659));
#70713=CARTESIAN_POINT('Ctrl Pts',(27.521965507246,19.4947254252231,42.7750631145966));
#70714=CARTESIAN_POINT('Ctrl Pts',(29.918805267606,18.1017354465642,42.9019938838274));
#70715=CARTESIAN_POINT('Ctrl Pts',(32.3898806293322,19.3583581123743,43.0289246530583));
#70716=CARTESIAN_POINT('Ctrl Pts',(32.6761044863914,22.1157574108982,43.1558554222889));
#70717=CARTESIAN_POINT('Ctrl Pts',(30.5158528780656,23.8531638208612,43.2827861915198));
#70718=CARTESIAN_POINT('Ctrl Pts',(27.8839492041854,22.9821246131684,43.4097169607505));
#70719=CARTESIAN_POINT('Ctrl Pts',(27.1866622496698,20.2991673270333,43.5366477299814));
#70720=CARTESIAN_POINT('Ctrl Pts',(29.0611061008494,18.2566179316801,43.663578499212));
#70721=CARTESIAN_POINT('Ctrl Pts',(31.7943571903737,18.7226724914995,43.7905092684428));
#70722=CARTESIAN_POINT('Ctrl Pts',(32.8862611019678,21.2694728856569,43.9174400376736));
#70723=CARTESIAN_POINT('Ctrl Pts',(31.3414348862857,23.5723269250707,44.0443708069043));
#70724=CARTESIAN_POINT('Ctrl Pts',(28.5663156435887,23.5186411284601,44.1713015761352));
#70725=CARTESIAN_POINT('Ctrl Pts',(27.597396578881,21.9551030800674,44.2559220889556));
#70726=CARTESIAN_POINT('Ctrl Pts',(27.5505003151765,21.1411245936918,44.2982323453659));
#70727=CARTESIAN_POINT('Ctrl Pts',(31.0089644699886,23.0666351544788,36.1365179670879));
#70728=CARTESIAN_POINT('Ctrl Pts',(30.3222133896125,23.4019180602806,36.1788282234981));
#70729=CARTESIAN_POINT('Ctrl Pts',(28.5996823442128,23.3277166346227,36.2634487363187));
#70730=CARTESIAN_POINT('Ctrl Pts',(27.2820520311131,21.0843842859889,36.3903795055494));
#70731=CARTESIAN_POINT('Ctrl Pts',(28.4550039674528,18.7648810540163,36.5173102747802));
#70732=CARTESIAN_POINT('Ctrl Pts',(31.0375577762294,18.4882833626621,36.644241044011));
#70733=CARTESIAN_POINT('Ctrl Pts',(32.6729804533697,20.5081251962915,36.7711718132417));
#70734=CARTESIAN_POINT('Ctrl Pts',(31.8640547976968,22.9775317726687,36.8981025824725));
#70735=CARTESIAN_POINT('Ctrl Pts',(29.3513521336173,23.6391260548901,37.0250333517032));
#70736=CARTESIAN_POINT('Ctrl Pts',(27.4314722416013,21.8879950790455,37.1519641209341));
#70737=CARTESIAN_POINT('Ctrl Pts',(27.8598357124969,19.3250693054486,37.2788948901648));
#70738=CARTESIAN_POINT('Ctrl Pts',(30.2447019461309,18.2933643696932,37.4058256593956));
#70739=CARTESIAN_POINT('Ctrl Pts',(32.4058821674807,19.7360785415657,37.5327564286263));
#70740=CARTESIAN_POINT('Ctrl Pts',(32.3675858424873,22.3342724897691,37.6596871978572));
#70741=CARTESIAN_POINT('Ctrl Pts',(30.1648395280379,23.7126706714596,37.7866179670878));
#70742=CARTESIAN_POINT('Ctrl Pts',(27.8113937062773,22.6111354028808,37.9135487363187));
#70743=CARTESIAN_POINT('Ctrl Pts',(27.4587807435006,20.0366947026765,38.0404795055494));
#70744=CARTESIAN_POINT('Ctrl Pts',(29.4293586848217,18.3429109820917,38.1674102747802));
#70745=CARTESIAN_POINT('Ctrl Pts',(31.9216192420625,19.0782474102089,38.2943410440109));
#70746=CARTESIAN_POINT('Ctrl Pts',(32.6571285878948,21.5704567701534,38.4212718132418));
#70747=CARTESIAN_POINT('Ctrl Pts',(30.9634817407904,23.5411525627962,38.5482025824725));
#70748=CARTESIAN_POINT('Ctrl Pts',(28.3890164674693,23.1887177648098,38.6751333517033));
#70749=CARTESIAN_POINT('Ctrl Pts',(27.2873180089985,20.8353495137682,38.802064120934));
#70750=CARTESIAN_POINT('Ctrl Pts',(28.6655629298386,18.6325053131091,38.9289948901648));
#70751=CARTESIAN_POINT('Ctrl Pts',(31.2637549048502,18.5940330584795,39.0559256593956));
#70752=CARTESIAN_POINT('Ctrl Pts',(32.7066177115661,20.7551042188318,39.1828564286264));
#70753=CARTESIAN_POINT('Ctrl Pts',(31.6750811158181,23.1400599613368,39.3097871978571));
#70754=CARTESIAN_POINT('Ctrl Pts',(29.1121794890824,23.5685653821706,39.4367179670879));
#70755=CARTESIAN_POINT('Ctrl Pts',(27.360926487205,21.6488793230334,39.5636487363187));
#70756=CARTESIAN_POINT('Ctrl Pts',(28.0223237454753,19.1359855112171,39.6905795055494));
#70757=CARTESIAN_POINT('Ctrl Pts',(30.4917195711702,18.3271802819235,39.8175102747802));
#70758=CARTESIAN_POINT('Ctrl Pts',(32.511583640465,19.961876212134,39.944441044011));
#70759=CARTESIAN_POINT('Ctrl Pts',(32.2353491378557,22.5456285497852,40.0713718132417));
#70760=CARTESIAN_POINT('Ctrl Pts',(29.9155506143189,23.7163618468944,40.1983025824725));
#70761=CARTESIAN_POINT('Ctrl Pts',(27.6729560153313,22.4037876176339,40.3252333517033));
#70762=CARTESIAN_POINT('Ctrl Pts',(27.5577531877748,19.8078658254209,40.452164120934));
#70763=CARTESIAN_POINT('Ctrl Pts',(29.6752609606157,18.3017972762811,40.5790948901649));
#70764=CARTESIAN_POINT('Ctrl Pts',(32.0896463020688,19.2624351194098,40.7060256593955));
#70765=CARTESIAN_POINT('Ctrl Pts',(32.5936696660659,21.8115608698265,40.8329564286264));
#70766=CARTESIAN_POINT('Ctrl Pts',(30.7265511256235,23.6187548269458,40.9598871978571));
#70767=CARTESIAN_POINT('Ctrl Pts',(28.1952169983062,23.0318739377452,41.0868179670879));
#70768=CARTESIAN_POINT('Ctrl Pts',(27.3138218200968,20.5874467688898,41.2137487363186));
#70769=CARTESIAN_POINT('Ctrl Pts',(28.8881401544254,18.5201772111709,41.3406795055495));
#70770=CARTESIAN_POINT('Ctrl Pts',(31.478924657969,18.7199703424573,41.4676102747802));
#70771=CARTESIAN_POINT('Ctrl Pts',(32.7176710543262,21.0041745843987,41.594541044011));
#70772=CARTESIAN_POINT('Ctrl Pts',(31.4719130392057,23.2845624027232,41.7214718132416));
#70773=CARTESIAN_POINT('Ctrl Pts',(28.8805269680182,23.4763952686807,41.8484025824725));
#70774=CARTESIAN_POINT('Ctrl Pts',(27.3125670560817,21.4042988797719,41.9753333517032));
#70775=CARTESIAN_POINT('Ctrl Pts',(28.2014677909627,18.9625910689611,42.1022641209341));
#70776=CARTESIAN_POINT('Ctrl Pts',(30.734592928342,18.3834895839184,42.2291948901648));
#70777=CARTESIAN_POINT('Ctrl Pts',(32.5961507354479,20.1964112254951,42.3561256593956));
#70778=CARTESIAN_POINT('Ctrl Pts',(32.0842982329819,22.7439762846564,42.4830564286263));
#70779=CARTESIAN_POINT('Ctrl Pts',(29.6669733841881,23.6971926272514,42.6099871978571));
#70780=CARTESIAN_POINT('Ctrl Pts',(27.5541018162817,22.1846249687918,42.7369179670879));
#70781=CARTESIAN_POINT('Ctrl Pts',(27.6772805915587,19.589071104502,42.8638487363187));
#70782=CARTESIAN_POINT('Ctrl Pts',(29.9238942874499,18.2833891744659,42.9907795055494));
#70783=CARTESIAN_POINT('Ctrl Pts',(32.240090740399,19.4612508481023,43.1177102747802));
#70784=CARTESIAN_POINT('Ctrl Pts',(32.5083750237268,22.0458253914477,43.244641044011));
#70785=CARTESIAN_POINT('Ctrl Pts',(30.4835209095301,23.6743368591337,43.3715718132417));
#70786=CARTESIAN_POINT('Ctrl Pts',(28.0165763361817,22.8578915355769,43.4985025824725));
#70787=CARTESIAN_POINT('Ctrl Pts',(27.362993043761,20.3430932231455,43.6254333517033));
#70788=CARTESIAN_POINT('Ctrl Pts',(29.1199528947636,18.428564132788,43.752364120934));
#70789=CARTESIAN_POINT('Ctrl Pts',(31.6818927597432,18.8654079195272,43.8792948901649));
#70790=CARTESIAN_POINT('Ctrl Pts',(32.7053597110826,21.2525832079393,44.0062256593955));
#70791=CARTESIAN_POINT('Ctrl Pts',(31.2573581419655,23.4111018999891,44.1331564286264));
#70792=CARTESIAN_POINT('Ctrl Pts',(28.6561742824999,23.3607809532429,44.2600871978571));
#70793=CARTESIAN_POINT('Ctrl Pts',(27.7479838907253,21.8952403477924,44.3447077106776));
#70794=CARTESIAN_POINT('Ctrl Pts',(27.7040269312043,21.1322793664635,44.3870179670879));
#70795=CARTESIAN_POINT('Ctrl Pts',(30.9414972584282,22.9284438550497,36.2253035888098));
#70796=CARTESIAN_POINT('Ctrl Pts',(30.3006676964081,23.2413071381481,36.26761384522));
#70797=CARTESIAN_POINT('Ctrl Pts',(28.693318473477,23.1720673969021,36.3522343580406));
#70798=CARTESIAN_POINT('Ctrl Pts',(27.4637951708188,21.0787416963392,36.4791651272713));
#70799=CARTESIAN_POINT('Ctrl Pts',(28.5583144182053,18.9143384901075,36.6060958965021));
#70800=CARTESIAN_POINT('Ctrl Pts',(30.9681785938328,18.6562362716017,36.7330266657328));
#70801=CARTESIAN_POINT('Ctrl Pts',(32.4942441914807,20.5410157711632,36.8599574349636));
#70802=CARTESIAN_POINT('Ctrl Pts',(31.739409596466,22.8452986183379,36.9868882041944));
#70803=CARTESIAN_POINT('Ctrl Pts',(29.3947257747426,23.462653561382,37.1138189734251));
#70804=CARTESIAN_POINT('Ctrl Pts',(27.6032239839365,21.828616821788,37.240749742656));
#70805=CARTESIAN_POINT('Ctrl Pts',(28.0029437416238,19.4370681982537,37.3676805118867));
#70806=CARTESIAN_POINT('Ctrl Pts',(30.2283392708734,18.474351078461,37.4946112811175));
#70807=CARTESIAN_POINT('Ctrl Pts',(32.2450061743102,19.8205941602703,37.6215420503482));
#70808=CARTESIAN_POINT('Ctrl Pts',(32.209270639451,22.245052653963,37.748472819579));
#70809=CARTESIAN_POINT('Ctrl Pts',(30.1538170751741,23.5312804129035,37.8754035888098));
#70810=CARTESIAN_POINT('Ctrl Pts',(27.9577409446919,22.5034023594369,38.0023343580406));
#70811=CARTESIAN_POINT('Ctrl Pts',(27.6287064270102,20.1011087868441,38.1292651272713));
#70812=CARTESIAN_POINT('Ctrl Pts',(29.4675162012472,18.520584619012,38.2561958965021));
#70813=CARTESIAN_POINT('Ctrl Pts',(31.793124834381,19.2067507345566,38.3831266657329));
#70814=CARTESIAN_POINT('Ctrl Pts',(32.4794523050175,21.5323115938435,38.5100574349637));
#70815=CARTESIAN_POINT('Ctrl Pts',(30.8990558582405,23.3712313389463,38.6369882041944));
#70816=CARTESIAN_POINT('Ctrl Pts',(28.4967393556804,23.0423630725713,38.7639189734252));
#70817=CARTESIAN_POINT('Ctrl Pts',(27.4687090244673,20.8463593258267,38.8908497426559));
#70818=CARTESIAN_POINT('Ctrl Pts',(28.7547937707697,18.7908144207732,39.0177805118867));
#70819=CARTESIAN_POINT('Ctrl Pts',(31.1792504232137,18.7549147203014,39.1447112811175));
#70820=CARTESIAN_POINT('Ctrl Pts',(32.5256322009844,20.7714798554076,39.2716420503482));
#70821=CARTESIAN_POINT('Ctrl Pts',(31.5630721646773,22.9969589082687,39.398572819579));
#70822=CARTESIAN_POINT('Ctrl Pts',(29.171546073357,23.3968111240174,39.5255035888098));
#70823=CARTESIAN_POINT('Ctrl Pts',(27.53739546734,21.6054902049163,39.6524343580406));
#70824=CARTESIAN_POINT('Ctrl Pts',(28.1545665609866,19.2606280170804,39.7793651272713));
#70825=CARTESIAN_POINT('Ctrl Pts',(30.4588393763534,18.5059057958006,39.9062958965021));
#70826=CARTESIAN_POINT('Ctrl Pts',(32.3436396247307,20.0312932424708,40.0332266657328));
#70827=CARTESIAN_POINT('Ctrl Pts',(32.0858763093458,22.4422758040107,40.1601574349636));
#70828=CARTESIAN_POINT('Ctrl Pts',(29.9211975570403,23.5347247676409,40.2870882041944));
#70829=CARTESIAN_POINT('Ctrl Pts',(27.8285602744445,22.3099194597335,40.4140189734252));
#70830=CARTESIAN_POINT('Ctrl Pts',(27.7210608039143,19.8875811880102,40.5409497426559));
#70831=CARTESIAN_POINT('Ctrl Pts',(29.6969755384068,18.4822200953287,40.6678805118867));
#70832=CARTESIAN_POINT('Ctrl Pts',(31.9499162983454,19.3786222210231,40.7948112811175));
#70833=CARTESIAN_POINT('Ctrl Pts',(32.420236740246,21.7572935982551,40.9217420503482));
#70834=CARTESIAN_POINT('Ctrl Pts',(30.6779682667023,23.4436445121727,41.048672819579));
#70835=CARTESIAN_POINT('Ctrl Pts',(28.3158988262772,22.896007043618,41.1756035888098));
#70836=CARTESIAN_POINT('Ctrl Pts',(27.4934405846254,20.6150332865038,41.3025343580405));
#70837=CARTESIAN_POINT('Ctrl Pts',(28.9624877510537,18.6859974493487,41.4294651272713));
#70838=CARTESIAN_POINT('Ctrl Pts',(31.3800322531826,18.8724308580108,41.5563958965021));
#70839=CARTESIAN_POINT('Ctrl Pts',(32.5359464312817,21.0038954392185,41.6833266657329));
#70840=CARTESIAN_POINT('Ctrl Pts',(31.3734894857819,23.1317987925741,41.8102574349636));
#70841=CARTESIAN_POINT('Ctrl Pts',(28.9553836415003,23.3108042211572,41.9371882041944));
#70842=CARTESIAN_POINT('Ctrl Pts',(27.4922697238911,21.3772643122856,42.0641189734252));
#70843=CARTESIAN_POINT('Ctrl Pts',(28.3217316423219,19.0988280757876,42.1910497426559));
#70844=CARTESIAN_POINT('Ctrl Pts',(30.685472331947,18.5584498199254,42.3179805118868));
#70845=CARTESIAN_POINT('Ctrl Pts',(32.422551906033,20.2501454207713,42.4449112811174));
#70846=CARTESIAN_POINT('Ctrl Pts',(31.9449258427517,22.6273604667032,42.5718420503483));
#70847=CARTESIAN_POINT('Ctrl Pts',(29.6892421337947,23.5168373511096,42.698772819579));
#70848=CARTESIAN_POINT('Ctrl Pts',(27.7176535915173,22.1054117301034,42.8257035888098));
#70849=CARTESIAN_POINT('Ctrl Pts',(27.8325956758717,19.6834167837808,42.9526343580406));
#70850=CARTESIAN_POINT('Ctrl Pts',(29.9289833072939,18.4650429023676,43.0795651272713));
#70851=CARTESIAN_POINT('Ctrl Pts',(32.0903008514657,19.5641435838305,43.2064958965021));
#70852=CARTESIAN_POINT('Ctrl Pts',(32.3406455610623,21.9758933719972,43.3334266657328));
#70853=CARTESIAN_POINT('Ctrl Pts',(30.4511889409944,23.4955098974062,43.4603574349637));
#70854=CARTESIAN_POINT('Ctrl Pts',(28.1492034681781,22.7336584579854,43.5872882041943));
#70855=CARTESIAN_POINT('Ctrl Pts',(27.5393238378524,20.3870191192575,43.7142189734252));
#70856=CARTESIAN_POINT('Ctrl Pts',(29.1787996886778,18.6005103338958,43.8411497426559));
#70857=CARTESIAN_POINT('Ctrl Pts',(31.5694283291128,19.0081433475549,43.9680805118867));
#70858=CARTESIAN_POINT('Ctrl Pts',(32.5244583201973,21.2356935302216,44.0950112811175));
#70859=CARTESIAN_POINT('Ctrl Pts',(31.1732813976455,23.2498768749074,44.2219420503483));
#70860=CARTESIAN_POINT('Ctrl Pts',(28.7460329214112,23.2029207780256,44.348872819579));
#70861=CARTESIAN_POINT('Ctrl Pts',(27.8985712025696,21.8353776155173,44.4334933323995));
#70862=CARTESIAN_POINT('Ctrl Pts',(27.857553547232,21.1234341392353,44.4758035888098));
#70863=CARTESIAN_POINT('Ctrl Pts',(30.8740300468677,22.7902525556206,36.3140892105317));
#70864=CARTESIAN_POINT('Ctrl Pts',(30.2791220032035,23.0806962160155,36.356399466942));
#70865=CARTESIAN_POINT('Ctrl Pts',(28.7869546027412,23.0164181591815,36.4410199797625));
#70866=CARTESIAN_POINT('Ctrl Pts',(27.6455383105245,21.0730991066897,36.5679507489932));
#70867=CARTESIAN_POINT('Ctrl Pts',(28.6616248689581,19.0637959261985,36.6948815182241));
#70868=CARTESIAN_POINT('Ctrl Pts',(30.8987994114361,18.8241891805412,36.8218122874547));
#70869=CARTESIAN_POINT('Ctrl Pts',(32.3155079295918,20.573906346035,36.9487430566855));
#70870=CARTESIAN_POINT('Ctrl Pts',(31.614764395235,22.7130654640073,37.0756738259163));
#70871=CARTESIAN_POINT('Ctrl Pts',(29.4380994158679,23.2861810678738,37.202604595147));
#70872=CARTESIAN_POINT('Ctrl Pts',(27.7749757262716,21.7692385645306,37.3295353643779));
#70873=CARTESIAN_POINT('Ctrl Pts',(28.1460517707507,19.5490670910589,37.4564661336086));
#70874=CARTESIAN_POINT('Ctrl Pts',(30.2119765956158,18.655337787229,37.5833969028394));
#70875=CARTESIAN_POINT('Ctrl Pts',(32.08413018114,19.9051097789748,37.7103276720702));
#70876=CARTESIAN_POINT('Ctrl Pts',(32.0509554364147,22.1558328181569,37.8372584413009));
#70877=CARTESIAN_POINT('Ctrl Pts',(30.1427946223102,23.3498901543472,37.9641892105317));
#70878=CARTESIAN_POINT('Ctrl Pts',(28.1040881831063,22.3956693159929,38.0911199797624));
#70879=CARTESIAN_POINT('Ctrl Pts',(27.7986321105198,20.1655228710115,38.2180507489932));
#70880=CARTESIAN_POINT('Ctrl Pts',(29.5056737176726,18.6982582559323,38.344981518224));
#70881=CARTESIAN_POINT('Ctrl Pts',(31.6646304266995,19.3352540589044,38.4719122874548));
#70882=CARTESIAN_POINT('Ctrl Pts',(32.3017760221401,21.4941664175338,38.5988430566855));
#70883=CARTESIAN_POINT('Ctrl Pts',(30.8346299756906,23.2013101150963,38.7257738259163));
#70884=CARTESIAN_POINT('Ctrl Pts',(28.6044622438917,22.8960083803331,38.852704595147));
#70885=CARTESIAN_POINT('Ctrl Pts',(27.6501000399361,20.857369137885,38.9796353643779));
#70886=CARTESIAN_POINT('Ctrl Pts',(28.8440246117008,18.9491235284374,39.1065661336086));
#70887=CARTESIAN_POINT('Ctrl Pts',(31.0947459415771,18.9157963821233,39.2334969028394));
#70888=CARTESIAN_POINT('Ctrl Pts',(32.3446466904029,20.7878554919833,39.3604276720701));
#70889=CARTESIAN_POINT('Ctrl Pts',(31.4510632135363,22.8538578552008,39.4873584413009));
#70890=CARTESIAN_POINT('Ctrl Pts',(29.2309126576318,23.2250568658642,39.6142892105317));
#70891=CARTESIAN_POINT('Ctrl Pts',(27.713864447475,21.5621010867992,39.7412199797624));
#70892=CARTESIAN_POINT('Ctrl Pts',(28.2868093764979,19.3852705229439,39.8681507489932));
#70893=CARTESIAN_POINT('Ctrl Pts',(30.4259591815364,18.6846313096777,39.9950815182239));
#70894=CARTESIAN_POINT('Ctrl Pts',(32.1756956089965,20.1007102728075,40.1220122874548));
#70895=CARTESIAN_POINT('Ctrl Pts',(31.9364034808358,22.3389230582362,40.2489430566856));
#70896=CARTESIAN_POINT('Ctrl Pts',(29.9268444997616,23.3530876883875,40.3758738259163));
#70897=CARTESIAN_POINT('Ctrl Pts',(27.9841645335578,22.2160513018329,40.5028045951471));
#70898=CARTESIAN_POINT('Ctrl Pts',(27.8843684200537,19.9672965505993,40.6297353643778));
#70899=CARTESIAN_POINT('Ctrl Pts',(29.718690116198,18.6626429143762,40.7566661336087));
#70900=CARTESIAN_POINT('Ctrl Pts',(31.8101862946221,19.4948093226364,40.8835969028394));
#70901=CARTESIAN_POINT('Ctrl Pts',(32.246803814426,21.7030263266837,41.0105276720702));
#70902=CARTESIAN_POINT('Ctrl Pts',(30.6293854077811,23.2685341973996,41.1374584413009));
#70903=CARTESIAN_POINT('Ctrl Pts',(28.4365806542482,22.7601401494908,41.2643892105318));
#70904=CARTESIAN_POINT('Ctrl Pts',(27.6730593491541,20.6426198041178,41.3913199797624));
#70905=CARTESIAN_POINT('Ctrl Pts',(29.0368353476819,18.8518176875265,41.5182507489933));
#70906=CARTESIAN_POINT('Ctrl Pts',(31.2811398483962,19.0248913735642,41.645181518224));
#70907=CARTESIAN_POINT('Ctrl Pts',(32.3542218082372,21.0036162940384,41.7721122874547));
#70908=CARTESIAN_POINT('Ctrl Pts',(31.275065932358,22.979035182425,41.8990430566856));
#70909=CARTESIAN_POINT('Ctrl Pts',(29.0302403149823,23.1452131736336,42.0259738259164));
#70910=CARTESIAN_POINT('Ctrl Pts',(27.6719723917006,21.3502297447993,42.152904595147));
#70911=CARTESIAN_POINT('Ctrl Pts',(28.4419954936812,19.2350650826142,42.2798353643778));
#70912=CARTESIAN_POINT('Ctrl Pts',(30.6363517355519,18.7334100559325,42.4067661336086));
#70913=CARTESIAN_POINT('Ctrl Pts',(32.248953076618,20.3038796160475,42.5336969028394));
#70914=CARTESIAN_POINT('Ctrl Pts',(31.8055534525214,22.5107446487501,42.6606276720701));
#70915=CARTESIAN_POINT('Ctrl Pts',(29.7115108834014,23.3364820749677,42.7875584413009));
#70916=CARTESIAN_POINT('Ctrl Pts',(27.8812053667529,22.026198491415,42.9144892105316));
#70917=CARTESIAN_POINT('Ctrl Pts',(27.9879107601844,19.7777624630598,43.0414199797625));
#70918=CARTESIAN_POINT('Ctrl Pts',(29.9340723271378,18.6466966302693,43.1683507489932));
#70919=CARTESIAN_POINT('Ctrl Pts',(31.9405109625326,19.6670363195586,43.295281518224));
#70920=CARTESIAN_POINT('Ctrl Pts',(32.1729160983978,21.9059613525467,43.4222122874547));
#70921=CARTESIAN_POINT('Ctrl Pts',(30.4188569724588,23.3166829356786,43.5491430566855));
#70922=CARTESIAN_POINT('Ctrl Pts',(28.2818306001745,22.6094253803939,43.6760738259163));
#70923=CARTESIAN_POINT('Ctrl Pts',(27.7156546319436,20.4309450153696,43.8030045951471));
#70924=CARTESIAN_POINT('Ctrl Pts',(29.237646482592,18.7724565350037,43.9299353643778));
#70925=CARTESIAN_POINT('Ctrl Pts',(31.4569638984824,19.1508787755826,44.0568661336086));
#70926=CARTESIAN_POINT('Ctrl Pts',(32.3435569293119,21.218803852504,44.1837969028393));
#70927=CARTESIAN_POINT('Ctrl Pts',(31.0892046533254,23.0886518498259,44.3107276720702));
#70928=CARTESIAN_POINT('Ctrl Pts',(28.8358915603223,23.0450606028084,44.4376584413009));
#70929=CARTESIAN_POINT('Ctrl Pts',(28.049158514414,21.7755148832423,44.5222789541214));
#70930=CARTESIAN_POINT('Ctrl Pts',(28.0110801632598,21.114588912007,44.5645892105317));
#70931=CARTESIAN_POINT('Ctrl Pts',(31.0493358146879,22.7002587726697,44.3));
#70932=CARTESIAN_POINT('Ctrl Pts',(31.0110837864123,22.7305054804131,44.3));
#70933=CARTESIAN_POINT('Ctrl Pts',(30.9717244691516,22.7591991002977,44.3));
#70934=CARTESIAN_POINT('Ctrl Pts',(30.9313170587865,22.7862512397935,44.3));
#70935=CARTESIAN_POINT('Ctrl Pts',(30.8717553609692,22.8261268800139,44.3));
#70936=CARTESIAN_POINT('Ctrl Pts',(30.8099181934742,22.8624382115192,44.3));
#70937=CARTESIAN_POINT('Ctrl Pts',(30.7461536935897,22.8952427892732,44.3));
#70938=CARTESIAN_POINT('Ctrl Pts',(30.710432840364,22.9136199036425,44.3));
#70939=CARTESIAN_POINT('Ctrl Pts',(30.6741064149253,22.93089587639,44.3));
#70940=CARTESIAN_POINT('Ctrl Pts',(30.6372309081889,22.9470757234022,44.3));
#70941=CARTESIAN_POINT('Ctrl Pts',(30.6230043527359,22.9533179017778,44.3));
#70942=CARTESIAN_POINT('Ctrl Pts',(30.6086960404744,22.9593968914265,44.3));
#70943=CARTESIAN_POINT('Ctrl Pts',(30.5943091070883,22.9653128279144,44.3));
#70944=CARTESIAN_POINT('Ctrl Pts',(30.5807067611259,22.9709061404461,44.3));
#70945=CARTESIAN_POINT('Ctrl Pts',(30.5670423559514,22.9763502989973,44.3));
#70946=CARTESIAN_POINT('Ctrl Pts',(30.5533210882546,22.9816450286663,44.3));
#70947=CARTESIAN_POINT('Ctrl Pts',(30.4832690776367,23.0086765294862,44.3));
#70948=CARTESIAN_POINT('Ctrl Pts',(30.4117194145467,23.0318241057179,44.3));
#70949=CARTESIAN_POINT('Ctrl Pts',(30.3390502812968,23.0511463865923,44.3));
#70950=CARTESIAN_POINT('Ctrl Pts',(30.2796354790101,23.0669444214185,44.3));
#70951=CARTESIAN_POINT('Ctrl Pts',(30.2194713251798,23.0801846338831,44.3));
#70952=CARTESIAN_POINT('Ctrl Pts',(30.1587495264957,23.0908780764479,44.3));
#70953=CARTESIAN_POINT('Ctrl Pts',(30.1344248905864,23.0951617785555,44.3));
#70954=CARTESIAN_POINT('Ctrl Pts',(30.1100106469206,23.0990365727744,44.3));
#70955=CARTESIAN_POINT('Ctrl Pts',(30.0855187098372,23.1025022765372,44.3));
#70956=CARTESIAN_POINT('Ctrl Pts',(30.0688128119039,23.1048662256659,44.3));
#70957=CARTESIAN_POINT('Ctrl Pts',(30.0520683767963,23.107039987055,44.3));
#70958=CARTESIAN_POINT('Ctrl Pts',(30.0353127006666,23.1090209570334,44.3));
#70959=CARTESIAN_POINT('Ctrl Pts',(29.9579615115999,23.1181659406286,44.3));
#70960=CARTESIAN_POINT('Ctrl Pts',(29.8802676556082,23.1232220884979,44.3));
#70961=CARTESIAN_POINT('Ctrl Pts',(29.8026183201236,23.1242482721955,44.3));
#70962=CARTESIAN_POINT('Ctrl Pts',(29.7236225788762,23.1252922494728,44.3));
#70963=CARTESIAN_POINT('Ctrl Pts',(29.6446719430159,23.1221656183407,44.3));
#70964=CARTESIAN_POINT('Ctrl Pts',(29.5661502640416,23.114882161993,44.3));
#70965=CARTESIAN_POINT('Ctrl Pts',(29.5085211535759,23.1095366432023,44.3));
#70966=CARTESIAN_POINT('Ctrl Pts',(29.4511225255262,23.1019510687179,44.3));
#70967=CARTESIAN_POINT('Ctrl Pts',(29.3941029595966,23.0921133067172,44.3));
#70968=CARTESIAN_POINT('Ctrl Pts',(29.3510914822676,23.0846924035525,44.3));
#70969=CARTESIAN_POINT('Ctrl Pts',(29.3082956236541,23.0759896795228,44.3));
#70970=CARTESIAN_POINT('Ctrl Pts',(29.265779522772,23.0659940680441,44.3));
#70971=CARTESIAN_POINT('Ctrl Pts',(29.2536330171228,23.0631384028073,44.3));
#70972=CARTESIAN_POINT('Ctrl Pts',(29.241507116384,23.0601766100956,44.3));
#70973=CARTESIAN_POINT('Ctrl Pts',(29.2294106201817,23.0571102122805,44.3));
#70974=CARTESIAN_POINT('Ctrl Pts',(29.1508116985187,23.0371858013084,44.3));
#70975=CARTESIAN_POINT('Ctrl Pts',(29.0736725133479,23.0129060533399,44.3));
#70976=CARTESIAN_POINT('Ctrl Pts',(28.9983903470095,22.9843016580501,44.3));
#70977=CARTESIAN_POINT('Ctrl Pts',(28.9641457091262,22.9712899820289,44.3));
#70978=CARTESIAN_POINT('Ctrl Pts',(28.9302851512349,22.9573827579083,44.3));
#70979=CARTESIAN_POINT('Ctrl Pts',(28.8968456509869,22.9425793284446,44.3));
#70980=CARTESIAN_POINT('Ctrl Pts',(28.8251173759661,22.9108257300968,44.3));
#70981=CARTESIAN_POINT('Ctrl Pts',(28.755325360237,22.8749522429844,44.3));
#70982=CARTESIAN_POINT('Ctrl Pts',(28.6876160787102,22.8352802507896,44.3));
#70983=CARTESIAN_POINT('Ctrl Pts',(28.6199067971835,22.7956082585949,44.3));
#70984=CARTESIAN_POINT('Ctrl Pts',(28.554279656942,22.7521371933869,44.3));
#70985=CARTESIAN_POINT('Ctrl Pts',(28.4908994911728,22.7051394630327,44.3));
#70986=CARTESIAN_POINT('Ctrl Pts',(28.4802385188713,22.6972341271053,44.3));
#70987=CARTESIAN_POINT('Ctrl Pts',(28.4696392286813,22.6892274062858,44.3));
#70988=CARTESIAN_POINT('Ctrl Pts',(28.4591088034363,22.6811253616606,44.3));
#70989=CARTESIAN_POINT('Ctrl Pts',(28.3951127315144,22.6318871762609,44.3));
#70990=CARTESIAN_POINT('Ctrl Pts',(28.3338332975407,22.5792690281287,44.3));
#70991=CARTESIAN_POINT('Ctrl Pts',(28.2754113048987,22.5236317699283,44.3));
#70992=CARTESIAN_POINT('Ctrl Pts',(28.2159087924481,22.4669654958237,44.3));
#70993=CARTESIAN_POINT('Ctrl Pts',(28.1593697260286,22.4071669102395,44.3));
#70994=CARTESIAN_POINT('Ctrl Pts',(28.1059614101741,22.3445654070193,44.3));
#70995=CARTESIAN_POINT('Ctrl Pts',(28.0519240633645,22.2812265975814,44.3));
#70996=CARTESIAN_POINT('Ctrl Pts',(28.0010909162046,22.215017840663,44.3));
#70997=CARTESIAN_POINT('Ctrl Pts',(27.95366470885,22.1462362325089,44.3));
#70998=CARTESIAN_POINT('Ctrl Pts',(27.9242510796939,22.1035780308972,44.3));
#70999=CARTESIAN_POINT('Ctrl Pts',(27.8961485348881,22.0599293588499,44.3));
#71000=CARTESIAN_POINT('Ctrl Pts',(27.8694129519346,22.0153543689321,44.3));
#71001=CARTESIAN_POINT('Ctrl Pts',(27.8627684362021,22.0042762778988,44.3));
#71002=CARTESIAN_POINT('Ctrl Pts',(27.856213317223,21.9931491635314,44.3));
#71003=CARTESIAN_POINT('Ctrl Pts',(27.8497487774402,21.9819753686283,44.3));
#71004=CARTESIAN_POINT('Ctrl Pts',(27.8067383584659,21.9076329380046,44.3));
#71005=CARTESIAN_POINT('Ctrl Pts',(27.7677258289858,21.8312122550966,44.3));
#71006=CARTESIAN_POINT('Ctrl Pts',(27.732887393996,21.7530632053734,44.3));
#71007=CARTESIAN_POINT('Ctrl Pts',(27.6980144559037,21.6748367588131,44.3));
#71008=CARTESIAN_POINT('Ctrl Pts',(27.6673231902278,21.5948777547204,44.3));
#71009=CARTESIAN_POINT('Ctrl Pts',(27.6410257761963,21.5134989584412,44.3));
#71010=CARTESIAN_POINT('Ctrl Pts',(27.6152975322414,21.4338814903161,44.3));
#71011=CARTESIAN_POINT('Ctrl Pts',(27.5937744971102,21.3529042062414,44.3));
#71012=CARTESIAN_POINT('Ctrl Pts',(27.5766978863451,21.2708353686905,44.3));
#71013=CARTESIAN_POINT('Ctrl Pts',(27.5677489591492,21.2278275340327,44.3));
#71014=CARTESIAN_POINT('Ctrl Pts',(27.5600218842896,21.1845195934477,44.3));
#71015=CARTESIAN_POINT('Ctrl Pts',(27.5535569140831,21.1409484919019,44.3));
#71016=CARTESIAN_POINT('Origin',(29.3411117931064,21.1369041098113,36.4999999999305));
#71017=CARTESIAN_POINT('Origin',(30.,21.,44.3));
#71018=CARTESIAN_POINT('',(28.4205166578229,19.1264518629656,44.3));
#71019=CARTESIAN_POINT('Origin',(30.,21.,44.3));
#71020=CARTESIAN_POINT('Ctrl Pts',(28.4205166578229,19.1264518629657,44.3));
#71021=CARTESIAN_POINT('Ctrl Pts',(28.4546614288766,19.1023864633534,44.3));
#71022=CARTESIAN_POINT('Ctrl Pts',(28.4894415473359,19.079285885032,44.3));
#71023=CARTESIAN_POINT('Ctrl Pts',(28.524842571324,19.0571918940411,44.3));
#71024=CARTESIAN_POINT('Ctrl Pts',(28.5971358507719,19.012073225571,44.3));
#71025=CARTESIAN_POINT('Ctrl Pts',(28.6720177454898,18.9711491070475,44.3));
#71026=CARTESIAN_POINT('Ctrl Pts',(28.7490901216485,18.934435204942,44.3));
#71027=CARTESIAN_POINT('Ctrl Pts',(28.7880521274008,18.9158754130124,44.3));
#71028=CARTESIAN_POINT('Ctrl Pts',(28.8275741586732,18.8983923694088,44.3));
#71029=CARTESIAN_POINT('Ctrl Pts',(28.8676055138014,18.8819930200461,44.3));
#71030=CARTESIAN_POINT('Ctrl Pts',(28.888102699806,18.873596089361,44.3));
#71031=CARTESIAN_POINT('Ctrl Pts',(28.9087334189042,18.8654833271773,44.3));
#71032=CARTESIAN_POINT('Ctrl Pts',(28.9294908535282,18.8576560003214,44.3));
#71033=CARTESIAN_POINT('Ctrl Pts',(28.9441432078653,18.852130810495,44.3));
#71034=CARTESIAN_POINT('Ctrl Pts',(28.9588573914148,18.8467484283512,44.3));
#71035=CARTESIAN_POINT('Ctrl Pts',(28.9736195638014,18.8415130807057,44.3));
#71036=CARTESIAN_POINT('Ctrl Pts',(29.0534511507612,18.8132011155095,44.3));
#71037=CARTESIAN_POINT('Ctrl Pts',(29.134775488115,18.7891505943989,44.3));
#71038=CARTESIAN_POINT('Ctrl Pts',(29.2172006713952,18.769378007905,44.3));
#71039=CARTESIAN_POINT('Ctrl Pts',(29.2995426019427,18.7496253925144,44.3));
#71040=CARTESIAN_POINT('Ctrl Pts',(29.3829842205534,18.7341421254923,44.3));
#71041=CARTESIAN_POINT('Ctrl Pts',(29.4671329462824,18.7229959840501,44.3));
#71042=CARTESIAN_POINT('Ctrl Pts',(29.4793170973916,18.7213821001744,44.3));
#71043=CARTESIAN_POINT('Ctrl Pts',(29.491516053808,18.7198592314163,44.3));
#71044=CARTESIAN_POINT('Ctrl Pts',(29.5037286001147,18.7184276719127,44.3));
#71045=CARTESIAN_POINT('Ctrl Pts',(29.517902907794,18.7167661539658,44.3));
#71046=CARTESIAN_POINT('Ctrl Pts',(29.5320955225091,18.7152276354238,44.3));
#71047=CARTESIAN_POINT('Ctrl Pts',(29.5463045291254,18.7138126137682,44.3));
#71048=CARTESIAN_POINT('Ctrl Pts',(29.5608591182573,18.7123631768464,44.3));
#71049=CARTESIAN_POINT('Ctrl Pts',(29.5754224087203,18.7110441895149,44.3));
#71050=CARTESIAN_POINT('Ctrl Pts',(29.5899879093375,18.7098560519243,44.3));
#71051=CARTESIAN_POINT('Ctrl Pts',(29.672786509973,18.7031020012086,44.3));
#71052=CARTESIAN_POINT('Ctrl Pts',(29.7557033576394,18.7005674053427,44.3));
#71053=CARTESIAN_POINT('Ctrl Pts',(29.8383717954221,18.7022736216555,44.3));
#71054=CARTESIAN_POINT('Ctrl Pts',(29.9192747629738,18.7039433999492,44.3));
#71055=CARTESIAN_POINT('Ctrl Pts',(29.9999407278769,18.7096750302976,44.3));
#71056=CARTESIAN_POINT('Ctrl Pts',(30.0800151893485,18.7195360765726,44.3));
#71057=CARTESIAN_POINT('Ctrl Pts',(30.1583858483894,18.7291873022093,44.3));
#71058=CARTESIAN_POINT('Ctrl Pts',(30.2361906578794,18.7427942913507,44.3));
#71059=CARTESIAN_POINT('Ctrl Pts',(30.3130747015946,18.760463173912,44.3));
#71060=CARTESIAN_POINT('Ctrl Pts',(30.3469544935414,18.7682491596144,44.3));
#71061=CARTESIAN_POINT('Ctrl Pts',(30.380655124679,18.776824439382,44.3));
#71062=CARTESIAN_POINT('Ctrl Pts',(30.4141442282618,18.7862006657701,44.3));
#71063=CARTESIAN_POINT('Ctrl Pts',(30.427620745083,18.7899737996889,44.3));
#71064=CARTESIAN_POINT('Ctrl Pts',(30.4410643696255,18.7938771640174,44.3));
#71065=CARTESIAN_POINT('Ctrl Pts',(30.4544553355144,18.7979060130015,44.3));
#71066=CARTESIAN_POINT('Ctrl Pts',(30.5292896225546,18.820420896828,44.3));
#71067=CARTESIAN_POINT('Ctrl Pts',(30.6026067169376,18.8468848998915,44.3));
#71068=CARTESIAN_POINT('Ctrl Pts',(30.6740806949432,18.8773535792392,44.3));
#71069=CARTESIAN_POINT('Ctrl Pts',(30.7023424983408,18.8894013181442,44.3));
#71070=CARTESIAN_POINT('Ctrl Pts',(30.730315878025,18.9020757018371,44.3));
#71071=CARTESIAN_POINT('Ctrl Pts',(30.7579795342966,18.9153821277604,44.3));
#71072=CARTESIAN_POINT('Ctrl Pts',(30.8296349957725,18.9498489415745,44.3));
#71073=CARTESIAN_POINT('Ctrl Pts',(30.8992151722481,18.9885538331303,44.3));
#71074=CARTESIAN_POINT('Ctrl Pts',(30.9664943099138,19.0311976270323,44.3));
#71075=CARTESIAN_POINT('Ctrl Pts',(31.031817757109,19.0726018381415,44.3));
#71076=CARTESIAN_POINT('Ctrl Pts',(31.0949723123221,19.1177202684067,44.3));
#71077=CARTESIAN_POINT('Ctrl Pts',(31.1557122805128,19.1663052414586,44.3));
#71078=CARTESIAN_POINT('Ctrl Pts',(31.1699003354004,19.1776540499106,44.3));
#71079=CARTESIAN_POINT('Ctrl Pts',(31.1839610180611,19.1891960925353,44.3));
#71080=CARTESIAN_POINT('Ctrl Pts',(31.1978653013046,19.2009063118251,44.3));
#71081=CARTESIAN_POINT('Ctrl Pts',(31.2573151687879,19.2509751267932,44.3));
#71082=CARTESIAN_POINT('Ctrl Pts',(31.3139848039203,19.3041725875463,44.3));
#71083=CARTESIAN_POINT('Ctrl Pts',(31.3676843811118,19.3601986999375,44.3));
#71084=CARTESIAN_POINT('Ctrl Pts',(31.4211957053017,19.4160284032622,44.3));
#71085=CARTESIAN_POINT('Ctrl Pts',(31.471758236847,19.4746678992268,44.3));
#71086=CARTESIAN_POINT('Ctrl Pts',(31.5191413084655,19.5358480817005,44.3));
#71087=CARTESIAN_POINT('Ctrl Pts',(31.5661269832405,19.5965151524116,44.3));
#71088=CARTESIAN_POINT('Ctrl Pts',(31.6099867130907,19.6596813525084,44.3));
#71089=CARTESIAN_POINT('Ctrl Pts',(31.6504468767739,19.7250980707919,44.3));
#71090=CARTESIAN_POINT('Ctrl Pts',(31.665885468332,19.7500594625094,44.3));
#71091=CARTESIAN_POINT('Ctrl Pts',(31.6808285446354,19.7753486039029,44.3));
#71092=CARTESIAN_POINT('Ctrl Pts',(31.6952588227872,19.8009518122182,44.3));
#71093=CARTESIAN_POINT('Ctrl Pts',(31.7013523222933,19.8117633250375,44.3));
#71094=CARTESIAN_POINT('Ctrl Pts',(31.7073543860773,19.8226310444429,44.3));
#71095=CARTESIAN_POINT('Ctrl Pts',(31.7132568737193,19.8335409018929,44.3));
#71096=CARTESIAN_POINT('Ctrl Pts',(31.7489430038996,19.8995013268572,44.3));
#71097=CARTESIAN_POINT('Ctrl Pts',(31.7810594676341,19.9671166497836,44.3));
#71098=CARTESIAN_POINT('Ctrl Pts',(31.8094014527161,20.0361358411783,44.3));
#71099=CARTESIAN_POINT('Ctrl Pts',(31.8372817751033,20.1040307787216,44.3));
#71100=CARTESIAN_POINT('Ctrl Pts',(31.8615098401969,20.1732850438433,44.3));
#71101=CARTESIAN_POINT('Ctrl Pts',(31.8818416939127,20.243668178961,44.3));
#71102=CARTESIAN_POINT('Ctrl Pts',(31.9015211854442,20.3117930204471,44.3));
#71103=CARTESIAN_POINT('Ctrl Pts',(31.9175505455949,20.3809761123184,44.3));
#71104=CARTESIAN_POINT('Ctrl Pts',(31.9296601688495,20.4510057916981,44.3));
#71105=CARTESIAN_POINT('Ctrl Pts',(31.9357076145878,20.4859780346176,44.3));
#71106=CARTESIAN_POINT('Ctrl Pts',(31.9407767358369,20.5211613068948,44.3));
#71107=CARTESIAN_POINT('Ctrl Pts',(31.9448291324621,20.5565282331122,44.3));
#71108=CARTESIAN_POINT('Ctrl Pts',(29.1264558385116,22.7892573294893,35.7842713731578));
#71109=CARTESIAN_POINT('Ctrl Pts',(28.5312306963436,22.4986588565127,35.826627728308));
#71110=CARTESIAN_POINT('Ctrl Pts',(27.6641321376413,21.2811530742106,35.9113404386083));
#71111=CARTESIAN_POINT('Ctrl Pts',(28.498480258771,19.1855515705045,36.0384095040588));
#71112=CARTESIAN_POINT('Ctrl Pts',(30.7107013872026,18.7565854023573,36.1654785695093));
#71113=CARTESIAN_POINT('Ctrl Pts',(32.2706914918877,20.3804476459957,36.2925476349598));
#71114=CARTESIAN_POINT('Ctrl Pts',(31.751265422737,22.5729299246014,36.4196167004103));
#71115=CARTESIAN_POINT('Ctrl Pts',(29.6273304332075,23.3240196151812,36.5466857658608));
#71116=CARTESIAN_POINT('Ctrl Pts',(27.8449208232258,21.9465121681938,36.6737548313113));
#71117=CARTESIAN_POINT('Ctrl Pts',(28.0365506611368,19.7018375639597,36.8008238967618));
#71118=CARTESIAN_POINT('Ctrl Pts',(30.0267931275245,18.6463840233588,36.9278929622123));
#71119=CARTESIAN_POINT('Ctrl Pts',(31.992473836526,19.746876227632,37.0549620276628));
#71120=CARTESIAN_POINT('Ctrl Pts',(32.1330009690077,21.9952822113242,37.1820310931133));
#71121=CARTESIAN_POINT('Ctrl Pts',(30.3196338647694,23.3319730130521,37.3091001585638));
#71122=CARTESIAN_POINT('Ctrl Pts',(28.2134753232459,22.5325142575818,37.4361692240143));
#71123=CARTESIAN_POINT('Ctrl Pts',(27.7438231346904,20.3292267213969,37.5632382894648));
#71124=CARTESIAN_POINT('Ctrl Pts',(29.340893789684,18.7403876454215,37.6903073549153));
#71125=CARTESIAN_POINT('Ctrl Pts',(31.5417242248616,19.2214173377329,37.8173764203657));
#71126=CARTESIAN_POINT('Ctrl Pts',(32.3302914952649,21.3316796671695,37.9444454858163));
#71127=CARTESIAN_POINT('Ctrl Pts',(30.984245307654,23.1381138461734,38.0715145512667));
#71128=CARTESIAN_POINT('Ctrl Pts',(28.7366024171385,22.9859749016701,38.1985836167173));
#71129=CARTESIAN_POINT('Ctrl Pts',(27.6462676828056,21.0146263453323,38.3256526821677));
#71130=CARTESIAN_POINT('Ctrl Pts',(28.7120188055034,19.0298796558089,38.4527217476182));
#71131=CARTESIAN_POINT('Ctrl Pts',(30.9575973860193,18.8498193123516,38.5797908130687));
#71132=CARTESIAN_POINT('Ctrl Pts',(32.3259894860523,20.6393857303374,38.7068598785192));
#71133=CARTESIAN_POINT('Ctrl Pts',(31.563708960251,22.7592850894379,38.8339289439697));
#71134=CARTESIAN_POINT('Ctrl Pts',(29.3690264853313,23.2676291945582,38.9609980094202));
#71135=CARTESIAN_POINT('Ctrl Pts',(27.752333722787,21.69876036383,39.0880670748707));
#71136=CARTESIAN_POINT('Ctrl Pts',(28.1945672948102,19.4898071359688,39.2151361403212));
#71137=CARTESIAN_POINT('Ctrl Pts',(30.2906286522575,18.6642335891045,39.3422052057717));
#71138=CARTESIAN_POINT('Ctrl Pts',(32.1204658857473,19.9782886087098,39.4692742712222));
#71139=CARTESIAN_POINT('Ctrl Pts',(32.0078959666568,22.2282603660349,39.5963433366727));
#71140=CARTESIAN_POINT('Ctrl Pts',(30.0560361474382,23.3531106412359,39.7234124021232));
#71141=CARTESIAN_POINT('Ctrl Pts',(28.0528456209794,22.32244454098,39.8504814675737));
#71142=CARTESIAN_POINT('Ctrl Pts',(27.8333039701667,20.0803815715138,39.9775505330242));
#71143=CARTESIAN_POINT('Ctrl Pts',(29.5985176007606,18.6807152777617,40.1046195984747));
#71144=CARTESIAN_POINT('Ctrl Pts',(31.7315005452354,19.4055798541298,40.2316886639252));
#71145=CARTESIAN_POINT('Ctrl Pts',(32.2783796686896,21.5909787009862,40.3587577293757));
#71146=CARTESIAN_POINT('Ctrl Pts',(30.7381981162433,23.2350242237756,40.4858267948262));
#71147=CARTESIAN_POINT('Ctrl Pts',(28.5218060618448,22.8317238931978,40.6128958602767));
#71148=CARTESIAN_POINT('Ctrl Pts',(27.6594817609504,20.7505122999901,40.7399649257271));
#71149=CARTESIAN_POINT('Ctrl Pts',(28.9411388364606,18.8978385466649,40.8670339911777));
#71150=CARTESIAN_POINT('Ctrl Pts',(31.1927428992058,18.9708045643224,40.9941030566281));
#71151=CARTESIAN_POINT('Ctrl Pts',(32.351760491343,20.9025714026366,41.1211721220787));
#71152=CARTESIAN_POINT('Ctrl Pts',(31.3564984833804,22.9235856110073,41.2482411875291));
#71153=CARTESIAN_POINT('Ctrl Pts',(29.1186452257674,23.1825406073307,41.3753102529796));
#71154=CARTESIAN_POINT('Ctrl Pts',(27.6881380449832,21.4422262364366,41.5023793184301));
#71155=CARTESIAN_POINT('Ctrl Pts',(28.3753622714282,19.2968200391992,41.6294483838806));
#71156=CARTESIAN_POINT('Ctrl Pts',(30.5508009281952,18.711575194925,41.7565174493311));
#71157=CARTESIAN_POINT('Ctrl Pts',(32.2216902586076,20.2225926696691,41.8835865147816));
#71158=CARTESIAN_POINT('Ctrl Pts',(31.8574480007175,22.4457373791487,42.0106555802321));
#71159=CARTESIAN_POINT('Ctrl Pts',(29.7917305188365,23.3445455162426,42.1377246456825));
#71160=CARTESIAN_POINT('Ctrl Pts',(27.9167937061589,22.0956830788796,42.2647937111331));
#71161=CARTESIAN_POINT('Ctrl Pts',(27.9501334154122,19.8431439264837,42.3918627765836));
#71162=CARTESIAN_POINT('Ctrl Pts',(29.8612088710918,18.6503174977494,42.5189318420341));
#71163=CARTESIAN_POINT('Ctrl Pts',(31.8994218278085,19.6098679593695,42.6460009074846));
#71164=CARTESIAN_POINT('Ctrl Pts',(32.1977085324443,21.8428173868236,42.7730699729351));
#71165=CARTESIAN_POINT('Ctrl Pts',(30.4828351379126,23.303725253489,42.9001390383856));
#71166=CARTESIAN_POINT('Ctrl Pts',(28.3256639434058,22.6543487986828,43.0272081038361));
#71167=CARTESIAN_POINT('Ctrl Pts',(27.7022464386769,20.4895544998625,43.1542771692865));
#71168=CARTESIAN_POINT('Ctrl Pts',(29.1836082129126,18.7923171725529,43.281346234737));
#71169=CARTESIAN_POINT('Ctrl Pts',(31.4128651827133,19.1174316697178,43.4084153001876));
#71170=CARTESIAN_POINT('Ctrl Pts',(32.3477828809716,21.166929091464,43.535484365638));
#71171=CARTESIAN_POINT('Ctrl Pts',(31.1322944104254,23.0637220008276,43.6625534310885));
#71172=CARTESIAN_POINT('Ctrl Pts',(28.8791307244882,23.0696707559168,43.7896224965391));
#71173=CARTESIAN_POINT('Ctrl Pts',(27.6536416772529,21.1805772409905,43.9166915619895));
#71174=CARTESIAN_POINT('Ctrl Pts',(28.5756138853417,19.124391076752,44.0437606274401));
#71175=CARTESIAN_POINT('Ctrl Pts',(30.8065507606822,18.7896800661229,44.1708475287837));
#71176=CARTESIAN_POINT('Ctrl Pts',(31.794437854879,19.912011627325,44.2555780749772));
#71177=CARTESIAN_POINT('Ctrl Pts',(31.9414666005005,20.5581532204799,44.2979522660205));
#71178=CARTESIAN_POINT('Ctrl Pts',(29.0588050875662,22.9278245677711,35.8732985293678));
#71179=CARTESIAN_POINT('Ctrl Pts',(28.4174833315984,22.6147209876834,35.915654884518));
#71180=CARTESIAN_POINT('Ctrl Pts',(27.48323319519,21.3029266918931,36.0003675948183));
#71181=CARTESIAN_POINT('Ctrl Pts',(28.3821965692544,19.0450334327634,36.1274366602689));
#71182=CARTESIAN_POINT('Ctrl Pts',(30.7657409429135,18.5828464102108,36.2545057257193));
#71183=CARTESIAN_POINT('Ctrl Pts',(32.4465429157353,20.3324670356887,36.3815747911698));
#71184=CARTESIAN_POINT('Ctrl Pts',(31.8868904159268,22.6947439041059,36.5086438566203));
#71185=CARTESIAN_POINT('Ctrl Pts',(29.5984694125981,23.5040009820202,36.6357129220708));
#71186=CARTESIAN_POINT('Ctrl Pts',(27.6780228790999,22.0198138531919,36.7627819875213));
#71187=CARTESIAN_POINT('Ctrl Pts',(27.8844932974987,19.6013026768652,36.8898510529718));
#71188=CARTESIAN_POINT('Ctrl Pts',(30.0288680943975,18.4641105960079,37.0169201184223));
#71189=CARTESIAN_POINT('Ctrl Pts',(32.1467789732582,19.6498293146473,37.1439891838728));
#71190=CARTESIAN_POINT('Ctrl Pts',(32.2981890884896,22.0723608433696,37.2710582493233));
#71191=CARTESIAN_POINT('Ctrl Pts',(30.3443875886594,23.5125703228076,37.3981273147737));
#71192=CARTESIAN_POINT('Ctrl Pts',(28.075119712513,22.6511982863129,37.5251963802243));
#71193=CARTESIAN_POINT('Ctrl Pts',(27.5690957815319,20.2772793579868,37.6522654456748));
#71194=CARTESIAN_POINT('Ctrl Pts',(29.2898499706689,18.5653942342443,37.7793345111252));
#71195=CARTESIAN_POINT('Ctrl Pts',(31.661121510266,19.0836767883417,37.9064035765758));
#71196=CARTESIAN_POINT('Ctrl Pts',(32.5107585815627,21.3573662661379,38.0334726420262));
#71197=CARTESIAN_POINT('Ctrl Pts',(31.0604691977706,23.3036979272963,38.1605417074767));
#71198=CARTESIAN_POINT('Ctrl Pts',(28.6387598592103,23.1397767349144,38.2876107729272));
#71199=CARTESIAN_POINT('Ctrl Pts',(27.4639852455773,21.0157590679684,38.4146798383777));
#71200=CARTESIAN_POINT('Ctrl Pts',(28.6122723944429,18.8773056628579,38.5417489038283));
#71201=CARTESIAN_POINT('Ctrl Pts',(31.0317575545873,18.6833007268003,38.6688179692787));
#71202=CARTESIAN_POINT('Ctrl Pts',(32.5061234075639,20.6114583201161,38.7958870347292));
#71203=CARTESIAN_POINT('Ctrl Pts',(31.6848088314249,22.8955311576673,38.9229561001797));
#71204=CARTESIAN_POINT('Ctrl Pts',(29.3201613746983,23.4432434618624,39.0500251656302));
#71205=CARTESIAN_POINT('Ctrl Pts',(27.5782654635829,21.7528751589692,39.1770942310807));
#71206=CARTESIAN_POINT('Ctrl Pts',(28.0547473707901,19.3728517651606,39.3041632965312));
#71207=CARTESIAN_POINT('Ctrl Pts',(30.3131360965726,18.4833425034599,39.4312323619817));
#71208=CARTESIAN_POINT('Ctrl Pts',(32.2846832382856,19.8991631953448,39.5583014274322));
#71209=CARTESIAN_POINT('Ctrl Pts',(32.1633954547801,22.3233817574676,39.6853704928827));
#71210=CARTESIAN_POINT('Ctrl Pts',(30.0603758106417,23.5353449333936,39.8124395583332));
#71211=CARTESIAN_POINT('Ctrl Pts',(27.9020502041535,22.4248599313233,39.9395086237837));
#71212=CARTESIAN_POINT('Ctrl Pts',(27.6655063705137,20.0091626451984,40.0665776892342));
#71213=CARTESIAN_POINT('Ctrl Pts',(29.5674251992573,18.501100599955,40.1936467546846));
#71214=CARTESIAN_POINT('Ctrl Pts',(31.865594867322,19.2821015860055,40.3207158201352));
#71215=CARTESIAN_POINT('Ctrl Pts',(32.4548264956743,21.6367464534102,40.4477848855856));
#71216=CARTESIAN_POINT('Ctrl Pts',(30.7953671285406,23.408113431838,40.5748539510361));
#71217=CARTESIAN_POINT('Ctrl Pts',(28.4073288157389,22.9735799118887,40.7019230164867));
#71218=CARTESIAN_POINT('Ctrl Pts',(27.478222674743,20.7311909754351,40.8289920819371));
#71219=CARTESIAN_POINT('Ctrl Pts',(28.8591363962653,18.7350387625254,40.9560611473876));
#71220=CARTESIAN_POINT('Ctrl Pts',(31.2851136760633,18.8136555601958,41.0831302128381));
#71221=CARTESIAN_POINT('Ctrl Pts',(32.5338902224971,20.8950261426877,41.2101992782886));
#71222=CARTESIAN_POINT('Ctrl Pts',(31.4615511471183,23.0725557682465,41.3372683437391));
#71223=CARTESIAN_POINT('Ctrl Pts',(29.0503895897562,23.3515652743872,41.4643374091896));
#71224=CARTESIAN_POINT('Ctrl Pts',(27.5090982159349,21.4764740035234,41.5914064746401));
#71225=CARTESIAN_POINT('Ctrl Pts',(28.2495438329364,19.1649189763531,41.7184755400906));
#71226=CARTESIAN_POINT('Ctrl Pts',(30.5934571533256,18.5343504324337,41.8455446055411));
#71227=CARTESIAN_POINT('Ctrl Pts',(32.3937468311188,20.162387139135,41.9726136709916));
#71228=CARTESIAN_POINT('Ctrl Pts',(32.0012961971001,22.5577010596139,42.0996827364421));
#71229=CARTESIAN_POINT('Ctrl Pts',(29.7756012978757,23.5261164908906,42.2267518018926));
#71230=CARTESIAN_POINT('Ctrl Pts',(27.7554618853241,22.1805371553559,42.3538208673431));
#71231=CARTESIAN_POINT('Ctrl Pts',(27.7913835549026,19.7535523688276,42.4808899327936));
#71232=CARTESIAN_POINT('Ctrl Pts',(29.8504603313968,18.4683486943752,42.607958998244));
#71233=CARTESIAN_POINT('Ctrl Pts',(32.0465206451074,19.5022105785432,42.7350280636946));
#71234=CARTESIAN_POINT('Ctrl Pts',(32.3679078642396,21.9080885335408,42.862097129145));
#71235=CARTESIAN_POINT('Ctrl Pts',(30.5202278206214,23.482134943853,42.9891661945956));
#71236=CARTESIAN_POINT('Ctrl Pts',(28.1959966677748,22.782468181183,43.116235260046));
#71237=CARTESIAN_POINT('Ctrl Pts',(27.5242992200198,20.4500235603596,43.2433043254965));
#71238=CARTESIAN_POINT('Ctrl Pts',(29.1203835702476,18.6213453914907,43.3703733909471));
#71239=CARTESIAN_POINT('Ctrl Pts',(31.5222831089145,18.9716380546215,43.4974424563975));
#71240=CARTESIAN_POINT('Ctrl Pts',(32.5296045700822,21.1798567474316,43.624511521848));
#71241=CARTESIAN_POINT('Ctrl Pts',(31.2199838147322,23.2235448801435,43.7515805872985));
#71242=CARTESIAN_POINT('Ctrl Pts',(28.7923261282892,23.2299543306006,43.878649652749));
#71243=CARTESIAN_POINT('Ctrl Pts',(27.4719303116244,21.1945618642016,44.0057187181995));
#71244=CARTESIAN_POINT('Ctrl Pts',(28.4653037321279,18.9791364259494,44.1327877836501));
#71245=CARTESIAN_POINT('Ctrl Pts',(30.869013274933,18.6185040569998,44.2598746849936));
#71246=CARTESIAN_POINT('Ctrl Pts',(31.9334062937505,19.8277534596486,44.3446052311871));
#71247=CARTESIAN_POINT('Ctrl Pts',(32.0918215330268,20.5239348400532,44.3869794222305));
#71248=CARTESIAN_POINT('Ctrl Pts',(28.9911543366207,23.0663918060528,35.9623256855777));
#71249=CARTESIAN_POINT('Ctrl Pts',(28.303735966853,22.7307831188541,36.0046820407279));
#71250=CARTESIAN_POINT('Ctrl Pts',(27.3023342527386,21.3247003095755,36.0893947510282));
#71251=CARTESIAN_POINT('Ctrl Pts',(28.2659128797378,18.9045152950221,36.2164638164787));
#71252=CARTESIAN_POINT('Ctrl Pts',(30.8207804986244,18.4091074180643,36.3435328819292));
#71253=CARTESIAN_POINT('Ctrl Pts',(32.622394339583,20.2844864253816,36.4706019473797));
#71254=CARTESIAN_POINT('Ctrl Pts',(32.0225154091167,22.8165578836103,36.5976710128302));
#71255=CARTESIAN_POINT('Ctrl Pts',(29.5696083919886,23.6839823488592,36.7247400782807));
#71256=CARTESIAN_POINT('Ctrl Pts',(27.511124934974,22.09311553819,36.8518091437312));
#71257=CARTESIAN_POINT('Ctrl Pts',(27.7324359338606,19.5007677897707,36.9788782091817));
#71258=CARTESIAN_POINT('Ctrl Pts',(30.0309430612705,18.2818371686568,37.1059472746322));
#71259=CARTESIAN_POINT('Ctrl Pts',(32.3010841099903,19.5527824016626,37.2330163400826));
#71260=CARTESIAN_POINT('Ctrl Pts',(32.4633772079716,22.1494394754149,37.3600854055332));
#71261=CARTESIAN_POINT('Ctrl Pts',(30.3691413125495,23.693167632563,37.4871544709836));
#71262=CARTESIAN_POINT('Ctrl Pts',(27.93676410178,22.769882315044,37.6142235364341));
#71263=CARTESIAN_POINT('Ctrl Pts',(27.3943684283736,20.2253319945767,37.7412926018847));
#71264=CARTESIAN_POINT('Ctrl Pts',(29.2388061516538,18.3904008230671,37.8683616673351));
#71265=CARTESIAN_POINT('Ctrl Pts',(31.7805187956705,18.9459362389506,37.9954307327856));
#71266=CARTESIAN_POINT('Ctrl Pts',(32.6912256678607,21.3830528651062,38.1224997982362));
#71267=CARTESIAN_POINT('Ctrl Pts',(31.1366930878873,23.4692820084193,38.2495688636866));
#71268=CARTESIAN_POINT('Ctrl Pts',(28.5409173012823,23.2935785681586,38.3766379291371));
#71269=CARTESIAN_POINT('Ctrl Pts',(27.2817028083489,21.0168917906046,38.5037069945876));
#71270=CARTESIAN_POINT('Ctrl Pts',(28.5125259833826,18.7247316699069,38.6307760600381));
#71271=CARTESIAN_POINT('Ctrl Pts',(31.1059177231553,18.5167821412488,38.7578451254886));
#71272=CARTESIAN_POINT('Ctrl Pts',(32.6862573290757,20.5835309098948,38.8849141909391));
#71273=CARTESIAN_POINT('Ctrl Pts',(31.8059087025989,23.0317772258968,39.0119832563896));
#71274=CARTESIAN_POINT('Ctrl Pts',(29.2712962640653,23.6188577291665,39.1390523218401));
#71275=CARTESIAN_POINT('Ctrl Pts',(27.4041972043789,21.8069899541084,39.2661213872906));
#71276=CARTESIAN_POINT('Ctrl Pts',(27.91492744677,19.2558963943526,39.3931904527411));
#71277=CARTESIAN_POINT('Ctrl Pts',(30.3356435408877,18.3024514178153,39.5202595181916));
#71278=CARTESIAN_POINT('Ctrl Pts',(32.4489005908239,19.82003778198,39.6473285836421));
#71279=CARTESIAN_POINT('Ctrl Pts',(32.3188949429034,22.4185031489004,39.7743976490926));
#71280=CARTESIAN_POINT('Ctrl Pts',(30.0647154738453,23.7175792255511,39.901466714543));
#71281=CARTESIAN_POINT('Ctrl Pts',(27.7512547873278,22.5272753216666,40.0285357799936));
#71282=CARTESIAN_POINT('Ctrl Pts',(27.4977087708607,19.9379437188829,40.155604845444));
#71283=CARTESIAN_POINT('Ctrl Pts',(29.5363327977539,18.3214859221484,40.2826739108945));
#71284=CARTESIAN_POINT('Ctrl Pts',(31.9996891894087,19.1586233178813,40.4097429763451));
#71285=CARTESIAN_POINT('Ctrl Pts',(32.631273322659,21.6825142058343,40.5368120417955));
#71286=CARTESIAN_POINT('Ctrl Pts',(30.8525361408378,23.5812026399005,40.6638811072461));
#71287=CARTESIAN_POINT('Ctrl Pts',(28.2928515696329,23.1154359305797,40.7909501726965));
#71288=CARTESIAN_POINT('Ctrl Pts',(27.2969635885356,20.7118696508799,40.918019238147));
#71289=CARTESIAN_POINT('Ctrl Pts',(28.7771339560702,18.5722389783859,41.0450883035975));
#71290=CARTESIAN_POINT('Ctrl Pts',(31.3774844529208,18.656506556069,41.172157369048));
#71291=CARTESIAN_POINT('Ctrl Pts',(32.7160199536512,20.887480882739,41.2992264344985));
#71292=CARTESIAN_POINT('Ctrl Pts',(31.5666038108562,23.2215259254859,41.426295499949));
#71293=CARTESIAN_POINT('Ctrl Pts',(28.9821339537452,23.5205899414438,41.5533645653995));
#71294=CARTESIAN_POINT('Ctrl Pts',(27.3300583868866,21.5107217706103,41.68043363085));
#71295=CARTESIAN_POINT('Ctrl Pts',(28.1237253944445,19.0330179135071,41.8075026963005));
#71296=CARTESIAN_POINT('Ctrl Pts',(30.636113378456,18.3571256699425,41.934571761751));
#71297=CARTESIAN_POINT('Ctrl Pts',(32.5658034036301,20.102181608601,42.0616408272015));
#71298=CARTESIAN_POINT('Ctrl Pts',(32.1451443934826,22.6696647400793,42.188709892652));
#71299=CARTESIAN_POINT('Ctrl Pts',(29.7594720769148,23.7076874655386,42.3157789581025));
#71300=CARTESIAN_POINT('Ctrl Pts',(27.5941300644893,22.2653912318322,42.442848023553));
#71301=CARTESIAN_POINT('Ctrl Pts',(27.6326336943931,19.6639608111716,42.5699170890035));
#71302=CARTESIAN_POINT('Ctrl Pts',(29.8397117917017,18.286379891001,42.6969861544539));
#71303=CARTESIAN_POINT('Ctrl Pts',(32.1936194624063,19.3945531977169,42.8240552199045));
#71304=CARTESIAN_POINT('Ctrl Pts',(32.5381071960349,21.973359680258,42.9511242853549));
#71305=CARTESIAN_POINT('Ctrl Pts',(30.5576205033301,23.6605446342171,43.0781933508055));
#71306=CARTESIAN_POINT('Ctrl Pts',(28.0663293921438,22.9105875636831,43.2052624162559));
#71307=CARTESIAN_POINT('Ctrl Pts',(27.3463520013628,20.4104926208566,43.3323314817064));
#71308=CARTESIAN_POINT('Ctrl Pts',(29.0571589275827,18.4503736104286,43.4594005471569));
#71309=CARTESIAN_POINT('Ctrl Pts',(31.6317010351155,18.8258444395252,43.5864696126075));
#71310=CARTESIAN_POINT('Ctrl Pts',(32.7114262591928,21.1927844033991,43.7135386780579));
#71311=CARTESIAN_POINT('Ctrl Pts',(31.3076732190389,23.3833677594592,43.8406077435085));
#71312=CARTESIAN_POINT('Ctrl Pts',(28.7055215320902,23.3902379052844,43.9676768089589));
#71313=CARTESIAN_POINT('Ctrl Pts',(27.2902189459959,21.2085464874127,44.0947458744094));
#71314=CARTESIAN_POINT('Ctrl Pts',(28.354993578914,18.8338817751468,44.2218149398599));
#71315=CARTESIAN_POINT('Ctrl Pts',(30.9314757891839,18.4473280478767,44.3489018412036));
#71316=CARTESIAN_POINT('Ctrl Pts',(32.0723747326222,19.7434952919723,44.4336323873971));
#71317=CARTESIAN_POINT('Ctrl Pts',(32.242176465553,20.4897164596265,44.4760065784404));
#71318=CARTESIAN_POINT('Ctrl Pts',(28.9235035856754,23.2049590443345,36.0513528417877));
#71319=CARTESIAN_POINT('Ctrl Pts',(28.1899886021078,22.8468452500248,36.0937091969379));
#71320=CARTESIAN_POINT('Ctrl Pts',(27.1214353102873,21.3464739272579,36.1784219072382));
#71321=CARTESIAN_POINT('Ctrl Pts',(28.1496291902213,18.7639971572809,36.3054909726887));
#71322=CARTESIAN_POINT('Ctrl Pts',(30.8758200543354,18.2353684259178,36.4325600381392));
#71323=CARTESIAN_POINT('Ctrl Pts',(32.7982457634307,20.2365058150745,36.5596291035897));
#71324=CARTESIAN_POINT('Ctrl Pts',(32.1581404023066,22.9383718631148,36.6866981690402));
#71325=CARTESIAN_POINT('Ctrl Pts',(29.5407473713791,23.8639637156981,36.8137672344907));
#71326=CARTESIAN_POINT('Ctrl Pts',(27.3442269908482,22.1664172231879,36.9408362999411));
#71327=CARTESIAN_POINT('Ctrl Pts',(27.5803785702225,19.4002329026764,37.0679053653917));
#71328=CARTESIAN_POINT('Ctrl Pts',(30.0330180281436,18.0995637413059,37.1949744308422));
#71329=CARTESIAN_POINT('Ctrl Pts',(32.4553892467225,19.455735488678,37.3220434962926));
#71330=CARTESIAN_POINT('Ctrl Pts',(32.6285653274533,22.2265181074601,37.4491125617432));
#71331=CARTESIAN_POINT('Ctrl Pts',(30.3938950364395,23.8737649423185,37.5761816271937));
#71332=CARTESIAN_POINT('Ctrl Pts',(27.7984084910471,22.8885663437751,37.7032506926441));
#71333=CARTESIAN_POINT('Ctrl Pts',(27.2196410752151,20.1733846311666,37.8303197580947));
#71334=CARTESIAN_POINT('Ctrl Pts',(29.1877623326388,18.21540741189,37.9573888235451));
#71335=CARTESIAN_POINT('Ctrl Pts',(31.8999160810749,18.8081956895594,38.0844578889956));
#71336=CARTESIAN_POINT('Ctrl Pts',(32.8716927541586,21.4087394640746,38.2115269544461));
#71337=CARTESIAN_POINT('Ctrl Pts',(31.2129169780038,23.6348660895422,38.3385960198966));
#71338=CARTESIAN_POINT('Ctrl Pts',(28.4430747433541,23.4473804014028,38.4656650853471));
#71339=CARTESIAN_POINT('Ctrl Pts',(27.0994203711206,21.0180245132406,38.5927341507976));
#71340=CARTESIAN_POINT('Ctrl Pts',(28.4127795723222,18.5721576769558,38.7198032162481));
#71341=CARTESIAN_POINT('Ctrl Pts',(31.1800778917232,18.3502635556974,38.8468722816986));
#71342=CARTESIAN_POINT('Ctrl Pts',(32.8663912505875,20.5556034996735,38.9739413471491));
#71343=CARTESIAN_POINT('Ctrl Pts',(31.9270085737729,23.1680232941261,39.1010104125996));
#71344=CARTESIAN_POINT('Ctrl Pts',(29.2224311534323,23.7944719964707,39.2280794780501));
#71345=CARTESIAN_POINT('Ctrl Pts',(27.2301289451749,21.8611047492476,39.3551485435006));
#71346=CARTESIAN_POINT('Ctrl Pts',(27.77510752275,19.1389410235446,39.4822176089511));
#71347=CARTESIAN_POINT('Ctrl Pts',(30.3581509852028,18.1215603321707,39.6092866744015));
#71348=CARTESIAN_POINT('Ctrl Pts',(32.6131179433622,19.740912368615,39.7363557398521));
#71349=CARTESIAN_POINT('Ctrl Pts',(32.4743944310268,22.5136245403331,39.8634248053025));
#71350=CARTESIAN_POINT('Ctrl Pts',(30.0690551370489,23.8998135177087,39.9904938707531));
#71351=CARTESIAN_POINT('Ctrl Pts',(27.6004593705019,22.6296907120099,40.1175629362035));
#71352=CARTESIAN_POINT('Ctrl Pts',(27.3299111712076,19.8667247925675,40.2446320016541));
#71353=CARTESIAN_POINT('Ctrl Pts',(29.5052403962506,18.1418712443417,40.3717010671045));
#71354=CARTESIAN_POINT('Ctrl Pts',(32.1337835114953,19.0351450497571,40.4987701325551));
#71355=CARTESIAN_POINT('Ctrl Pts',(32.8077201496436,21.7282819582582,40.6258391980055));
#71356=CARTESIAN_POINT('Ctrl Pts',(30.9097051531351,23.7542918479628,40.7529082634561));
#71357=CARTESIAN_POINT('Ctrl Pts',(28.1783743235269,23.2572919492706,40.8799773289065));
#71358=CARTESIAN_POINT('Ctrl Pts',(27.1157045023283,20.6925483263249,41.0070463943571));
#71359=CARTESIAN_POINT('Ctrl Pts',(28.6951315158749,18.4094391942464,41.1341154598075));
#71360=CARTESIAN_POINT('Ctrl Pts',(31.4698552297785,18.4993575519423,41.261184525258));
#71361=CARTESIAN_POINT('Ctrl Pts',(32.8981496848052,20.8799356227902,41.3882535907085));
#71362=CARTESIAN_POINT('Ctrl Pts',(31.6716564745941,23.3704960827252,41.515322656159));
#71363=CARTESIAN_POINT('Ctrl Pts',(28.9138783177342,23.6896146085003,41.6423917216095));
#71364=CARTESIAN_POINT('Ctrl Pts',(27.1510185578384,21.5449695376971,41.76946078706));
#71365=CARTESIAN_POINT('Ctrl Pts',(27.9979069559526,18.9011168506609,41.8965298525105));
#71366=CARTESIAN_POINT('Ctrl Pts',(30.6787696035865,18.1799009074512,42.023598917961));
#71367=CARTESIAN_POINT('Ctrl Pts',(32.7378599761413,20.0419760780668,42.1506679834115));
#71368=CARTESIAN_POINT('Ctrl Pts',(32.2889925898651,22.7816284205446,42.277737048862));
#71369=CARTESIAN_POINT('Ctrl Pts',(29.743342855954,23.8892584401866,42.4048061143125));
#71370=CARTESIAN_POINT('Ctrl Pts',(27.4327982436545,22.3502453083086,42.531875179763));
#71371=CARTESIAN_POINT('Ctrl Pts',(27.4738838338834,19.5743692535154,42.6589442452135));
#71372=CARTESIAN_POINT('Ctrl Pts',(29.8289632520064,18.1044110876269,42.7860133106639));
#71373=CARTESIAN_POINT('Ctrl Pts',(32.3407182797052,19.2868958168906,42.9130823761145));
#71374=CARTESIAN_POINT('Ctrl Pts',(32.7083065278301,22.0386308269752,43.0401514415649));
#71375=CARTESIAN_POINT('Ctrl Pts',(30.5950131860389,23.8389543245811,43.1672205070154));
#71376=CARTESIAN_POINT('Ctrl Pts',(27.9366621165128,23.0387069461834,43.2942895724659));
#71377=CARTESIAN_POINT('Ctrl Pts',(27.1684047827057,20.3709616813536,43.4213586379164));
#71378=CARTESIAN_POINT('Ctrl Pts',(28.9939342849178,18.2794018293665,43.5484277033669));
#71379=CARTESIAN_POINT('Ctrl Pts',(31.7411189613168,18.680050824429,43.6754967688175));
#71380=CARTESIAN_POINT('Ctrl Pts',(32.8932479483033,21.2057120593666,43.8025658342679));
#71381=CARTESIAN_POINT('Ctrl Pts',(31.3953626233458,23.543190638775,43.9296348997184));
#71382=CARTESIAN_POINT('Ctrl Pts',(28.6187169358912,23.5505214799681,44.0567039651689));
#71383=CARTESIAN_POINT('Ctrl Pts',(27.1085075803675,21.2225311106238,44.1837730306194));
#71384=CARTESIAN_POINT('Ctrl Pts',(28.2446834257002,18.6886271243442,44.3108420960699));
#71385=CARTESIAN_POINT('Ctrl Pts',(30.9939383034346,18.2761520387535,44.4379289974135));
#71386=CARTESIAN_POINT('Ctrl Pts',(32.2113431714937,19.659237124296,44.522659543607));
#71387=CARTESIAN_POINT('Ctrl Pts',(32.3925313980793,20.4554980791997,44.5650337346504));
#71388=CARTESIAN_POINT('Origin',(30.4136184579328,21.5025377287161,36.4999999999269));
#71389=CARTESIAN_POINT('Ctrl Pts',(28.3849103233787,19.1570578993166,44.3));
#71390=CARTESIAN_POINT('Ctrl Pts',(28.3967791015268,19.1468558871996,44.3));
#71391=CARTESIAN_POINT('Ctrl Pts',(28.4086478796748,19.1366538750826,44.3));
#71392=CARTESIAN_POINT('Ctrl Pts',(28.4205166578229,19.1264518629656,44.3));
#71393=CARTESIAN_POINT('Origin',(32.,21.,36.5));
#71394=CARTESIAN_POINT('Origin',(30.,21.,44.3));
#71395=CARTESIAN_POINT('',(27.3495,21.,44.5));
#71396=CARTESIAN_POINT('Origin',(30.,21.,44.5));
#71397=CARTESIAN_POINT('Origin',(27.3495,21.,44.3));
#71398=CARTESIAN_POINT('Origin',(34.75,21.,44.5));
#71399=CARTESIAN_POINT('',(25.25,21.,44.5));
#71400=CARTESIAN_POINT('Origin',(30.,21.,44.5));
#71401=CARTESIAN_POINT('Origin',(30.,21.,45.05));
#71402=CARTESIAN_POINT('',(29.1339745962156,19.5,45.05));
#71403=CARTESIAN_POINT('',(28.2679491924311,21.,45.05));
#71404=CARTESIAN_POINT('',(28.2679491924311,21.,45.05));
#71405=CARTESIAN_POINT('Origin',(30.,21.,45.05));
#71406=CARTESIAN_POINT('Origin',(30.,21.,45.05));
#71407=CARTESIAN_POINT('',(29.1339745962156,22.5,45.05));
#71408=CARTESIAN_POINT('',(29.1339745962156,22.5,45.05));
#71409=CARTESIAN_POINT('Origin',(30.,21.,45.05));
#71410=CARTESIAN_POINT('Origin',(30.,21.,45.05));
#71411=CARTESIAN_POINT('',(30.8660254037844,22.5,45.05));
#71412=CARTESIAN_POINT('',(30.8660254037844,22.5,45.05));
#71413=CARTESIAN_POINT('Origin',(30.,21.,45.05));
#71414=CARTESIAN_POINT('Origin',(30.,21.,45.05));
#71415=CARTESIAN_POINT('',(31.7320508075689,21.,45.05));
#71416=CARTESIAN_POINT('',(31.7320508075689,21.,45.05));
#71417=CARTESIAN_POINT('Origin',(30.,21.,45.05));
#71418=CARTESIAN_POINT('Origin',(30.,21.,45.05));
#71419=CARTESIAN_POINT('',(30.8660254037844,19.5,45.05));
#71420=CARTESIAN_POINT('',(30.8660254037844,19.5,45.05));
#71421=CARTESIAN_POINT('Origin',(30.,21.,45.05));
#71422=CARTESIAN_POINT('Origin',(30.,21.,45.05));
#71423=CARTESIAN_POINT('',(29.1339745962156,19.5,45.05));
#71424=CARTESIAN_POINT('Origin',(30.,21.,45.05));
#71425=CARTESIAN_POINT('Origin',(30.,21.,44.5296394397885));
#71426=CARTESIAN_POINT('',(30.,21.,44.009278879577));
#71427=CARTESIAN_POINT('',(29.1339745962156,21.,44.5296394397885));
#71428=CARTESIAN_POINT('Origin',(29.1339745962156,19.5,47.25));
#71429=CARTESIAN_POINT('',(29.1339745962156,19.5,46.996979834127));
#71430=CARTESIAN_POINT('',(28.2679491924311,21.,46.996979834127));
#71431=CARTESIAN_POINT('Origin',(28.7009618943233,20.25,41.1951086956522));
#71432=CARTESIAN_POINT('',(29.1339745962156,19.5,47.25));
#71433=CARTESIAN_POINT('',(28.2679491924311,21.,47.25));
#71434=CARTESIAN_POINT('Origin',(28.2679491924311,21.,47.25));
#71435=CARTESIAN_POINT('',(29.1339745962156,22.5,46.996979834127));
#71436=CARTESIAN_POINT('Origin',(28.7009618943233,21.75,41.1951086956522));
#71437=CARTESIAN_POINT('',(29.1339745962156,22.5,47.25));
#71438=CARTESIAN_POINT('Origin',(29.1339745962156,22.5,47.25));
#71439=CARTESIAN_POINT('',(30.8660254037844,22.5,46.996979834127));
#71440=CARTESIAN_POINT('Origin',(30.,22.5,41.1951086956522));
#71441=CARTESIAN_POINT('',(30.8660254037844,22.5,47.25));
#71442=CARTESIAN_POINT('Origin',(30.8660254037844,22.5,47.25));
#71443=CARTESIAN_POINT('',(31.7320508075689,21.,46.996979834127));
#71444=CARTESIAN_POINT('Origin',(31.2990381056767,21.75,41.1951086956522));
#71445=CARTESIAN_POINT('',(31.7320508075689,21.,47.25));
#71446=CARTESIAN_POINT('Origin',(30.8660254037844,19.5,47.25));
#71447=CARTESIAN_POINT('',(30.8660254037844,19.5,46.996979834127));
#71448=CARTESIAN_POINT('Origin',(30.,19.5,41.1951086956522));
#71449=CARTESIAN_POINT('',(30.8660254037844,19.5,47.25));
#71450=CARTESIAN_POINT('Origin',(31.7320508075689,21.,47.25));
#71451=CARTESIAN_POINT('Origin',(31.2990381056767,20.25,41.1951086956522));
#71452=CARTESIAN_POINT('Origin',(30.,21.,44.725));
#71453=CARTESIAN_POINT('',(25.25,21.,44.95));
#71454=CARTESIAN_POINT('Origin',(30.,21.,44.95));
#71455=CARTESIAN_POINT('',(25.25,21.,44.725));
#71456=CARTESIAN_POINT('Origin',(30.,21.,41.1951086956522));
#71457=CARTESIAN_POINT('Origin',(30.,21.,41.1951086956522));
#81026=UNCERTAINTY_MEASURE_WITH_UNIT(LENGTH_MEASURE(0.01),#81041,
'DISTANCE_ACCURACY_VALUE',
'Maximum model space distance between geometric entities at asserted c
onnectivities');
#81028=UNCERTAINTY_MEASURE_WITH_UNIT(LENGTH_MEASURE(0.01),#81041,
'DISTANCE_ACCURACY_VALUE',
'Maximum model space distance between geometric entities at asserted c
onnectivities');
#81038=(
GEOMETRIC_REPRESENTATION_CONTEXT(3)
GLOBAL_UNCERTAINTY_ASSIGNED_CONTEXT((#81026))
GLOBAL_UNIT_ASSIGNED_CONTEXT((#81041,#81043,#81044))
REPRESENTATION_CONTEXT('','3D')
);
#81040=(
GEOMETRIC_REPRESENTATION_CONTEXT(3)
GLOBAL_UNCERTAINTY_ASSIGNED_CONTEXT((#81028))
GLOBAL_UNIT_ASSIGNED_CONTEXT((#81041,#81043,#81044))
REPRESENTATION_CONTEXT('','3D')
);
#81041=(
LENGTH_UNIT()
NAMED_UNIT(*)
SI_UNIT(.MILLI.,.METRE.)
);
#81043=(
NAMED_UNIT(*)
PLANE_ANGLE_UNIT()
SI_UNIT($,.RADIAN.)
);
#81044=(
NAMED_UNIT(*)
SI_UNIT($,.STERADIAN.)
SOLID_ANGLE_UNIT()
);
#81054=SHAPE_DEFINITION_REPRESENTATION(#81065,#81138);
#81065=PRODUCT_DEFINITION_SHAPE('',$,#81150);
#81138=SHAPE_REPRESENTATION('',(#16450),#81038);
#81140=PRODUCT_DEFINITION_CONTEXT('part definition',#81175,'design');
#81150=PRODUCT_DEFINITION('ISO 7380-1 - M5 x 8 - 10.9',
'ISO 7380-1 - M5 x 8 - 10.9',#81161,#81140);
#81161=PRODUCT_DEFINITION_FORMATION('',$,#81186);
#81175=APPLICATION_CONTEXT(
'Core Data for Automotive Mechanical Design Process');
#81176=PRODUCT_CONTEXT('part definition',#81175,'mechanical');
#81186=PRODUCT('ISO 7380-1 - M5 x 8 - 10.9',
'ISO 7380-1 - M5 x 8 - 10.9',$,(#81176));
#81197=PRESENTATION_STYLE_ASSIGNMENT((#81208));
#81208=SURFACE_STYLE_USAGE(.BOTH.,#81219);
#81219=SURFACE_SIDE_STYLE('',(#81230));
#81230=SURFACE_STYLE_FILL_AREA(#81241);
#81241=FILL_AREA_STYLE('Opaque(202,206,212)',(#81252));
#81252=FILL_AREA_STYLE_COLOUR('Opaque(202,206,212)',#81263);
#81263=COLOUR_RGB('Opaque(202,206,212)', 0.31764706, 0.68627451, 0.89019608);
ENDSEC;
END-ISO-10303-21;
